ISO-10303-21;
HEADER;
/* Generated by software containing ST-Developer
 * from STEP Tools, Inc. (www.steptools.com) 
 */

FILE_DESCRIPTION(
/* description */ (''),
/* implementation_level */ '2;1');

FILE_NAME(
/* name */ 'Nut_01.step',
/* time_stamp */ '2026-10-04T16:49:01-07:00',
/* author */ (''),
/* organization */ (''),
/* preprocessor_version */ 'ST-DEVELOPER v20.2',
/* originating_system */ 'Autodesk Translation Framework v15.15.0.0',
/* authorisation */ '');

FILE_SCHEMA (('AUTOMOTIVE_DESIGN { 1 0 10303 214 3 1 1 }'));
ENDSEC;

DATA;
#10=MECHANICAL_DESIGN_GEOMETRIC_PRESENTATION_REPRESENTATION('',(#84),#51553);
#60=B_SPLINE_SURFACE_WITH_KNOTS('',3,3,((#31226,#31227,#31228,#31229,#31230,
#31231,#31232,#31233,#31234,#31235,#31236,#31237,#31238,#31239,#31240,#31241,
#31242,#31243,#31244,#31245,#31246,#31247,#31248,#31249,#31250,#31251,#31252,
#31253,#31254,#31255,#31256),(#31257,#31258,#31259,#31260,#31261,#31262,
#31263,#31264,#31265,#31266,#31267,#31268,#31269,#31270,#31271,#31272,#31273,
#31274,#31275,#31276,#31277,#31278,#31279,#31280,#31281,#31282,#31283,#31284,
#31285,#31286,#31287),(#31288,#31289,#31290,#31291,#31292,#31293,#31294,
#31295,#31296,#31297,#31298,#31299,#31300,#31301,#31302,#31303,#31304,#31305,
#31306,#31307,#31308,#31309,#31310,#31311,#31312,#31313,#31314,#31315,#31316,
#31317,#31318),(#31319,#31320,#31321,#31322,#31323,#31324,#31325,#31326,
#31327,#31328,#31329,#31330,#31331,#31332,#31333,#31334,#31335,#31336,#31337,
#31338,#31339,#31340,#31341,#31342,#31343,#31344,#31345,#31346,#31347,#31348,
#31349)),.UNSPECIFIED.,.F.,.F.,.F.,(4,4),(4,1,1,1,1,1,1,1,1,1,1,1,1,1,1,
1,1,1,1,1,1,1,1,1,1,1,1,1,4),(-0.000675443843025915,0.0807213590385511),
(11.8568623789734,12.8271953814412,13.7968529400659,14.7665104986906,15.7361680573154,
16.7058256159401,17.6754831745648,18.6451407331896,19.6147982918143,20.584455850439,
21.5541134090638,22.5237709676885,23.4934285263132,24.4630860849379,25.4327436435627,
26.4024012021874,27.3720587608121,28.3417163194369,29.3113738780616,30.2810314366863,
31.2506889953111,32.2203465539358,33.1900041125605,34.1596616711853,35.12931922981,
36.0989767884347,37.0686343470595,38.0382919056842,39.0079494643089),
 .UNSPECIFIED.);
#61=B_SPLINE_SURFACE_WITH_KNOTS('',3,3,((#31546,#31547,#31548,#31549,#31550,
#31551,#31552,#31553,#31554,#31555,#31556,#31557,#31558,#31559,#31560,#31561,
#31562,#31563,#31564,#31565,#31566,#31567,#31568,#31569,#31570,#31571,#31572,
#31573,#31574,#31575,#31576),(#31577,#31578,#31579,#31580,#31581,#31582,
#31583,#31584,#31585,#31586,#31587,#31588,#31589,#31590,#31591,#31592,#31593,
#31594,#31595,#31596,#31597,#31598,#31599,#31600,#31601,#31602,#31603,#31604,
#31605,#31606,#31607),(#31608,#31609,#31610,#31611,#31612,#31613,#31614,
#31615,#31616,#31617,#31618,#31619,#31620,#31621,#31622,#31623,#31624,#31625,
#31626,#31627,#31628,#31629,#31630,#31631,#31632,#31633,#31634,#31635,#31636,
#31637,#31638),(#31639,#31640,#31641,#31642,#31643,#31644,#31645,#31646,
#31647,#31648,#31649,#31650,#31651,#31652,#31653,#31654,#31655,#31656,#31657,
#31658,#31659,#31660,#31661,#31662,#31663,#31664,#31665,#31666,#31667,#31668,
#31669)),.UNSPECIFIED.,.F.,.F.,.F.,(4,4),(4,1,1,1,1,1,1,1,1,1,1,1,1,1,1,
1,1,1,1,1,1,1,1,1,1,1,1,1,4),(-0.000338746594202325,0.0807654267453605),
(14.3988578448057,15.3687832053423,16.338440763967,17.3080983225917,18.2777558812165,
19.2474134398412,20.2170709984659,21.1867285570907,22.1563861157154,23.1260436743401,
24.0957012329649,25.0653587915896,26.0350163502143,27.0046739088391,27.9743314674638,
28.9439890260885,29.9136465847132,30.883304143338,31.8529617019627,32.8226192605874,
33.7922768192122,34.7619343778369,35.7315919364616,36.7012494950864,37.6709070537111,
38.6405646123358,39.6102221709606,40.5798797295853,41.54953728821),
 .UNSPECIFIED.);
#68=SHAPE_REPRESENTATION_RELATIONSHIP('SRR','None',#51589,#76);
#76=ADVANCED_BREP_SHAPE_REPRESENTATION('',(#93),#51549);
#84=STYLED_ITEM('',(#51634),#93);
#93=MANIFOLD_SOLID_BREP('Body1',#4263);
#108=FACE_BOUND('',#500,.T.);
#109=FACE_BOUND('',#508,.T.);
#149=PLANE('',#4522);
#150=PLANE('',#4523);
#151=PLANE('',#4524);
#152=PLANE('',#4525);
#153=PLANE('',#4526);
#154=PLANE('',#4527);
#155=PLANE('',#4528);
#156=PLANE('',#4529);
#282=FACE_OUTER_BOUND('',#487,.T.);
#283=FACE_OUTER_BOUND('',#488,.T.);
#284=FACE_OUTER_BOUND('',#489,.T.);
#285=FACE_OUTER_BOUND('',#490,.T.);
#286=FACE_OUTER_BOUND('',#491,.T.);
#287=FACE_OUTER_BOUND('',#492,.T.);
#288=FACE_OUTER_BOUND('',#493,.T.);
#289=FACE_OUTER_BOUND('',#494,.T.);
#290=FACE_OUTER_BOUND('',#495,.T.);
#291=FACE_OUTER_BOUND('',#496,.T.);
#292=FACE_OUTER_BOUND('',#497,.T.);
#293=FACE_OUTER_BOUND('',#498,.T.);
#294=FACE_OUTER_BOUND('',#499,.T.);
#295=FACE_OUTER_BOUND('',#501,.T.);
#296=FACE_OUTER_BOUND('',#502,.T.);
#297=FACE_OUTER_BOUND('',#503,.T.);
#298=FACE_OUTER_BOUND('',#504,.T.);
#299=FACE_OUTER_BOUND('',#505,.T.);
#300=FACE_OUTER_BOUND('',#506,.T.);
#301=FACE_OUTER_BOUND('',#507,.T.);
#487=EDGE_LOOP('',(#3297,#3298,#3299,#3300));
#488=EDGE_LOOP('',(#3301,#3302,#3303,#3304,#3305,#3306));
#489=EDGE_LOOP('',(#3307,#3308,#3309,#3310,#3311,#3312));
#490=EDGE_LOOP('',(#3313,#3314,#3315,#3316,#3317,#3318));
#491=EDGE_LOOP('',(#3319,#3320,#3321,#3322,#3323));
#492=EDGE_LOOP('',(#3324,#3325,#3326,#3327,#3328,#3329));
#493=EDGE_LOOP('',(#3330,#3331,#3332,#3333,#3334));
#494=EDGE_LOOP('',(#3335,#3336,#3337,#3338));
#495=EDGE_LOOP('',(#3339,#3340,#3341,#3342,#3343,#3344));
#496=EDGE_LOOP('',(#3345,#3346,#3347,#3348,#3349,#3350));
#497=EDGE_LOOP('',(#3351,#3352,#3353,#3354,#3355,#3356,#3357,#3358,#3359,
#3360,#3361,#3362,#3363,#3364,#3365,#3366,#3367,#3368,#3369));
#498=EDGE_LOOP('',(#3370,#3371,#3372,#3373,#3374,#3375,#3376,#3377,#3378,
#3379,#3380,#3381,#3382,#3383,#3384,#3385,#3386,#3387,#3388,#3389));
#499=EDGE_LOOP('',(#3390,#3391,#3392,#3393,#3394,#3395));
#500=EDGE_LOOP('',(#3396,#3397,#3398,#3399));
#501=EDGE_LOOP('',(#3400,#3401,#3402,#3403));
#502=EDGE_LOOP('',(#3404,#3405,#3406,#3407));
#503=EDGE_LOOP('',(#3408,#3409,#3410,#3411));
#504=EDGE_LOOP('',(#3412,#3413,#3414,#3415));
#505=EDGE_LOOP('',(#3416,#3417,#3418,#3419));
#506=EDGE_LOOP('',(#3420,#3421,#3422,#3423));
#507=EDGE_LOOP('',(#3424,#3425,#3426,#3427,#3428,#3429));
#508=EDGE_LOOP('',(#3430,#3431,#3432,#3433,#3434));
#649=CIRCLE('',#4509,4.08499999999996);
#650=CIRCLE('',#4513,4.08499999999996);
#651=CIRCLE('',#4515,3.38975);
#652=CIRCLE('',#4519,3.38975);
#826=LINE('',#28115,#1054);
#827=LINE('',#28225,#1055);
#828=LINE('',#28597,#1056);
#829=LINE('',#29042,#1057);
#830=LINE('',#29322,#1058);
#831=LINE('',#29503,#1059);
#832=LINE('',#29856,#1060);
#833=LINE('',#30206,#1061);
#834=LINE('',#31864,#1062);
#835=LINE('',#31866,#1063);
#836=LINE('',#31868,#1064);
#837=LINE('',#31870,#1065);
#838=LINE('',#31872,#1066);
#839=LINE('',#31873,#1067);
#840=LINE('',#31876,#1068);
#841=LINE('',#31878,#1069);
#842=LINE('',#31879,#1070);
#843=LINE('',#31882,#1071);
#844=LINE('',#31883,#1072);
#845=LINE('',#31886,#1073);
#846=LINE('',#31887,#1074);
#847=LINE('',#31890,#1075);
#848=LINE('',#31891,#1076);
#849=LINE('',#31894,#1077);
#850=LINE('',#31895,#1078);
#851=LINE('',#31897,#1079);
#1054=VECTOR('',#5090,4.08499999999997);
#1055=VECTOR('',#5095,4.08499999999997);
#1056=VECTOR('',#5098,4.08499999999997);
#1057=VECTOR('',#5101,4.08499999999997);
#1058=VECTOR('',#5106,3.38975);
#1059=VECTOR('',#5111,3.38975);
#1060=VECTOR('',#5114,3.38975);
#1061=VECTOR('',#5117,3.38975);
#1062=VECTOR('',#5126,10.);
#1063=VECTOR('',#5127,10.);
#1064=VECTOR('',#5128,10.);
#1065=VECTOR('',#5129,10.);
#1066=VECTOR('',#5130,10.);
#1067=VECTOR('',#5131,10.);
#1068=VECTOR('',#5134,10.);
#1069=VECTOR('',#5135,10.);
#1070=VECTOR('',#5136,10.);
#1071=VECTOR('',#5139,10.);
#1072=VECTOR('',#5140,10.);
#1073=VECTOR('',#5143,10.);
#1074=VECTOR('',#5144,10.);
#1075=VECTOR('',#5147,10.);
#1076=VECTOR('',#5148,10.);
#1077=VECTOR('',#5151,10.);
#1078=VECTOR('',#5152,10.);
#1079=VECTOR('',#5155,10.);
#1330=B_SPLINE_CURVE_WITH_KNOTS('',3,(#28117,#28118,#28119,#28120,#28121,
#28122),.UNSPECIFIED.,.F.,.F.,(4,1,1,4),(36.7819582801311,37.0686343470595,
38.0382919056842,39.0079494643089),.UNSPECIFIED.);
#1331=B_SPLINE_CURVE_WITH_KNOTS('',3,(#28125,#28126,#28127,#28128,#28129,
#28130,#28131,#28132,#28133,#28134,#28135,#28136,#28137,#28138,#28139,#28140,
#28141,#28142,#28143,#28144,#28145,#28146,#28147,#28148,#28149,#28150,#28151,
#28152,#28153,#28154,#28155,#28156,#28157,#28158,#28159,#28160,#28161,#28162,
#28163,#28164,#28165,#28166,#28167,#28168,#28169,#28170,#28171,#28172,#28173,
#28174,#28175,#28176,#28177,#28178,#28179,#28180,#28181,#28182,#28183,#28184,
#28185,#28186,#28187,#28188,#28189,#28190,#28191,#28192,#28193,#28194,#28195,
#28196,#28197,#28198,#28199,#28200,#28201,#28202,#28203,#28204,#28205,#28206,
#28207,#28208,#28209,#28210,#28211,#28212,#28213,#28214,#28215,#28216,#28217,
#28218,#28219,#28220,#28221),.UNSPECIFIED.,.F.,.F.,(4,3,3,3,3,3,3,3,3,3,
3,3,3,3,3,3,3,3,3,3,3,3,3,3,3,3,3,3,3,3,3,3,4),(36.7829914305774,36.8708819232571,
36.9586870217953,37.0477145257848,37.1354254541176,37.2231243381835,37.31083161634,
37.4008504756827,37.4886815057119,37.5797942797115,37.6709070537111,37.759070730442,
37.847128117236,37.9351017332666,38.0232845931502,38.1111667826965,38.1990374597897,
38.2869168614638,38.3753287991818,38.4633292016657,38.5519469070008,38.6405646123358,
38.7276206141432,38.8145723290877,38.9042341473813,38.9910502374452,39.0778404802797,
39.1646262745643,39.2514290109438,39.3383129672329,39.425245923642,39.5122918403307,
39.5318668754359),.UNSPECIFIED.);
#1332=B_SPLINE_CURVE_WITH_KNOTS('',3,(#28227,#28228,#28229,#28230,#28231,
#28232,#28233,#28234,#28235,#28236,#28237,#28238,#28239,#28240,#28241,#28242,
#28243,#28244,#28245,#28246,#28247,#28248,#28249,#28250,#28251,#28252,#28253,
#28254,#28255,#28256,#28257,#28258,#28259,#28260,#28261,#28262,#28263,#28264,
#28265,#28266,#28267,#28268,#28269,#28270,#28271,#28272,#28273,#28274,#28275,
#28276,#28277,#28278,#28279,#28280,#28281,#28282,#28283,#28284,#28285,#28286,
#28287,#28288,#28289,#28290,#28291,#28292,#28293,#28294,#28295,#28296,#28297,
#28298,#28299,#28300,#28301,#28302,#28303,#28304,#28305,#28306,#28307,#28308,
#28309,#28310,#28311,#28312,#28313,#28314,#28315,#28316,#28317,#28318,#28319,
#28320,#28321,#28322,#28323,#28324,#28325,#28326,#28327,#28328,#28329,#28330,
#28331,#28332,#28333,#28334,#28335,#28336,#28337,#28338,#28339,#28340,#28341,
#28342,#28343,#28344,#28345,#28346,#28347,#28348,#28349,#28350,#28351,#28352,
#28353,#28354,#28355,#28356,#28357,#28358,#28359,#28360,#28361,#28362,#28363,
#28364,#28365,#28366,#28367,#28368),.UNSPECIFIED.,.F.,.F.,(4,3,3,3,3,3,
3,3,3,3,3,3,3,3,3,3,3,3,3,3,3,3,3,3,3,3,3,3,3,3,3,3,3,3,3,3,3,3,3,3,3,3,
3,3,3,3,3,4),(30.4999802413289,30.5878062964545,30.6755881792872,30.7633486037829,
30.8511079442691,30.9388865691735,31.02675362669,31.1146697101077,31.2027123231484,
31.2506889953111,31.3387311548989,31.426666934949,31.5145190110592,31.6027474539188,
31.6905090631315,31.7782597453881,31.8660198781115,31.9546015470676,32.0424855397654,
32.1314160468506,32.2203465539358,32.3084047690471,32.3963565839447,32.4842246535543,
32.5724470859301,32.6602244808093,32.7479908409051,32.8357665249892,32.9243259218821,
33.0122250125786,33.1011145625696,33.1900041125605,33.2780544852982,33.365998586373,
33.4538590783409,33.5420844024465,33.6298545967303,33.71761391022,33.805382708972,
33.8939524495253,33.9818451089349,34.0707533900601,34.1596616711853,34.259126012611,
34.3554308697042,34.4564749532961,34.5521891341409,34.5575190368881),
 .UNSPECIFIED.);
#1333=B_SPLINE_CURVE_WITH_KNOTS('',3,(#28369,#28370,#28371,#28372,#28373,
#28374),.UNSPECIFIED.,.F.,.F.,(4,1,1,4),(34.5575191894877,35.12931922981,
36.0989767884347,36.7819582801311),.UNSPECIFIED.);
#1334=B_SPLINE_CURVE_WITH_KNOTS('',3,(#28376,#28377,#28378,#28379,#28380,
#28381,#28382,#28383,#28384,#28385,#28386,#28387,#28388,#28389,#28390,#28391,
#28392,#28393,#28394,#28395,#28396,#28397,#28398,#28399,#28400,#28401,#28402,
#28403,#28404,#28405,#28406,#28407,#28408,#28409,#28410,#28411,#28412,#28413,
#28414,#28415,#28416,#28417,#28418,#28419,#28420,#28421,#28422,#28423,#28424,
#28425,#28426,#28427,#28428,#28429,#28430,#28431,#28432,#28433,#28434,#28435,
#28436,#28437,#28438,#28439,#28440,#28441,#28442,#28443,#28444,#28445,#28446,
#28447,#28448,#28449,#28450,#28451),.UNSPECIFIED.,.F.,.F.,(4,3,3,3,3,3,
3,3,3,3,3,3,3,3,3,3,3,3,3,3,3,3,3,3,3,4),(34.5575191894877,34.6769472396894,
34.7619343778369,34.8499925930133,34.9379444079826,35.0258124776704,35.1140349100193,
35.2018123049931,35.28957866519,35.3773543493816,35.4659137461516,35.5538128369715,
35.6427023867165,35.7315919364616,35.8196423109753,35.9075864138477,35.9954469076329,
36.0836722310646,36.1714424272047,36.2592017425627,36.3469705431935,36.4355402811667,
36.5234329424662,36.6123412187763,36.7012494950864,36.7829914305774),
 .UNSPECIFIED.);
#1335=B_SPLINE_CURVE_WITH_KNOTS('',3,(#28452,#28453,#28454,#28455,#28456,
#28457,#28458,#28459,#28460,#28461,#28462,#28463,#28464,#28465,#28466,#28467,
#28468,#28469,#28470,#28471,#28472,#28473,#28474,#28475,#28476,#28477,#28478,
#28479,#28480,#28481,#28482,#28483,#28484,#28485,#28486,#28487,#28488,#28489,
#28490,#28491,#28492,#28493,#28494,#28495,#28496,#28497,#28498,#28499,#28500,
#28501,#28502,#28503,#28504,#28505,#28506,#28507,#28508,#28509,#28510,#28511,
#28512,#28513,#28514,#28515,#28516,#28517,#28518,#28519,#28520,#28521,#28522,
#28523,#28524,#28525,#28526,#28527,#28528,#28529,#28530,#28531,#28532,#28533,
#28534,#28535,#28536,#28537,#28538,#28539,#28540,#28541,#28542,#28543,#28544,
#28545,#28546,#28547,#28548,#28549,#28550,#28551,#28552,#28553,#28554,#28555,
#28556,#28557,#28558,#28559,#28560,#28561,#28562,#28563,#28564,#28565,#28566,
#28567,#28568,#28569,#28570,#28571,#28572,#28573,#28574,#28575,#28576,#28577,
#28578,#28579,#28580,#28581,#28582,#28583,#28584,#28585,#28586,#28587,#28588,
#28589,#28590,#28591,#28592,#28593),.UNSPECIFIED.,.F.,.F.,(4,3,3,3,3,3,
3,3,3,3,3,3,3,3,3,3,3,3,3,3,3,3,3,3,3,3,3,3,3,3,3,3,3,3,3,3,3,3,3,3,3,3,
3,3,3,3,3,4),(30.4992051003504,30.586988429761,30.6748619877165,30.7627878035445,
30.8508361315155,30.883304143338,30.971351451518,31.0592923914219,31.1471496318142,
31.2353761405828,31.3231428902903,31.4108986944367,31.4986639243403,31.5872383687459,
31.6751273510732,31.764044526518,31.8529617019627,31.9410103456195,32.0289526183393,
32.1168111872057,32.2050371963784,32.2928052552214,32.3805623588041,32.4683288769244,
32.5569014728401,32.6447917041248,32.7337054823561,32.8226192605874,32.9106680482244,
32.9986104795465,33.0864692212407,33.1746951709871,33.2624634359629,33.350220757762,
33.4379875058746,33.526559834209,33.6144503220714,33.7033635706418,33.7922768192122,
33.8791556016581,33.9659061262488,34.0525836832044,34.139209898208,34.2258063494768,
34.3124246592063,34.3990516191918,34.4857583354495,34.5575191893441),
 .UNSPECIFIED.);
#1336=B_SPLINE_CURVE_WITH_KNOTS('',3,(#28599,#28600,#28601,#28602,#28603,
#28604,#28605,#28606,#28607,#28608,#28609,#28610,#28611,#28612,#28613,#28614,
#28615,#28616,#28617,#28618,#28619,#28620,#28621,#28622,#28623,#28624,#28625,
#28626,#28627,#28628,#28629,#28630,#28631,#28632,#28633,#28634,#28635,#28636,
#28637,#28638,#28639,#28640,#28641,#28642,#28643,#28644,#28645,#28646,#28647,
#28648,#28649,#28650,#28651,#28652,#28653,#28654,#28655,#28656,#28657,#28658,
#28659,#28660,#28661,#28662,#28663,#28664,#28665,#28666,#28667,#28668,#28669,
#28670,#28671,#28672,#28673,#28674,#28675,#28676,#28677,#28678,#28679,#28680,
#28681,#28682,#28683,#28684,#28685,#28686,#28687,#28688,#28689,#28690,#28691,
#28692,#28693,#28694,#28695,#28696,#28697,#28698,#28699,#28700,#28701,#28702,
#28703,#28704,#28705,#28706,#28707,#28708,#28709,#28710,#28711,#28712,#28713,
#28714,#28715,#28716,#28717,#28718,#28719,#28720,#28721,#28722,#28723,#28724,
#28725,#28726,#28727,#28728,#28729,#28730,#28731,#28732,#28733,#28734,#28735,
#28736,#28737,#28738,#28739,#28740),.UNSPECIFIED.,.F.,.F.,(4,3,3,3,3,3,
3,3,3,3,3,3,3,3,3,3,3,3,3,3,3,3,3,3,3,3,3,3,3,3,3,3,3,3,3,3,3,3,3,3,3,3,
3,3,3,3,3,4),(24.2157887599059,24.303689123736,24.3917223366668,24.4630860849379,
24.5511339407958,24.6390754281485,24.7269332150507,24.8151595186147,24.9029268088915,
24.9906831503585,25.0784489136963,25.1670225961629,25.2549120974833,25.343827870523,
25.4327436435627,25.5207914947271,25.6087329783038,25.6965907623439,25.7848170673243,
25.8725843569884,25.9603406986909,26.0481064631111,26.1366801478801,26.224569652357,
26.3134854272722,26.4024012021874,26.4904491403875,26.5783907104697,26.6662485803799,
26.754474852934,26.8422422263594,26.9299986508759,27.0177644970671,27.1063380630033,
27.1942276459502,27.2831432033812,27.3720587608121,27.4592850110154,27.5464051922551,
27.63739627849,27.7243753691936,27.811326806192,27.8982718392512,27.985231708504,
28.0722711378777,28.1593574305664,28.2465577551069,28.2743338821347),
 .UNSPECIFIED.);
#1337=B_SPLINE_CURVE_WITH_KNOTS('',3,(#28741,#28742,#28743,#28744,#28745,
#28746,#28747,#28748,#28749,#28750,#28751,#28752,#28753,#28754,#28755,#28756,
#28757,#28758,#28759,#28760,#28761,#28762,#28763,#28764,#28765,#28766,#28767,
#28768,#28769,#28770,#28771,#28772,#28773,#28774,#28775,#28776,#28777,#28778,
#28779,#28780,#28781,#28782,#28783,#28784,#28785,#28786,#28787,#28788,#28789,
#28790,#28791,#28792,#28793,#28794,#28795,#28796,#28797,#28798,#28799,#28800,
#28801,#28802,#28803,#28804,#28805,#28806,#28807,#28808,#28809,#28810,#28811,
#28812,#28813,#28814,#28815,#28816,#28817,#28818,#28819),.UNSPECIFIED.,
 .F.,.F.,(4,3,3,3,3,3,3,3,3,3,3,3,3,3,3,3,3,3,3,3,3,3,3,3,3,3,4),(28.2743338823081,
28.3417163194369,28.429763627663,28.5177045676132,28.6055618080517,28.6937883168029,
28.7815550665564,28.8693108707486,28.9570761006978,29.0456505450387,29.1335395274105,
29.2224567027361,29.3113738780616,29.3994225216949,29.4873647943923,29.575223363237,
29.6634493724182,29.7512174312415,29.8389745348052,29.9267410529077,30.0153136488524,
30.1032038801215,30.1921176584039,30.2810314366863,30.3690856030647,30.4570218464002,
30.4999802413289),.UNSPECIFIED.);
#1338=B_SPLINE_CURVE_WITH_KNOTS('',3,(#28821,#28822,#28823,#28824,#28825,
#28826,#28827,#28828,#28829,#28830,#28831,#28832,#28833,#28834,#28835,#28836,
#28837,#28838,#28839,#28840,#28841,#28842,#28843,#28844,#28845,#28846,#28847,
#28848,#28849,#28850,#28851,#28852,#28853,#28854,#28855,#28856,#28857,#28858,
#28859,#28860,#28861,#28862,#28863,#28864,#28865,#28866,#28867,#28868,#28869,
#28870,#28871,#28872,#28873,#28874,#28875,#28876,#28877,#28878,#28879,#28880,
#28881,#28882,#28883,#28884,#28885,#28886,#28887,#28888,#28889,#28890,#28891,
#28892,#28893,#28894,#28895,#28896,#28897,#28898,#28899),.UNSPECIFIED.,
 .F.,.F.,(4,3,3,3,3,3,3,3,3,3,3,3,3,3,3,3,3,3,3,3,3,3,3,3,3,3,4),(28.2743338823081,
28.3617389036755,28.4491201917934,28.5364985207119,28.6238946573556,28.711380340344,
28.7989143739467,28.8865805773436,28.9439890260885,29.0320369642888,29.1199785343708,
29.2078364042814,29.2960626768354,29.3838300502608,29.4715864747772,29.5593523209684,
29.6479258869046,29.7358154698515,29.8247310272824,29.9136465847132,30.0016844203211,
30.089621717054,30.177479011169,30.2652759791166,30.3530368519356,30.4407979020362,
30.4992051003504),.UNSPECIFIED.);
#1339=B_SPLINE_CURVE_WITH_KNOTS('',3,(#28900,#28901,#28902,#28903,#28904,
#28905,#28906,#28907,#28908,#28909,#28910,#28911,#28912,#28913,#28914,#28915,
#28916,#28917,#28918,#28919,#28920,#28921,#28922,#28923,#28924,#28925,#28926,
#28927,#28928,#28929,#28930,#28931,#28932,#28933,#28934,#28935,#28936,#28937,
#28938,#28939,#28940,#28941,#28942,#28943,#28944,#28945,#28946,#28947,#28948,
#28949,#28950,#28951,#28952,#28953,#28954,#28955,#28956,#28957,#28958,#28959,
#28960,#28961,#28962,#28963,#28964,#28965,#28966,#28967,#28968,#28969,#28970,
#28971,#28972,#28973,#28974,#28975,#28976,#28977,#28978,#28979,#28980,#28981,
#28982,#28983,#28984,#28985,#28986,#28987,#28988,#28989,#28990,#28991,#28992,
#28993,#28994,#28995,#28996,#28997,#28998,#28999,#29000,#29001,#29002,#29003,
#29004,#29005,#29006,#29007,#29008,#29009,#29010,#29011,#29012,#29013,#29014,
#29015,#29016,#29017,#29018,#29019,#29020,#29021,#29022,#29023,#29024,#29025,
#29026,#29027,#29028,#29029,#29030,#29031,#29032,#29033,#29034,#29035,#29036,
#29037,#29038),.UNSPECIFIED.,.F.,.F.,(4,3,3,3,3,3,3,3,3,3,3,3,3,3,3,3,3,
3,3,3,3,3,3,3,3,3,3,3,3,3,3,3,3,3,3,3,3,3,3,3,3,3,3,3,3,3,4),(24.2167210304736,
24.3046279764685,24.3924596906217,24.4802438127573,24.5680041412365,24.6557610538041,
24.7435349206615,24.8313960220632,24.9193040568845,25.0073412999443,25.0653587915896,
25.1534068139401,25.2413484697431,25.3292064268125,25.4174326672377,25.5052001307177,
25.592956646202,25.6807225841602,25.7692960256737,25.857185701481,25.9461010258477,
26.0350163502143,26.1230642813644,26.2110058457738,26.2988637113841,26.387089986066,
26.474857358571,26.5626137834407,26.6503796312588,26.7389532006539,26.8268427883422,
26.9157583485906,27.0046739088391,27.0927217646944,27.1806632520445,27.2685210389441,
27.3567473425091,27.444514632783,27.5322709742474,27.6200367375818,27.7086104200523,
27.7964999213698,27.8854156944168,27.9743314674638,28.0790231847901,28.1827305263691,
28.2743338820653),.UNSPECIFIED.);
#1340=B_SPLINE_CURVE_WITH_KNOTS('',3,(#29044,#29045,#29046,#29047,#29048,
#29049,#29050,#29051,#29052,#29053,#29054,#29055,#29056,#29057,#29058,#29059,
#29060,#29061,#29062,#29063,#29064,#29065,#29066,#29067,#29068,#29069,#29070,
#29071,#29072,#29073,#29074,#29075,#29076,#29077,#29078,#29079,#29080,#29081,
#29082,#29083,#29084,#29085,#29086,#29087,#29088,#29089,#29090,#29091,#29092,
#29093,#29094,#29095,#29096,#29097,#29098,#29099,#29100,#29101,#29102,#29103,
#29104,#29105,#29106,#29107,#29108,#29109,#29110,#29111,#29112,#29113,#29114,
#29115,#29116,#29117,#29118,#29119,#29120,#29121,#29122),.UNSPECIFIED.,
 .F.,.F.,(4,3,3,3,3,3,3,3,3,3,3,3,3,3,3,3,3,3,3,3,3,3,3,3,3,3,4),(15.707963267949,
15.7957710138543,15.8835745324552,15.9713940336816,16.063155716253,16.1511191802592,
16.2391470622587,16.3273025206811,16.338440763967,16.4264705709007,16.5143915318638,
16.6022263810891,16.6904603737769,16.7781990734251,16.8659247701018,16.9536578857083,
17.0422679949292,17.1301202964837,17.2191093095377,17.3080983225917,17.3962407088205,
17.4842848625976,17.5722511788473,17.6623720645742,17.7502488322418,17.8414917769983,
17.9327347217548),.UNSPECIFIED.);
#1341=B_SPLINE_CURVE_WITH_KNOTS('',3,(#29124,#29125,#29126,#29127,#29128,
#29129,#29130,#29131,#29132,#29133,#29134,#29135,#29136,#29137,#29138,#29139,
#29140,#29141,#29142,#29143,#29144,#29145,#29146,#29147,#29148,#29149,#29150,
#29151,#29152,#29153,#29154,#29155,#29156,#29157,#29158,#29159,#29160,#29161,
#29162,#29163,#29164,#29165,#29166,#29167,#29168,#29169),.UNSPECIFIED.,
 .F.,.F.,(4,3,3,3,3,3,3,3,3,3,3,3,3,3,3,4),(14.3991256467175,14.4887372625192,
14.5782938203675,14.6678142643898,14.7573380508082,14.846866749863,14.9364175372311,
15.0260076033398,15.1157142880607,15.2054812603592,15.2953997278843,15.3687832053423,
15.4680291464829,15.5669343832768,15.6652600362453,15.7079632677411),
 .UNSPECIFIED.);
#1342=B_SPLINE_CURVE_WITH_KNOTS('',3,(#29173,#29174,#29175,#29176,#29177,
#29178,#29179,#29180,#29181,#29182,#29183,#29184,#29185,#29186,#29187,#29188,
#29189,#29190,#29191,#29192,#29193,#29194,#29195,#29196,#29197,#29198,#29199,
#29200,#29201,#29202,#29203,#29204,#29205,#29206,#29207,#29208,#29209,#29210,
#29211,#29212,#29213,#29214,#29215,#29216,#29217,#29218,#29219,#29220,#29221,
#29222,#29223,#29224,#29225,#29226,#29227,#29228,#29229,#29230,#29231,#29232,
#29233,#29234,#29235,#29236,#29237,#29238,#29239),.UNSPECIFIED.,.F.,.F.,
(4,3,3,3,3,3,3,3,3,3,3,3,3,3,3,3,3,3,3,3,3,3,4),(13.8752082355906,13.9622520542611,
14.0491941465953,14.1388586906072,14.2256715524859,14.3124609367983,14.3992482407091,
14.4860548552488,14.5729461563241,14.6598884952872,14.7469466691964,14.7665104986906,
14.8542641117252,14.9419129820413,15.0294801549438,15.1169913640356,15.2044736406601,
15.2919477097064,15.3794342851205,15.4670040516123,15.5546174446298,15.642360377797,
15.7079632677762),.UNSPECIFIED.);
#1343=B_SPLINE_CURVE_WITH_KNOTS('',3,(#29240,#29241,#29242,#29243,#29244,
#29245,#29246,#29247,#29248,#29249,#29250,#29251,#29252,#29253,#29254,#29255,
#29256,#29257,#29258,#29259,#29260,#29261,#29262,#29263,#29264,#29265,#29266,
#29267,#29268,#29269,#29270,#29271,#29272,#29273,#29274,#29275,#29276,#29277,
#29278,#29279,#29280,#29281,#29282,#29283,#29284,#29285,#29286,#29287,#29288,
#29289,#29290,#29291,#29292,#29293,#29294,#29295,#29296,#29297,#29298,#29299,
#29300,#29301,#29302,#29303,#29304,#29305,#29306,#29307,#29308,#29309,#29310,
#29311,#29312,#29313,#29314,#29315,#29316,#29317,#29318),.UNSPECIFIED.,
 .F.,.F.,(4,3,3,3,3,3,3,3,3,3,3,3,3,3,3,3,3,3,3,3,3,3,3,3,3,3,4),(15.707963267949,
15.7361680573154,15.8241610831544,15.9120470328636,15.9998486521347,16.0880957726104,
16.1758057263136,16.2635043973197,16.3512122236995,16.4398655717597,16.5276970079318,
16.616761311936,16.7058256159401,16.7938766861026,16.8818213483134,16.9696822656569,
17.0579073792704,17.1456776645914,17.2334369431071,17.3212055808951,17.4097749793125,
17.4976671696677,17.5865751721162,17.6754831745648,17.7635369171519,17.8514734423075,
17.9335803047654),.UNSPECIFIED.);
#1344=B_SPLINE_CURVE_WITH_KNOTS('',3,(#29324,#29325,#29326,#29327,#29328,
#29329,#29330,#29331,#29332,#29333,#29334,#29335,#29336,#29337,#29338,#29339,
#29340,#29341,#29342,#29343,#29344,#29345,#29346,#29347,#29348,#29349,#29350,
#29351,#29352,#29353,#29354,#29355,#29356,#29357,#29358,#29359,#29360,#29361,
#29362,#29363,#29364,#29365,#29366,#29367,#29368,#29369,#29370,#29371,#29372,
#29373,#29374,#29375,#29376,#29377,#29378,#29379,#29380,#29381,#29382,#29383,
#29384,#29385,#29386,#29387,#29388,#29389,#29390),.UNSPECIFIED.,.F.,.F.,
(4,3,3,3,3,3,3,3,3,3,3,3,3,3,3,3,3,3,3,3,3,3,4),(24.5162658903767,24.6082166985082,
24.7001384561039,24.7920546616798,24.8839888029008,24.9760185491963,25.0681011382561,
25.1603243519034,25.211096524243,25.3029055078245,25.3945969257777,25.4861975074927,
25.5777382907594,25.6692490484609,25.7607538070406,25.852276581861,25.9438972266317,
26.0355716555317,26.1273911794012,26.1807540828677,26.3014629469111,26.419796833611,
26.4415677385481),.UNSPECIFIED.);
#1345=B_SPLINE_CURVE_WITH_KNOTS('',3,(#29392,#29393,#29394,#29395,#29396,
#29397,#29398,#29399,#29400,#29401,#29402,#29403,#29404,#29405,#29406,#29407,
#29408,#29409),.UNSPECIFIED.,.F.,.F.,(4,2,2,2,2,2,2,2,4),(-0.241287041643189,
-0.201278706532095,-0.169751970886667,-0.147404851836541,-0.120690417364664,
-0.0894452412599869,-0.0185648330825772,-0.00833841566500538,0.),
 .UNSPECIFIED.);
#1346=B_SPLINE_CURVE_WITH_KNOTS('',3,(#29412,#29413,#29414,#29415,#29416,
#29417,#29418,#29419,#29420,#29421,#29422,#29423,#29424,#29425,#29426,#29427,
#29428,#29429,#29430,#29431,#29432,#29433,#29434,#29435,#29436,#29437,#29438,
#29439,#29440,#29441,#29442,#29443,#29444,#29445,#29446,#29447,#29448,#29449,
#29450,#29451,#29452,#29453,#29454,#29455,#29456,#29457,#29458,#29459,#29460,
#29461,#29462,#29463,#29464,#29465,#29466,#29467,#29468,#29469,#29470,#29471,
#29472,#29473,#29474,#29475,#29476,#29477,#29478,#29479,#29480,#29481,#29482,
#29483,#29484,#29485,#29486,#29487,#29488,#29489,#29490,#29491,#29492,#29493,
#29494,#29495,#29496,#29497,#29498,#29499),.UNSPECIFIED.,.F.,.F.,(4,2,2,
2,2,2,2,2,2,2,2,2,2,2,2,2,2,2,2,2,2,2,2,2,2,2,2,2,2,2,2,2,2,2,2,2,2,2,2,
2,2,2,2,4),(-2.95683205450919,-2.86790352209954,-2.83680152208547,-2.81554813900449,
-2.79126588069924,-2.72638080838598,-2.69160704482108,-2.66872106054633,
-2.65615319116664,-2.64105148047836,-2.56539716564425,-2.51854787912015,
-2.49584443926592,-2.47409451419977,-2.43754352803279,-2.36406204816355,
-2.34011675234167,-2.32748571753471,-2.31302440587022,-2.24660389965472,
-2.20875882479134,-2.17909299647199,-2.15819216538313,-2.13388645412246,
-2.05870209572999,-2.0158818595516,-2.00158111968677,-1.98895608666696,
-1.96546548961181,-1.90449453714366,-1.8590959800648,-1.8365639919602,-1.81484042688886,
-1.77798281779561,-1.70491213313605,-1.6810549345542,-1.66845638116302,
-1.65394117366334,-1.61494840554818,-1.56104678509474,-1.52528634866078,
-1.50368686658543,-1.48099447654482,-1.48084820763969),.UNSPECIFIED.);
#1347=B_SPLINE_CURVE_WITH_KNOTS('',3,(#29505,#29506,#29507,#29508,#29509,
#29510,#29511,#29512,#29513,#29514,#29515,#29516,#29517,#29518,#29519,#29520,
#29521,#29522,#29523,#29524,#29525,#29526,#29527,#29528,#29529,#29530,#29531,
#29532,#29533,#29534,#29535,#29536,#29537,#29538,#29539,#29540,#29541,#29542,
#29543,#29544,#29545,#29546,#29547,#29548,#29549,#29550,#29551,#29552,#29553,
#29554,#29555,#29556,#29557,#29558,#29559,#29560,#29561,#29562,#29563,#29564,
#29565,#29566,#29567,#29568,#29569,#29570,#29571),.UNSPECIFIED.,.F.,.F.,
(4,3,3,3,3,3,3,3,3,3,3,3,3,3,3,3,3,3,3,3,3,3,4),(18.2320682153439,18.3277809146069,
18.4234936138699,18.5157463972682,18.6078830172538,18.6999295422289,18.7919154110862,
18.8838705252868,18.9758183248721,19.0677822376285,19.1598383932109,19.25194573998,
19.3441899321623,19.3931511724946,19.4888064687578,19.5796902392352,19.6704968772054,
19.7612512482406,19.8519781640647,19.9427327251429,20.0335034792163,20.1243541251064,
20.1583935426),.UNSPECIFIED.);
#1348=B_SPLINE_CURVE_WITH_KNOTS('',3,(#29572,#29573,#29574,#29575,#29576,
#29577,#29578,#29579,#29580,#29581,#29582,#29583,#29584,#29585,#29586,#29587,
#29588,#29589,#29590,#29591,#29592,#29593,#29594,#29595,#29596,#29597,#29598,
#29599,#29600,#29601,#29602,#29603,#29604,#29605,#29606,#29607,#29608,#29609,
#29610,#29611,#29612,#29613,#29614,#29615,#29616,#29617,#29618,#29619,#29620,
#29621,#29622,#29623,#29624,#29625,#29626,#29627,#29628,#29629,#29630,#29631,
#29632,#29633,#29634,#29635,#29636,#29637,#29638,#29639,#29640,#29641,#29642,
#29643,#29644,#29645,#29646,#29647,#29648,#29649,#29650,#29651,#29652,#29653,
#29654,#29655,#29656,#29657,#29658,#29659,#29660,#29661,#29662,#29663,#29664,
#29665,#29666,#29667,#29668,#29669,#29670,#29671,#29672,#29673,#29674,#29675,
#29676,#29677,#29678,#29679,#29680,#29681,#29682,#29683,#29684,#29685,#29686,
#29687,#29688,#29689,#29690,#29691,#29692,#29693,#29694,#29695,#29696,#29697,
#29698,#29699,#29700,#29701,#29702,#29703,#29704,#29705,#29706,#29707,#29708,
#29709,#29710,#29711,#29712,#29713,#29714,#29715,#29716,#29717,#29718,#29719),
 .UNSPECIFIED.,.F.,.F.,(4,3,3,3,3,3,3,3,3,3,3,3,3,3,3,3,3,3,3,3,3,3,3,3,
3,3,3,3,3,3,3,3,3,3,3,3,3,3,3,3,3,3,3,3,3,3,3,3,3,4),(20.1583935427702,
20.2835238295359,20.3628087311194,20.4550713921864,20.5472178413458,20.6392741334725,
20.7312696360706,20.82323429651,20.9151915425651,21.0071647896763,21.0992300537185,
21.1913463922247,21.2835993107372,21.3324662897441,21.4247207357871,21.5168591112654,
21.6089074798315,21.7008953116684,21.7928524611761,21.8848023644005,21.9767684451869,
22.0688268502357,22.1609364952792,22.2531830376279,22.3021238483688,22.3943152466139,
22.4863902988358,22.5783751618252,22.6702994876033,22.7621931622762,22.8540797045629,
22.945982621076,23.0379785399895,23.130026004017,23.222211422785,23.2717814069936,
23.3641545650046,23.4564116286072,23.5485784965439,23.6406840587817,23.7327584028345,
23.8248248167588,23.9169065758691,24.0090787190171,24.1013011415748,24.193657934791,
24.2414389656183,24.3336416928871,24.4257215341127,24.5162658903767),
 .UNSPECIFIED.);
#1349=B_SPLINE_CURVE_WITH_KNOTS('',3,(#29721,#29722,#29723,#29724,#29725,
#29726,#29727,#29728,#29729,#29730,#29731,#29732,#29733,#29734,#29735,#29736,
#29737,#29738,#29739,#29740,#29741,#29742,#29743,#29744,#29745,#29746,#29747,
#29748,#29749,#29750,#29751,#29752,#29753,#29754,#29755,#29756,#29757,#29758,
#29759,#29760,#29761,#29762,#29763,#29764,#29765,#29766,#29767,#29768,#29769,
#29770,#29771,#29772,#29773,#29774,#29775,#29776,#29777,#29778,#29779,#29780,
#29781,#29782,#29783,#29784,#29785,#29786,#29787,#29788,#29789,#29790,#29791,
#29792,#29793,#29794,#29795,#29796,#29797,#29798,#29799,#29800,#29801,#29802,
#29803,#29804,#29805,#29806,#29807,#29808,#29809,#29810,#29811,#29812),
 .UNSPECIFIED.,.F.,.F.,(4,2,2,2,2,2,2,2,2,2,2,2,2,2,2,2,2,2,2,2,2,2,2,2,
2,2,2,2,2,2,2,2,2,2,2,2,2,2,2,2,2,2,2,2,2,4),(-1.48084820763969,-1.43329533170974,
-1.37132751089461,-1.35010317640515,-1.33794394056275,-1.32265784737522,
-1.30412790396548,-1.26164454881705,-1.20350041856723,-1.1802595174912,
-1.15895538514111,-1.12582808339709,-1.06670722704322,-1.02838445314857,
-1.01388575701412,-1.00131160682934,-0.977558379347592,-0.905174625587634,
-0.867656378337848,-0.845873370891219,-0.82346873664529,-0.779447826705011,
-0.699291096654322,-0.684670886669094,-0.672141558145518,-0.648769291765022,
-0.578828284061989,-0.539347239257186,-0.517362300251839,-0.495202218953017,
-0.453916966488133,-0.376883831426887,-0.359114276288713,-0.347065989059489,
-0.3294347080856,-0.3065446534078,-0.234282136893858,-0.203602891856948,
-0.182535210417779,-0.15847243035184,-0.131761322573367,-0.0735433135885103,
-0.0387754740265174,-0.0248091469507901,-0.0134569621051135,-0.000876788281526703),
 .UNSPECIFIED.);
#1350=B_SPLINE_CURVE_WITH_KNOTS('',3,(#29813,#29814,#29815,#29816,#29817,
#29818,#29819,#29820,#29821,#29822,#29823,#29824,#29825,#29826,#29827,#29828,
#29829,#29830,#29831,#29832,#29833,#29834,#29835,#29836,#29837,#29838,#29839,
#29840,#29841,#29842,#29843,#29844,#29845,#29846,#29847,#29848,#29849,#29850,
#29851,#29852),.UNSPECIFIED.,.F.,.F.,(4,2,2,2,2,2,2,2,2,2,2,2,2,2,2,2,2,
2,2,4),(-4.27008307975396,-4.19036405881084,-4.1501032589128,-4.12803790197118,
-4.10595437322849,-4.06549781421076,-3.99675679471902,-3.97357760736626,
-3.9610709666391,-3.94639393247533,-3.90500558091448,-3.85292088405322,
-3.81773409769697,-3.79619916165051,-3.77340722906428,-3.68808992672072,
-3.64942509893504,-3.63532334730152,-3.62253225736476,-3.61563567609935),
 .UNSPECIFIED.);
#1351=B_SPLINE_CURVE_WITH_KNOTS('',3,(#29858,#29859,#29860,#29861,#29862,
#29863,#29864,#29865,#29866,#29867,#29868,#29869,#29870,#29871,#29872,#29873,
#29874,#29875,#29876,#29877,#29878,#29879,#29880,#29881,#29882,#29883,#29884,
#29885,#29886,#29887,#29888,#29889,#29890,#29891,#29892,#29893,#29894,#29895,
#29896,#29897,#29898,#29899,#29900,#29901,#29902,#29903,#29904,#29905,#29906,
#29907,#29908,#29909,#29910,#29911,#29912,#29913,#29914,#29915,#29916,#29917,
#29918,#29919,#29920,#29921),.UNSPECIFIED.,.F.,.F.,(4,3,3,3,3,3,3,3,3,3,
3,3,3,3,3,3,3,3,3,3,3,4),(11.9498038827978,12.0417734588683,12.1337218267211,
12.2256724204771,12.3206413808882,12.4127165016283,12.5091323818749,12.6055482621215,
12.6978000692492,12.7899356996167,12.8819812232005,12.9739660775169,13.0659201695579,
13.1578669407371,13.249829820208,13.3418849413676,13.4339912517699,13.5262344142757,
13.5752058207462,13.6848961706205,13.7935323056319,13.8752082353862),
 .UNSPECIFIED.);
#1352=B_SPLINE_CURVE_WITH_KNOTS('',3,(#29922,#29923,#29924,#29925,#29926,
#29927,#29928,#29929,#29930,#29931,#29932,#29933,#29934,#29935,#29936,#29937,
#29938,#29939,#29940,#29941,#29942,#29943,#29944,#29945,#29946,#29947,#29948,
#29949,#29950,#29951,#29952,#29953,#29954,#29955,#29956,#29957,#29958,#29959,
#29960,#29961,#29962,#29963,#29964,#29965,#29966,#29967,#29968,#29969,#29970,
#29971,#29972,#29973,#29974,#29975,#29976,#29977,#29978,#29979,#29980,#29981,
#29982,#29983,#29984,#29985,#29986,#29987,#29988,#29989,#29990,#29991,#29992,
#29993,#29994,#29995,#29996,#29997,#29998,#29999,#30000,#30001,#30002,#30003,
#30004,#30005,#30006,#30007,#30008,#30009,#30010,#30011,#30012,#30013,#30014,
#30015,#30016,#30017,#30018,#30019,#30020,#30021,#30022,#30023,#30024,#30025,
#30026,#30027,#30028,#30029,#30030,#30031,#30032,#30033,#30034,#30035,#30036,
#30037,#30038,#30039,#30040,#30041,#30042,#30043,#30044,#30045,#30046,#30047,
#30048,#30049,#30050,#30051,#30052,#30053,#30054,#30055,#30056,#30057,#30058,
#30059,#30060,#30061,#30062,#30063,#30064,#30065,#30066,#30067,#30068,#30069,
#30070,#30071,#30072),.UNSPECIFIED.,.F.,.F.,(4,3,3,3,3,3,3,3,3,3,3,3,3,
3,3,3,3,3,3,3,3,3,3,3,3,3,3,3,3,3,3,3,3,3,3,3,3,3,3,3,3,3,3,3,3,3,3,3,3,
3,4),(13.8752082355906,13.966786515321,14.0583392857893,14.1498904407232,
14.2414638661191,14.3331348167784,14.4248632482533,14.5167262289635,14.544863379371,
14.6371152727752,14.7292509898415,14.8212966004213,14.9132815418156,15.0052357209429,
15.0971825791062,15.1891455453485,15.2812007524455,15.3733071484209,15.4655503951418,
15.5145209379957,15.6067729212884,15.6989087296117,15.7909544326659,15.8829394679299,
15.9748937417402,16.0668406952681,16.1588037574262,16.2508590606815,16.3429655530728,
16.4352088956974,16.4841784966204,16.5764297299234,16.6685647867363,16.7606097378519,
16.8525940237409,16.9445475501442,17.0364937592073,17.1284560808191,17.2205106539199,
17.3126164211333,17.404859053096,17.4538360552452,17.5461006300452,17.6382219581942,
17.7302613152847,17.8222422297013,17.9141881766539,18.0061482785894,18.0981158143603,
18.1901507760465,18.2320682153439),.UNSPECIFIED.);
#1353=B_SPLINE_CURVE_WITH_KNOTS('',3,(#30073,#30074,#30075,#30076,#30077,
#30078,#30079,#30080,#30081,#30082,#30083,#30084,#30085,#30086,#30087,#30088,
#30089,#30090,#30091,#30092,#30093,#30094,#30095,#30096,#30097,#30098,#30099,
#30100,#30101,#30102,#30103,#30104,#30105,#30106,#30107,#30108,#30109,#30110,
#30111,#30112,#30113,#30114,#30115,#30116,#30117,#30118,#30119,#30120,#30121,
#30122,#30123,#30124,#30125,#30126,#30127,#30128,#30129,#30130,#30131,#30132,
#30133,#30134,#30135,#30136,#30137,#30138,#30139,#30140,#30141,#30142,#30143,
#30144,#30145,#30146,#30147,#30148,#30149,#30150,#30151,#30152,#30153,#30154,
#30155,#30156,#30157,#30158,#30159,#30160,#30161,#30162,#30163,#30164,#30165,
#30166,#30167,#30168,#30169,#30170,#30171,#30172,#30173,#30174,#30175,#30176,
#30177,#30178,#30179,#30180,#30181,#30182,#30183,#30184,#30185,#30186,#30187,
#30188,#30189,#30190,#30191,#30192,#30193,#30194,#30195,#30196,#30197,#30198,
#30199,#30200,#30201,#30202),.UNSPECIFIED.,.F.,.F.,(4,2,2,2,2,2,2,2,2,2,
2,2,2,2,2,2,2,2,2,2,2,2,2,2,2,2,2,2,2,2,2,2,2,2,2,2,2,2,2,2,2,2,2,2,2,2,
2,2,2,2,2,2,2,2,2,2,2,2,2,2,2,2,2,2,4),(-3.61563567609935,-3.59707278652811,
-3.53670443164277,-3.4927916853173,-3.47039092706641,-3.44859865477452,
-3.41101756909211,-3.34862210908414,-3.32688633479163,-3.3098501478452,
-3.29778510175537,-3.27934071796878,-3.20328579142537,-3.16216848920136,
-3.14002029114605,-3.11801718888111,-3.07837698961676,-3.01848227903406,
-2.99707669182181,-2.98021466254453,-2.96814092523396,-2.94947755048121,
-2.87375295013127,-2.83269831188747,-2.81055657012403,-2.78854856362336,
-2.74885436654806,-2.67920456151832,-2.6558792618633,-2.64335492463655,
-2.62872161719908,-2.58676161681923,-2.5294746957831,-2.49745588185999,
-2.47625631513722,-2.45267124683846,-2.37896921866108,-2.34718790487122,
-2.32547563260878,-2.3131417310094,-2.29796159310292,-2.23913679044331,
-2.18003244284178,-2.1563477812173,-2.13518234071414,-2.10347915092546,
-2.06095557425161,-2.00579933929683,-1.99031568667032,-1.97806024715624,
-1.95707054386516,-1.92701113996785,-1.84865166362859,-1.82552256914947,
-1.80415534906218,-1.77051479778477,-1.72293991708584,-1.67699779514533,
-1.66125849499533,-1.64916906903982,-1.62885690363851,-1.60035004587229,
-1.52232246792104,-1.49831885547463,-1.48105208187109),.UNSPECIFIED.);
#1354=B_SPLINE_CURVE_WITH_KNOTS('',3,(#30208,#30209,#30210,#30211,#30212,
#30213,#30214,#30215,#30216,#30217,#30218,#30219,#30220,#30221,#30222,#30223,
#30224,#30225,#30226,#30227,#30228,#30229,#30230,#30231,#30232,#30233,#30234,
#30235,#30236,#30237,#30238,#30239,#30240,#30241,#30242,#30243,#30244,#30245,
#30246,#30247,#30248,#30249,#30250,#30251,#30252,#30253,#30254,#30255,#30256,
#30257,#30258,#30259,#30260,#30261,#30262,#30263,#30264,#30265,#30266,#30267,
#30268,#30269,#30270,#30271,#30272,#30273,#30274),.UNSPECIFIED.,.F.,.F.,
(4,3,3,3,3,3,3,3,3,3,3,3,3,3,3,3,3,3,3,3,3,3,4),(-1.92436839018911,-1.83258031210896,
-1.74090544344235,-1.64932058448165,-1.55778627637879,-1.46627808473474,
-1.37477198624503,-1.28324396560501,-1.19161600512138,-1.09993074983352,
-1.00810461130262,-0.96965755862473,-0.875424683643867,-0.781323325762907,
-0.683657910042544,-0.589768614211507,-0.495936151858874,-0.402140717131423,
-0.308362541712838,-0.214555248867951,-0.120731767065434,-0.0268415123618111,
0.),.UNSPECIFIED.);
#1355=B_SPLINE_CURVE_WITH_KNOTS('',3,(#30277,#30278,#30279,#30280,#30281,
#30282,#30283,#30284,#30285,#30286,#30287,#30288,#30289,#30290,#30291,#30292,
#30293,#30294,#30295,#30296,#30297,#30298,#30299,#30300,#30301,#30302,#30303,
#30304,#30305,#30306,#30307,#30308,#30309,#30310,#30311,#30312,#30313,#30314,
#30315,#30316,#30317,#30318,#30319,#30320,#30321,#30322,#30323,#30324,#30325,
#30326,#30327,#30328,#30329,#30330,#30331,#30332,#30333,#30334,#30335,#30336,
#30337,#30338,#30339,#30340,#30341,#30342,#30343,#30344,#30345,#30346,#30347,
#30348,#30349,#30350,#30351,#30352,#30353,#30354,#30355,#30356,#30357,#30358,
#30359,#30360,#30361,#30362,#30363,#30364,#30365,#30366,#30367,#30368,#30369,
#30370,#30371,#30372,#30373,#30374,#30375,#30376,#30377,#30378,#30379,#30380,
#30381,#30382,#30383,#30384,#30385,#30386,#30387,#30388,#30389,#30390,#30391,
#30392,#30393,#30394,#30395,#30396,#30397,#30398,#30399,#30400),
 .UNSPECIFIED.,.F.,.F.,(4,3,3,3,3,3,3,3,3,3,3,3,3,3,3,3,3,3,3,3,3,3,3,3,
3,3,3,3,3,3,3,3,3,3,3,3,3,3,3,3,3,4),(2.0176960437804,2.10889583919491,
2.19998459169105,2.29098582172404,2.38193982122487,2.47287122408923,2.56380463909107,
2.65481792315395,2.7458720173498,2.83706482123993,2.90897267587419,3.00133749550434,
3.09358792998079,3.18574987119399,3.27785305426829,3.36992659951255,3.46199379371309,
3.55407791216226,3.64625479384758,3.73848331266857,3.83084825439588,3.87863023449892,
3.97082459235909,4.06290199864244,4.15488861259772,4.24681378604394,4.33870774856359,
4.43059401932917,4.52249610496381,4.6144903485617,4.70653565631031,4.79871818850885,
4.84828779312365,4.94055232855515,5.03267482099036,5.12471616095592,5.2166998705942,
5.30864941974567,5.40062107605425,5.49260045125405,5.58466667839021,5.66572400274839),
 .UNSPECIFIED.);
#1356=B_SPLINE_CURVE_WITH_KNOTS('',3,(#30403,#30404,#30405,#30406,#30407,
#30408,#30409,#30410,#30411,#30412,#30413,#30414,#30415,#30416,#30417,#30418,
#30419,#30420,#30421,#30422,#30423,#30424,#30425,#30426,#30427,#30428,#30429,
#30430,#30431,#30432,#30433,#30434,#30435,#30436,#30437,#30438,#30439,#30440,
#30441,#30442,#30443,#30444,#30445,#30446,#30447,#30448,#30449,#30450,#30451,
#30452,#30453,#30454,#30455,#30456,#30457,#30458,#30459,#30460,#30461,#30462,
#30463,#30464,#30465,#30466,#30467,#30468,#30469),.UNSPECIFIED.,.F.,.F.,
(4,3,3,3,3,3,3,3,3,3,3,3,3,3,3,3,3,3,3,3,3,3,4),(5.66572400274839,5.75796559638503,
5.81794535174838,5.91020685033311,6.00235237503373,6.09440797976452,6.1864031499091,
6.27836769795418,6.37032505149634,6.4622986259719,6.55436454906352,6.64648173567859,
6.73873578885576,6.78760291037311,6.87854574101344,6.96935218416102,7.06008153265442,
7.1507587229741,7.24140863757461,7.33209537265635,7.42279809674976,7.51360445676476,
7.59202292823699),.UNSPECIFIED.);
#1357=B_SPLINE_CURVE_WITH_KNOTS('',3,(#30470,#30471,#30472,#30473,#30474,
#30475,#30476,#30477,#30478,#30479,#30480,#30481,#30482,#30483,#30484,#30485,
#30486,#30487,#30488,#30489,#30490,#30491,#30492,#30493,#30494,#30495,#30496,
#30497,#30498,#30499,#30500,#30501,#30502,#30503,#30504,#30505,#30506,#30507,
#30508,#30509,#30510,#30511,#30512,#30513,#30514,#30515,#30516,#30517,#30518,
#30519,#30520,#30521,#30522,#30523,#30524,#30525,#30526,#30527,#30528,#30529,
#30530,#30531,#30532,#30533,#30534,#30535,#30536,#30537,#30538,#30539,#30540,
#30541,#30542,#30543,#30544,#30545,#30546,#30547,#30548,#30549,#30550,#30551,
#30552,#30553,#30554,#30555,#30556,#30557,#30558,#30559,#30560,#30561,#30562,
#30563,#30564,#30565,#30566,#30567,#30568,#30569,#30570,#30571,#30572,#30573,
#30574,#30575,#30576,#30577,#30578,#30579,#30580,#30581,#30582,#30583,#30584,
#30585,#30586,#30587,#30588,#30589,#30590,#30591,#30592,#30593,#30594,#30595,
#30596,#30597,#30598,#30599,#30600,#30601,#30602,#30603,#30604,#30605,#30606,
#30607,#30608,#30609,#30610,#30611,#30612,#30613,#30614,#30615,#30616,#30617,
#30618,#30619,#30620),.UNSPECIFIED.,.F.,.F.,(4,3,3,3,3,3,3,3,3,3,3,3,3,
3,3,3,3,3,3,3,3,3,3,3,3,3,3,3,3,3,3,3,3,3,3,3,3,3,3,3,3,3,3,3,3,3,3,3,3,
3,4),(7.592022928411,7.73002674859181,7.75726046899785,7.84951329700286,
7.94164995246269,8.03369650381667,8.12568238543364,8.21763750395079,8.30958529941616,
8.40154919961633,8.49360532991555,8.58571264414763,8.67795679279574,8.72691802762258,
8.81917056833466,8.91130694839282,9.00335323657964,9.09533887448395,9.18729376149322,
9.27924133799731,9.37120503213437,9.46326097733344,9.55536811813824,9.64761211328743,
9.69657558624731,9.78882686092544,9.88096195064293,9.97300692622614,10.0649912239508,
10.1569447543583,10.2488909596008,10.340853269567,10.4329078192168,10.525013556251,
10.6172561478338,10.666233144872,10.7584851264444,10.8506209333997,10.9426666354368,
11.0346516702088,11.1266059438525,11.2185528975395,11.3105159601817,11.4025712644119,
11.4946777580579,11.5869211023612,11.6358907034968,11.7281280137823,11.820263349795,
11.9123037001377,11.9498038827978),.UNSPECIFIED.);
#1358=B_SPLINE_CURVE_WITH_KNOTS('',3,(#30622,#30623,#30624,#30625,#30626,
#30627,#30628,#30629,#30630,#30631,#30632,#30633,#30634,#30635,#30636,#30637,
#30638,#30639,#30640,#30641,#30642,#30643,#30644,#30645,#30646,#30647,#30648,
#30649,#30650,#30651,#30652,#30653,#30654,#30655,#30656,#30657,#30658,#30659,
#30660,#30661,#30662,#30663,#30664,#30665,#30666,#30667,#30668,#30669,#30670,
#30671,#30672,#30673,#30674,#30675,#30676,#30677,#30678,#30679,#30680,#30681,
#30682,#30683,#30684,#30685,#30686,#30687,#30688,#30689,#30690,#30691,#30692,
#30693,#30694,#30695,#30696,#30697,#30698,#30699,#30700,#30701,#30702,#30703,
#30704,#30705,#30706,#30707,#30708,#30709,#30710,#30711,#30712,#30713),
 .UNSPECIFIED.,.F.,.F.,(4,2,2,2,2,2,2,2,2,2,2,2,2,2,2,2,2,2,2,2,2,2,2,2,
2,2,2,2,2,2,2,2,2,2,2,2,2,2,2,2,2,2,2,2,2,4),(-1.48105208187109,-1.47723202852845,
-1.44638155789707,-1.36042020369283,-1.3378247980845,-1.32551240332599,
-1.31074165133099,-1.25968614889842,-1.19377480945142,-1.16948545946754,
-1.14847361746651,-1.11835730611952,-1.03710095242182,-1.01048351932531,
-0.997551245477823,-0.983677889304862,-0.948149263517353,-0.878152216446806,
-0.848263275169742,-0.827258278678024,-0.802834045623177,-0.775467624264196,
-0.714879430991743,-0.683780419244092,-0.669986975788721,-0.656964392336876,
-0.629700329593723,-0.58148735246408,-0.530544102745518,-0.507584410023389,
-0.486111062093909,-0.451603610301627,-0.401584260728747,-0.359850339699052,
-0.344145714276371,-0.332026565269392,-0.312215708944257,-0.28479702414513,
-0.200486142329031,-0.177699231763394,-0.156320302408579,-0.121906422413231,
-0.0623764867994372,-0.0255370712176183,-0.0117280735918997,-0.000901374079214656),
 .UNSPECIFIED.);
#1359=B_SPLINE_CURVE_WITH_KNOTS('',3,(#30714,#30715,#30716,#30717,#30718,
#30719,#30720,#30721,#30722,#30723,#30724,#30725,#30726,#30727,#30728,#30729,
#30730,#30731,#30732,#30733,#30734,#30735,#30736,#30737,#30738,#30739,#30740,
#30741,#30742,#30743,#30744,#30745,#30746,#30747,#30748,#30749,#30750,#30751,
#30752,#30753,#30754,#30755,#30756,#30757,#30758,#30759,#30760,#30761,#30762,
#30763,#30764,#30765,#30766,#30767,#30768,#30769,#30770,#30771,#30772,#30773,
#30774,#30775,#30776,#30777,#30778,#30779,#30780,#30781,#30782,#30783),
 .UNSPECIFIED.,.F.,.F.,(4,3,3,3,3,3,3,3,3,3,3,3,3,3,3,3,3,3,3,3,3,3,3,4),
(-3.85042544491851,-3.7584786014718,-3.66664683940555,-3.57193756896413,
-3.48025410630045,-3.38859847531267,-3.2969468418714,-3.20527538156021,
-3.11351194514312,-3.02169316046402,-2.92974733078309,-2.90897267587419,
-2.81676305457636,-2.72466756475499,-2.63266007968529,-2.54070992917899,
-2.44878844927304,-2.35687214176041,-2.26493751899187,-2.17290708811915,
-2.08082347305532,-1.98859964503748,-1.93931511724946,-1.92436839018911),
 .UNSPECIFIED.);
#1360=B_SPLINE_CURVE_WITH_KNOTS('',3,(#30786,#30787,#30788,#30789,#30790,
#30791,#30792,#30793,#30794,#30795,#30796,#30797,#30798,#30799,#30800,#30801,
#30802,#30803,#30804,#30805,#30806,#30807,#30808,#30809,#30810,#30811,#30812,
#30813,#30814,#30815,#30816,#30817,#30818,#30819,#30820,#30821,#30822,#30823,
#30824,#30825,#30826,#30827,#30828,#30829,#30830,#30831,#30832,#30833,#30834,
#30835,#30836,#30837,#30838,#30839,#30840,#30841,#30842,#30843,#30844,#30845,
#30846,#30847,#30848,#30849,#30850,#30851,#30852,#30853,#30854,#30855,#30856,
#30857,#30858,#30859,#30860,#30861,#30862,#30863,#30864,#30865,#30866,#30867,
#30868,#30869,#30870,#30871,#30872,#30873,#30874,#30875,#30876,#30877,#30878,
#30879,#30880,#30881,#30882,#30883,#30884,#30885,#30886,#30887,#30888,#30889,
#30890,#30891,#30892,#30893,#30894,#30895,#30896,#30897,#30898,#30899,#30900,
#30901,#30902,#30903,#30904,#30905,#30906,#30907,#30908,#30909,#30910,#30911,
#30912,#30913,#30914,#30915,#30916,#30917,#30918,#30919,#30920,#30921,#30922,
#30923,#30924),.UNSPECIFIED.,.F.,.F.,(4,3,3,3,3,3,3,3,3,3,3,3,3,3,3,3,3,
3,3,3,3,3,3,3,3,3,3,3,3,3,3,3,3,3,3,3,3,3,3,3,3,3,3,3,3,3,4),(17.9335803047654,
18.0225253583185,18.1103038525756,18.1980703397971,18.2858451790672,18.3756690675978,
18.4635667843356,18.5543537587626,18.6451407331896,18.7331832167028,18.8211192573837,
18.9089715310756,18.997199876168,19.0849615276785,19.1727121937118,19.2604722517004,
19.3490537617289,19.4369375365909,19.5258679142026,19.6147982918143,19.7028471218928,
19.7907895873348,19.8786483548595,19.9668742918069,20.0546425621996,20.1423998817223,
20.230166619867,20.31873892751,20.406629386596,20.4955426185175,20.584455850439,
20.6725044064358,20.7604466086221,20.8483051240143,20.9365311596455,21.0242992070283,
21.1120563149855,21.1998228533126,21.2883954922504,21.3762857824584,21.4651995957611,
21.5541134090638,21.6485773884456,21.7427641575297,21.8367783692867,21.9305359866766,
21.9911485749473),.UNSPECIFIED.);
#1361=B_SPLINE_CURVE_WITH_KNOTS('',3,(#30925,#30926,#30927,#30928,#30929,
#30930,#30931,#30932,#30933,#30934,#30935,#30936,#30937,#30938,#30939,#30940,
#30941,#30942,#30943,#30944,#30945,#30946,#30947,#30948,#30949,#30950,#30951,
#30952,#30953,#30954,#30955,#30956,#30957,#30958,#30959,#30960,#30961,#30962,
#30963,#30964,#30965,#30966,#30967,#30968,#30969,#30970,#30971,#30972,#30973,
#30974,#30975,#30976,#30977,#30978,#30979,#30980,#30981,#30982,#30983,#30984,
#30985,#30986,#30987,#30988,#30989,#30990,#30991,#30992,#30993,#30994,#30995,
#30996,#30997,#30998,#30999,#31000,#31001,#31002,#31003),.UNSPECIFIED.,
 .F.,.F.,(4,3,3,3,3,3,3,3,3,3,3,3,3,3,3,3,3,3,3,3,3,3,3,3,3,3,4),(21.9911485751286,
22.0812832713838,22.1714804226723,22.261826529727,22.3522487536846,22.4428476766967,
22.5237709676885,22.6118189900162,22.6997606457963,22.7876186028424,22.8758448432762,
22.9636123067326,23.0513688221931,23.1391347601272,23.2277082016737,23.3155978774572,
23.4045132018852,23.4934285263132,23.5837235555123,23.6716503950898,23.7595005030845,
23.8472943416567,23.939417946219,24.0271767650983,24.1149384979725,24.2027438832918,
24.2157887599059),.UNSPECIFIED.);
#1362=B_SPLINE_CURVE_WITH_KNOTS('',3,(#31005,#31006,#31007,#31008,#31009,
#31010,#31011,#31012,#31013,#31014,#31015,#31016,#31017,#31018,#31019,#31020,
#31021,#31022,#31023,#31024,#31025,#31026,#31027,#31028,#31029,#31030,#31031,
#31032,#31033,#31034,#31035,#31036,#31037,#31038,#31039,#31040,#31041,#31042,
#31043,#31044,#31045,#31046,#31047,#31048,#31049,#31050,#31051,#31052,#31053,
#31054,#31055,#31056,#31057,#31058,#31059,#31060,#31061,#31062,#31063,#31064,
#31065,#31066,#31067,#31068,#31069,#31070,#31071,#31072,#31073,#31074,#31075,
#31076,#31077,#31078,#31079,#31080,#31081,#31082,#31083),.UNSPECIFIED.,
 .F.,.F.,(4,3,3,3,3,3,3,3,3,3,3,3,3,3,3,3,3,3,3,3,3,3,3,3,3,3,4),(21.9911485751286,
22.1228635067403,22.1563861157154,22.2444349459262,22.3323774115027,22.4202361791641,
22.5084621160611,22.5962303865945,22.6839877062593,22.7717544445469,22.8603267519952,
22.9482172112254,23.0371304427827,23.1260436743401,23.2140922303503,23.302034432551,
23.3898929479589,23.4781189835846,23.5658870309858,23.6536441389621,23.7414106773092,
23.8299833162231,23.9178736064531,24.006787419709,24.0957012329649,24.1837486634078,
24.2167210304736),.UNSPECIFIED.);
#1363=B_SPLINE_CURVE_WITH_KNOTS('',3,(#31084,#31085,#31086,#31087,#31088,
#31089,#31090,#31091,#31092,#31093,#31094,#31095,#31096,#31097,#31098,#31099,
#31100,#31101,#31102,#31103,#31104,#31105,#31106,#31107,#31108,#31109,#31110,
#31111,#31112,#31113,#31114,#31115,#31116,#31117,#31118,#31119,#31120,#31121,
#31122,#31123,#31124,#31125,#31126,#31127,#31128,#31129,#31130,#31131,#31132,
#31133,#31134,#31135,#31136,#31137,#31138,#31139,#31140,#31141,#31142,#31143,
#31144,#31145,#31146,#31147,#31148,#31149,#31150,#31151,#31152,#31153,#31154,
#31155,#31156,#31157,#31158,#31159,#31160,#31161,#31162,#31163,#31164,#31165,
#31166,#31167,#31168,#31169,#31170,#31171,#31172,#31173,#31174,#31175,#31176,
#31177,#31178,#31179,#31180,#31181,#31182,#31183,#31184,#31185,#31186,#31187,
#31188,#31189,#31190,#31191,#31192,#31193,#31194,#31195,#31196,#31197,#31198,
#31199,#31200,#31201,#31202,#31203,#31204,#31205,#31206,#31207,#31208,#31209,
#31210,#31211,#31212,#31213,#31214,#31215,#31216,#31217,#31218,#31219,#31220,
#31221,#31222,#31223,#31224,#31225),.UNSPECIFIED.,.F.,.F.,(4,3,3,3,3,3,
3,3,3,3,3,3,3,3,3,3,3,3,3,3,3,3,3,3,3,3,3,3,3,3,3,3,3,3,3,3,3,3,3,3,3,3,
3,3,3,3,3,4),(17.9327347217548,18.0207028334297,18.1087133098411,18.1968591847413,
18.2777558812165,18.3657489057899,18.4536348542302,18.5414364722316,18.6296835931828,
18.7173935456239,18.8050922153734,18.8928000405043,18.9814533903386,19.0692848252938,
19.1583491325675,19.2474134398412,19.3354645118875,19.4234091759826,19.5112700952095,
19.5994952081166,19.687265495308,19.775024775687,19.8627934153293,19.9513628111135,
20.0392550032863,20.1281630008761,20.2170709984659,20.3051281041348,20.3930790264297,
20.4809464194359,20.5691691866428,20.6569464368303,20.7447128527237,20.8324887930608,
20.9210487340683,21.008948571148,21.0978385641194,21.1867285570907,21.273527087034,
21.3632297730275,21.4498281548608,21.5363771958627,21.6228985324255,21.7094137732703,
21.7959775267575,21.8825708026085,21.9692510829171,21.9911485749818),
 .UNSPECIFIED.);
#1364=B_SPLINE_CURVE_WITH_KNOTS('',3,(#31351,#31352,#31353,#31354,#31355,
#31356,#31357,#31358,#31359,#31360,#31361,#31362,#31363,#31364,#31365,#31366,
#31367,#31368,#31369,#31370,#31371,#31372,#31373,#31374,#31375,#31376,#31377,
#31378,#31379,#31380,#31381,#31382,#31383,#31384,#31385,#31386,#31387,#31388,
#31389,#31390,#31391,#31392,#31393,#31394,#31395,#31396,#31397,#31398,#31399,
#31400,#31401,#31402,#31403,#31404,#31405,#31406,#31407,#31408,#31409,#31410,
#31411,#31412,#31413,#31414,#31415,#31416,#31417,#31418,#31419,#31420,#31421,
#31422,#31423,#31424,#31425,#31426,#31427,#31428,#31429,#31430,#31431,#31432,
#31433,#31434,#31435,#31436,#31437,#31438,#31439,#31440,#31441,#31442,#31443,
#31444,#31445,#31446,#31447),.UNSPECIFIED.,.F.,.F.,(4,3,3,3,3,3,3,3,3,3,
3,3,3,3,3,3,3,3,3,3,3,3,3,3,3,3,3,3,3,3,3,3,4),(0.,0.0368147651103806,0.074501375546203,
0.112342565701432,0.146724444798353,0.154519180409614,0.159861819792071,
0.196798717360609,0.233592540188374,0.269524566381248,0.298932809818202,
0.306076330027527,0.311216260529057,0.347078994221376,0.382941727913695,
0.418902115841158,0.438585912474743,0.449351195385943,0.454626931743855,
0.489598596886897,0.524685601953606,0.559397454224109,0.58120313019341,
0.59285263403861,0.598656049365913,0.632452752519065,0.657800279883928,
0.670541577997107,0.677750468942682,0.683202198273149,0.715752223335255,
0.733842861978519,0.7607598169945),.UNSPECIFIED.);
#1365=B_SPLINE_CURVE_WITH_KNOTS('',3,(#31448,#31449,#31450,#31451,#31452,
#31453,#31454,#31455,#31456,#31457,#31458,#31459,#31460,#31461,#31462,#31463,
#31464,#31465,#31466,#31467,#31468,#31469,#31470,#31471,#31472,#31473,#31474,
#31475,#31476,#31477,#31478,#31479,#31480,#31481,#31482,#31483,#31484,#31485,
#31486,#31487,#31488,#31489,#31490,#31491,#31492,#31493,#31494,#31495,#31496,
#31497,#31498,#31499,#31500,#31501,#31502,#31503,#31504,#31505,#31506,#31507,
#31508,#31509,#31510,#31511,#31512,#31513,#31514,#31515,#31516,#31517,#31518,
#31519,#31520,#31521,#31522,#31523,#31524,#31525,#31526,#31527,#31528,#31529,
#31530,#31531,#31532,#31533,#31534,#31535,#31536,#31537,#31538,#31539,#31540,
#31541),.UNSPECIFIED.,.F.,.F.,(4,3,3,3,3,3,3,3,3,3,3,3,3,3,3,3,3,3,3,3,
3,3,3,3,3,3,3,3,3,3,3,4),(0.,0.0317286290156565,0.0642501424452636,0.0974595459930366,
0.128683472946203,0.13417368264342,0.138863677582811,0.172961043862833,
0.207570732336978,0.242490789657325,0.268680832647586,0.273374565791653,
0.278378882268977,0.314014888610594,0.347250961618367,0.381919138299765,
0.403413416033706,0.414921668851046,0.421531186875753,0.456779694785063,
0.493075652037049,0.529371609289035,0.553928605883257,0.562469494994855,
0.567815809877077,0.60521901315643,0.635283559248348,0.660319223571335,
0.666105225726651,0.703933093791132,0.725827582042816,0.757697664562209),
 .UNSPECIFIED.);
#1366=B_SPLINE_CURVE_WITH_KNOTS('',3,(#31542,#31543,#31544,#31545),
 .UNSPECIFIED.,.F.,.F.,(4,4),(-0.0141321293118755,0.),.UNSPECIFIED.);
#1367=B_SPLINE_CURVE_WITH_KNOTS('',3,(#31670,#31671,#31672,#31673,#31674,
#31675,#31676,#31677,#31678,#31679,#31680,#31681,#31682,#31683,#31684,#31685,
#31686,#31687,#31688,#31689,#31690,#31691,#31692,#31693,#31694,#31695,#31696,
#31697,#31698,#31699,#31700,#31701,#31702,#31703,#31704,#31705,#31706,#31707,
#31708,#31709,#31710,#31711,#31712,#31713,#31714,#31715,#31716,#31717,#31718,
#31719,#31720,#31721,#31722,#31723,#31724,#31725,#31726,#31727,#31728,#31729,
#31730,#31731,#31732,#31733,#31734,#31735,#31736,#31737,#31738,#31739,#31740,
#31741,#31742,#31743,#31744,#31745,#31746,#31747,#31748,#31749,#31750,#31751,
#31752,#31753,#31754,#31755,#31756,#31757,#31758,#31759,#31760,#31761,#31762,
#31763),.UNSPECIFIED.,.F.,.F.,(4,3,3,3,3,3,3,3,3,3,3,3,3,3,3,3,3,3,3,3,
3,3,3,3,3,3,3,3,3,3,3,4),(0.,0.0321250758863861,0.0642501517727722,0.0977017688573295,
0.128683484204146,0.134173763202423,0.13886369439468,0.172961064488349,
0.207570755159294,0.242490806774014,0.268680845485055,0.273374584290101,
0.278378886542516,0.314014893103864,0.347250961618176,0.381919136552636,
0.403413414395757,0.414921666320687,0.421531186815446,0.456944022746122,
0.492989037452285,0.529588353331513,0.553928602645526,0.562469488501506,
0.567815809339951,0.605219012373712,0.63528355843125,0.660319221884543,
0.666105223775399,0.703933092116297,0.725827582042572,0.757697666925817),
 .UNSPECIFIED.);
#1368=B_SPLINE_CURVE_WITH_KNOTS('',3,(#31764,#31765,#31766,#31767,#31768,
#31769,#31770,#31771,#31772,#31773,#31774,#31775,#31776,#31777,#31778,#31779,
#31780,#31781,#31782,#31783,#31784,#31785,#31786,#31787,#31788,#31789,#31790,
#31791,#31792,#31793,#31794,#31795,#31796,#31797,#31798,#31799,#31800,#31801,
#31802,#31803,#31804,#31805,#31806,#31807,#31808,#31809,#31810,#31811,#31812,
#31813,#31814,#31815,#31816,#31817,#31818,#31819,#31820,#31821,#31822,#31823,
#31824,#31825,#31826,#31827,#31828,#31829,#31830,#31831,#31832,#31833,#31834,
#31835,#31836,#31837,#31838,#31839,#31840,#31841,#31842,#31843,#31844,#31845,
#31846,#31847,#31848,#31849,#31850,#31851,#31852,#31853,#31854,#31855,#31856,
#31857,#31858,#31859,#31860),.UNSPECIFIED.,.F.,.F.,(4,3,3,3,3,3,3,3,3,3,
3,3,3,3,3,3,3,3,3,3,3,3,3,3,3,3,3,3,3,3,3,3,4),(0.,0.0371460267140582,0.0748361240619943,
0.112676081007043,0.146724449836877,0.15451918997546,0.159861821081083,
0.19680457436756,0.233592541347715,0.269524566606476,0.298932810470348,
0.306076332066899,0.311216261220193,0.347078994566964,0.382941727913735,
0.418902116039512,0.438585912660715,0.449351195759605,0.454626932097783,
0.489598597399228,0.524659768090933,0.559397455171815,0.581203131022683,
0.592852635112903,0.598656049141822,0.632468594886279,0.657800279757981,
0.67054157736057,0.677750458032431,0.683202182754059,0.715752207345716,
0.733842861978756,0.760759816994732),.UNSPECIFIED.);
#1723=VERTEX_POINT('',#28113);
#1724=VERTEX_POINT('',#28114);
#1725=VERTEX_POINT('',#28116);
#1726=VERTEX_POINT('',#28123);
#1727=VERTEX_POINT('',#28223);
#1728=VERTEX_POINT('',#28224);
#1729=VERTEX_POINT('',#28226);
#1730=VERTEX_POINT('',#28375);
#1731=VERTEX_POINT('',#28595);
#1732=VERTEX_POINT('',#28596);
#1733=VERTEX_POINT('',#28598);
#1734=VERTEX_POINT('',#28820);
#1735=VERTEX_POINT('',#29040);
#1736=VERTEX_POINT('',#29041);
#1737=VERTEX_POINT('',#29043);
#1738=VERTEX_POINT('',#29123);
#1739=VERTEX_POINT('',#29170);
#1740=VERTEX_POINT('',#29172);
#1741=VERTEX_POINT('',#29320);
#1742=VERTEX_POINT('',#29321);
#1743=VERTEX_POINT('',#29323);
#1744=VERTEX_POINT('',#29391);
#1745=VERTEX_POINT('',#29410);
#1746=VERTEX_POINT('',#29501);
#1747=VERTEX_POINT('',#29502);
#1748=VERTEX_POINT('',#29504);
#1749=VERTEX_POINT('',#29720);
#1750=VERTEX_POINT('',#29854);
#1751=VERTEX_POINT('',#29855);
#1752=VERTEX_POINT('',#29857);
#1753=VERTEX_POINT('',#30204);
#1754=VERTEX_POINT('',#30205);
#1755=VERTEX_POINT('',#30207);
#1756=VERTEX_POINT('',#30275);
#1757=VERTEX_POINT('',#30402);
#1758=VERTEX_POINT('',#30621);
#1759=VERTEX_POINT('',#30785);
#1760=VERTEX_POINT('',#31004);
#1761=VERTEX_POINT('',#31350);
#1762=VERTEX_POINT('',#31862);
#1763=VERTEX_POINT('',#31863);
#1764=VERTEX_POINT('',#31865);
#1765=VERTEX_POINT('',#31867);
#1766=VERTEX_POINT('',#31869);
#1767=VERTEX_POINT('',#31871);
#1768=VERTEX_POINT('',#31875);
#1769=VERTEX_POINT('',#31877);
#1770=VERTEX_POINT('',#31881);
#1771=VERTEX_POINT('',#31885);
#1772=VERTEX_POINT('',#31889);
#1773=VERTEX_POINT('',#31893);
#2302=EDGE_CURVE('',#1723,#1724,#826,.T.);
#2303=EDGE_CURVE('',#1724,#1725,#1330,.T.);
#2304=EDGE_CURVE('',#1726,#1725,#649,.T.);
#2305=EDGE_CURVE('',#1723,#1726,#1331,.T.);
#2306=EDGE_CURVE('',#1727,#1728,#827,.T.);
#2307=EDGE_CURVE('',#1728,#1729,#1332,.T.);
#2308=EDGE_CURVE('',#1729,#1724,#1333,.T.);
#2309=EDGE_CURVE('',#1730,#1723,#1334,.T.);
#2310=EDGE_CURVE('',#1727,#1730,#1335,.T.);
#2311=EDGE_CURVE('',#1731,#1732,#828,.T.);
#2312=EDGE_CURVE('',#1732,#1733,#1336,.T.);
#2313=EDGE_CURVE('',#1733,#1728,#1337,.T.);
#2314=EDGE_CURVE('',#1734,#1727,#1338,.T.);
#2315=EDGE_CURVE('',#1731,#1734,#1339,.T.);
#2316=EDGE_CURVE('',#1735,#1736,#829,.T.);
#2317=EDGE_CURVE('',#1737,#1735,#1340,.T.);
#2318=EDGE_CURVE('',#1738,#1737,#1341,.T.);
#2319=EDGE_CURVE('',#1739,#1738,#650,.T.);
#2320=EDGE_CURVE('',#1739,#1740,#1342,.T.);
#2321=EDGE_CURVE('',#1740,#1736,#1343,.T.);
#2322=EDGE_CURVE('',#1741,#1742,#830,.T.);
#2323=EDGE_CURVE('',#1742,#1743,#1344,.T.);
#2324=EDGE_CURVE('',#1743,#1744,#1345,.T.);
#2325=EDGE_CURVE('',#1745,#1744,#651,.T.);
#2326=EDGE_CURVE('',#1745,#1741,#1346,.T.);
#2327=EDGE_CURVE('',#1746,#1747,#831,.T.);
#2328=EDGE_CURVE('',#1747,#1748,#1347,.T.);
#2329=EDGE_CURVE('',#1748,#1742,#1348,.T.);
#2330=EDGE_CURVE('',#1741,#1749,#1349,.T.);
#2331=EDGE_CURVE('',#1749,#1746,#1350,.T.);
#2332=EDGE_CURVE('',#1750,#1751,#832,.T.);
#2333=EDGE_CURVE('',#1751,#1752,#1351,.T.);
#2334=EDGE_CURVE('',#1752,#1747,#1352,.T.);
#2335=EDGE_CURVE('',#1746,#1750,#1353,.T.);
#2336=EDGE_CURVE('',#1753,#1754,#833,.T.);
#2337=EDGE_CURVE('',#1753,#1755,#1354,.T.);
#2338=EDGE_CURVE('',#1756,#1755,#652,.F.);
#2339=EDGE_CURVE('',#1756,#1754,#1355,.T.);
#2340=EDGE_CURVE('',#1754,#1757,#1356,.T.);
#2341=EDGE_CURVE('',#1757,#1751,#1357,.T.);
#2342=EDGE_CURVE('',#1750,#1758,#1358,.T.);
#2343=EDGE_CURVE('',#1758,#1753,#1359,.T.);
#2344=EDGE_CURVE('',#1736,#1759,#1360,.T.);
#2345=EDGE_CURVE('',#1759,#1732,#1361,.T.);
#2346=EDGE_CURVE('',#1760,#1731,#1362,.T.);
#2347=EDGE_CURVE('',#1735,#1760,#1363,.T.);
#2348=EDGE_CURVE('',#1725,#1761,#1364,.T.);
#2349=EDGE_CURVE('',#1755,#1739,#1365,.T.);
#2350=EDGE_CURVE('',#1761,#1745,#1366,.T.);
#2351=EDGE_CURVE('',#1744,#1726,#1367,.T.);
#2352=EDGE_CURVE('',#1738,#1756,#1368,.T.);
#2353=EDGE_CURVE('',#1762,#1763,#834,.T.);
#2354=EDGE_CURVE('',#1763,#1764,#835,.T.);
#2355=EDGE_CURVE('',#1764,#1765,#836,.T.);
#2356=EDGE_CURVE('',#1765,#1766,#837,.T.);
#2357=EDGE_CURVE('',#1766,#1767,#838,.T.);
#2358=EDGE_CURVE('',#1767,#1762,#839,.T.);
#2359=EDGE_CURVE('',#1763,#1768,#840,.T.);
#2360=EDGE_CURVE('',#1769,#1768,#841,.T.);
#2361=EDGE_CURVE('',#1764,#1769,#842,.T.);
#2362=EDGE_CURVE('',#1770,#1769,#843,.T.);
#2363=EDGE_CURVE('',#1765,#1770,#844,.T.);
#2364=EDGE_CURVE('',#1771,#1770,#845,.T.);
#2365=EDGE_CURVE('',#1766,#1771,#846,.T.);
#2366=EDGE_CURVE('',#1772,#1771,#847,.T.);
#2367=EDGE_CURVE('',#1767,#1772,#848,.T.);
#2368=EDGE_CURVE('',#1773,#1772,#849,.T.);
#2369=EDGE_CURVE('',#1762,#1773,#850,.T.);
#2370=EDGE_CURVE('',#1768,#1773,#851,.T.);
#3297=ORIENTED_EDGE('',*,*,#2302,.T.);
#3298=ORIENTED_EDGE('',*,*,#2303,.T.);
#3299=ORIENTED_EDGE('',*,*,#2304,.F.);
#3300=ORIENTED_EDGE('',*,*,#2305,.F.);
#3301=ORIENTED_EDGE('',*,*,#2306,.T.);
#3302=ORIENTED_EDGE('',*,*,#2307,.T.);
#3303=ORIENTED_EDGE('',*,*,#2308,.T.);
#3304=ORIENTED_EDGE('',*,*,#2302,.F.);
#3305=ORIENTED_EDGE('',*,*,#2309,.F.);
#3306=ORIENTED_EDGE('',*,*,#2310,.F.);
#3307=ORIENTED_EDGE('',*,*,#2311,.T.);
#3308=ORIENTED_EDGE('',*,*,#2312,.T.);
#3309=ORIENTED_EDGE('',*,*,#2313,.T.);
#3310=ORIENTED_EDGE('',*,*,#2306,.F.);
#3311=ORIENTED_EDGE('',*,*,#2314,.F.);
#3312=ORIENTED_EDGE('',*,*,#2315,.F.);
#3313=ORIENTED_EDGE('',*,*,#2316,.F.);
#3314=ORIENTED_EDGE('',*,*,#2317,.F.);
#3315=ORIENTED_EDGE('',*,*,#2318,.F.);
#3316=ORIENTED_EDGE('',*,*,#2319,.F.);
#3317=ORIENTED_EDGE('',*,*,#2320,.T.);
#3318=ORIENTED_EDGE('',*,*,#2321,.T.);
#3319=ORIENTED_EDGE('',*,*,#2322,.T.);
#3320=ORIENTED_EDGE('',*,*,#2323,.T.);
#3321=ORIENTED_EDGE('',*,*,#2324,.T.);
#3322=ORIENTED_EDGE('',*,*,#2325,.F.);
#3323=ORIENTED_EDGE('',*,*,#2326,.T.);
#3324=ORIENTED_EDGE('',*,*,#2327,.T.);
#3325=ORIENTED_EDGE('',*,*,#2328,.T.);
#3326=ORIENTED_EDGE('',*,*,#2329,.T.);
#3327=ORIENTED_EDGE('',*,*,#2322,.F.);
#3328=ORIENTED_EDGE('',*,*,#2330,.T.);
#3329=ORIENTED_EDGE('',*,*,#2331,.T.);
#3330=ORIENTED_EDGE('',*,*,#2332,.T.);
#3331=ORIENTED_EDGE('',*,*,#2333,.T.);
#3332=ORIENTED_EDGE('',*,*,#2334,.T.);
#3333=ORIENTED_EDGE('',*,*,#2327,.F.);
#3334=ORIENTED_EDGE('',*,*,#2335,.T.);
#3335=ORIENTED_EDGE('',*,*,#2336,.F.);
#3336=ORIENTED_EDGE('',*,*,#2337,.T.);
#3337=ORIENTED_EDGE('',*,*,#2338,.F.);
#3338=ORIENTED_EDGE('',*,*,#2339,.T.);
#3339=ORIENTED_EDGE('',*,*,#2336,.T.);
#3340=ORIENTED_EDGE('',*,*,#2340,.T.);
#3341=ORIENTED_EDGE('',*,*,#2341,.T.);
#3342=ORIENTED_EDGE('',*,*,#2332,.F.);
#3343=ORIENTED_EDGE('',*,*,#2342,.T.);
#3344=ORIENTED_EDGE('',*,*,#2343,.T.);
#3345=ORIENTED_EDGE('',*,*,#2316,.T.);
#3346=ORIENTED_EDGE('',*,*,#2344,.T.);
#3347=ORIENTED_EDGE('',*,*,#2345,.T.);
#3348=ORIENTED_EDGE('',*,*,#2311,.F.);
#3349=ORIENTED_EDGE('',*,*,#2346,.F.);
#3350=ORIENTED_EDGE('',*,*,#2347,.F.);
#3351=ORIENTED_EDGE('',*,*,#2348,.F.);
#3352=ORIENTED_EDGE('',*,*,#2303,.F.);
#3353=ORIENTED_EDGE('',*,*,#2308,.F.);
#3354=ORIENTED_EDGE('',*,*,#2307,.F.);
#3355=ORIENTED_EDGE('',*,*,#2313,.F.);
#3356=ORIENTED_EDGE('',*,*,#2312,.F.);
#3357=ORIENTED_EDGE('',*,*,#2345,.F.);
#3358=ORIENTED_EDGE('',*,*,#2344,.F.);
#3359=ORIENTED_EDGE('',*,*,#2321,.F.);
#3360=ORIENTED_EDGE('',*,*,#2320,.F.);
#3361=ORIENTED_EDGE('',*,*,#2349,.F.);
#3362=ORIENTED_EDGE('',*,*,#2337,.F.);
#3363=ORIENTED_EDGE('',*,*,#2343,.F.);
#3364=ORIENTED_EDGE('',*,*,#2342,.F.);
#3365=ORIENTED_EDGE('',*,*,#2335,.F.);
#3366=ORIENTED_EDGE('',*,*,#2331,.F.);
#3367=ORIENTED_EDGE('',*,*,#2330,.F.);
#3368=ORIENTED_EDGE('',*,*,#2326,.F.);
#3369=ORIENTED_EDGE('',*,*,#2350,.F.);
#3370=ORIENTED_EDGE('',*,*,#2351,.F.);
#3371=ORIENTED_EDGE('',*,*,#2324,.F.);
#3372=ORIENTED_EDGE('',*,*,#2323,.F.);
#3373=ORIENTED_EDGE('',*,*,#2329,.F.);
#3374=ORIENTED_EDGE('',*,*,#2328,.F.);
#3375=ORIENTED_EDGE('',*,*,#2334,.F.);
#3376=ORIENTED_EDGE('',*,*,#2333,.F.);
#3377=ORIENTED_EDGE('',*,*,#2341,.F.);
#3378=ORIENTED_EDGE('',*,*,#2340,.F.);
#3379=ORIENTED_EDGE('',*,*,#2339,.F.);
#3380=ORIENTED_EDGE('',*,*,#2352,.F.);
#3381=ORIENTED_EDGE('',*,*,#2318,.T.);
#3382=ORIENTED_EDGE('',*,*,#2317,.T.);
#3383=ORIENTED_EDGE('',*,*,#2347,.T.);
#3384=ORIENTED_EDGE('',*,*,#2346,.T.);
#3385=ORIENTED_EDGE('',*,*,#2315,.T.);
#3386=ORIENTED_EDGE('',*,*,#2314,.T.);
#3387=ORIENTED_EDGE('',*,*,#2310,.T.);
#3388=ORIENTED_EDGE('',*,*,#2309,.T.);
#3389=ORIENTED_EDGE('',*,*,#2305,.T.);
#3390=ORIENTED_EDGE('',*,*,#2353,.T.);
#3391=ORIENTED_EDGE('',*,*,#2354,.T.);
#3392=ORIENTED_EDGE('',*,*,#2355,.T.);
#3393=ORIENTED_EDGE('',*,*,#2356,.T.);
#3394=ORIENTED_EDGE('',*,*,#2357,.T.);
#3395=ORIENTED_EDGE('',*,*,#2358,.T.);
#3396=ORIENTED_EDGE('',*,*,#2349,.T.);
#3397=ORIENTED_EDGE('',*,*,#2319,.T.);
#3398=ORIENTED_EDGE('',*,*,#2352,.T.);
#3399=ORIENTED_EDGE('',*,*,#2338,.T.);
#3400=ORIENTED_EDGE('',*,*,#2354,.F.);
#3401=ORIENTED_EDGE('',*,*,#2359,.T.);
#3402=ORIENTED_EDGE('',*,*,#2360,.F.);
#3403=ORIENTED_EDGE('',*,*,#2361,.F.);
#3404=ORIENTED_EDGE('',*,*,#2355,.F.);
#3405=ORIENTED_EDGE('',*,*,#2361,.T.);
#3406=ORIENTED_EDGE('',*,*,#2362,.F.);
#3407=ORIENTED_EDGE('',*,*,#2363,.F.);
#3408=ORIENTED_EDGE('',*,*,#2356,.F.);
#3409=ORIENTED_EDGE('',*,*,#2363,.T.);
#3410=ORIENTED_EDGE('',*,*,#2364,.F.);
#3411=ORIENTED_EDGE('',*,*,#2365,.F.);
#3412=ORIENTED_EDGE('',*,*,#2357,.F.);
#3413=ORIENTED_EDGE('',*,*,#2365,.T.);
#3414=ORIENTED_EDGE('',*,*,#2366,.F.);
#3415=ORIENTED_EDGE('',*,*,#2367,.F.);
#3416=ORIENTED_EDGE('',*,*,#2358,.F.);
#3417=ORIENTED_EDGE('',*,*,#2367,.T.);
#3418=ORIENTED_EDGE('',*,*,#2368,.F.);
#3419=ORIENTED_EDGE('',*,*,#2369,.F.);
#3420=ORIENTED_EDGE('',*,*,#2353,.F.);
#3421=ORIENTED_EDGE('',*,*,#2369,.T.);
#3422=ORIENTED_EDGE('',*,*,#2370,.F.);
#3423=ORIENTED_EDGE('',*,*,#2359,.F.);
#3424=ORIENTED_EDGE('',*,*,#2370,.T.);
#3425=ORIENTED_EDGE('',*,*,#2368,.T.);
#3426=ORIENTED_EDGE('',*,*,#2366,.T.);
#3427=ORIENTED_EDGE('',*,*,#2364,.T.);
#3428=ORIENTED_EDGE('',*,*,#2362,.T.);
#3429=ORIENTED_EDGE('',*,*,#2360,.T.);
#3430=ORIENTED_EDGE('',*,*,#2348,.T.);
#3431=ORIENTED_EDGE('',*,*,#2350,.T.);
#3432=ORIENTED_EDGE('',*,*,#2325,.T.);
#3433=ORIENTED_EDGE('',*,*,#2351,.T.);
#3434=ORIENTED_EDGE('',*,*,#2304,.T.);
#4008=CYLINDRICAL_SURFACE('',#4508,4.08499999999997);
#4009=CYLINDRICAL_SURFACE('',#4510,4.08499999999997);
#4010=CYLINDRICAL_SURFACE('',#4511,4.08499999999997);
#4011=CYLINDRICAL_SURFACE('',#4512,4.08499999999997);
#4012=CYLINDRICAL_SURFACE('',#4514,3.38975);
#4013=CYLINDRICAL_SURFACE('',#4516,3.38975);
#4014=CYLINDRICAL_SURFACE('',#4517,3.38975);
#4015=CYLINDRICAL_SURFACE('',#4518,3.38975);
#4016=CYLINDRICAL_SURFACE('',#4520,3.38975);
#4017=CYLINDRICAL_SURFACE('',#4521,4.08499999999997);
#4165=ADVANCED_FACE('',(#282),#4008,.F.);
#4166=ADVANCED_FACE('',(#283),#4009,.F.);
#4167=ADVANCED_FACE('',(#284),#4010,.F.);
#4168=ADVANCED_FACE('',(#285),#4011,.F.);
#4169=ADVANCED_FACE('',(#286),#4012,.F.);
#4170=ADVANCED_FACE('',(#287),#4013,.F.);
#4171=ADVANCED_FACE('',(#288),#4014,.F.);
#4172=ADVANCED_FACE('',(#289),#4015,.F.);
#4173=ADVANCED_FACE('',(#290),#4016,.F.);
#4174=ADVANCED_FACE('',(#291),#4017,.F.);
#4175=ADVANCED_FACE('',(#292),#60,.F.);
#4176=ADVANCED_FACE('',(#293),#61,.F.);
#4177=ADVANCED_FACE('',(#294,#108),#149,.T.);
#4178=ADVANCED_FACE('',(#295),#150,.T.);
#4179=ADVANCED_FACE('',(#296),#151,.T.);
#4180=ADVANCED_FACE('',(#297),#152,.T.);
#4181=ADVANCED_FACE('',(#298),#153,.T.);
#4182=ADVANCED_FACE('',(#299),#154,.T.);
#4183=ADVANCED_FACE('',(#300),#155,.T.);
#4184=ADVANCED_FACE('',(#301,#109),#156,.F.);
#4263=CLOSED_SHELL('',(#4165,#4166,#4167,#4168,#4169,#4170,#4171,#4172,
#4173,#4174,#4175,#4176,#4177,#4178,#4179,#4180,#4181,#4182,#4183,#4184));
#4507=AXIS2_PLACEMENT_3D('',#28111,#5086,#5087);
#4508=AXIS2_PLACEMENT_3D('',#28112,#5088,#5089);
#4509=AXIS2_PLACEMENT_3D('',#28124,#5091,#5092);
#4510=AXIS2_PLACEMENT_3D('',#28222,#5093,#5094);
#4511=AXIS2_PLACEMENT_3D('',#28594,#5096,#5097);
#4512=AXIS2_PLACEMENT_3D('',#29039,#5099,#5100);
#4513=AXIS2_PLACEMENT_3D('',#29171,#5102,#5103);
#4514=AXIS2_PLACEMENT_3D('',#29319,#5104,#5105);
#4515=AXIS2_PLACEMENT_3D('',#29411,#5107,#5108);
#4516=AXIS2_PLACEMENT_3D('',#29500,#5109,#5110);
#4517=AXIS2_PLACEMENT_3D('',#29853,#5112,#5113);
#4518=AXIS2_PLACEMENT_3D('',#30203,#5115,#5116);
#4519=AXIS2_PLACEMENT_3D('',#30276,#5118,#5119);
#4520=AXIS2_PLACEMENT_3D('',#30401,#5120,#5121);
#4521=AXIS2_PLACEMENT_3D('',#30784,#5122,#5123);
#4522=AXIS2_PLACEMENT_3D('',#31861,#5124,#5125);
#4523=AXIS2_PLACEMENT_3D('',#31874,#5132,#5133);
#4524=AXIS2_PLACEMENT_3D('',#31880,#5137,#5138);
#4525=AXIS2_PLACEMENT_3D('',#31884,#5141,#5142);
#4526=AXIS2_PLACEMENT_3D('',#31888,#5145,#5146);
#4527=AXIS2_PLACEMENT_3D('',#31892,#5149,#5150);
#4528=AXIS2_PLACEMENT_3D('',#31896,#5153,#5154);
#4529=AXIS2_PLACEMENT_3D('',#31898,#5156,#5157);
#5086=DIRECTION('axis',(0.,0.,1.));
#5087=DIRECTION('refdir',(1.,0.,0.));
#5088=DIRECTION('center_axis',(0.,-1.,0.));
#5089=DIRECTION('ref_axis',(-0.608635263423501,0.,0.793450134613011));
#5090=DIRECTION('',(0.,-1.,0.));
#5091=DIRECTION('center_axis',(0.,1.,0.));
#5092=DIRECTION('ref_axis',(1.,0.,3.91712146416972E-15));
#5093=DIRECTION('center_axis',(0.,-1.,0.));
#5094=DIRECTION('ref_axis',(-0.608635263423501,0.,0.793450134613011));
#5095=DIRECTION('',(0.,-1.,0.));
#5096=DIRECTION('center_axis',(0.,-1.,0.));
#5097=DIRECTION('ref_axis',(-0.608635263423501,0.,0.793450134613011));
#5098=DIRECTION('',(0.,-1.,0.));
#5099=DIRECTION('center_axis',(0.,-1.,0.));
#5100=DIRECTION('ref_axis',(-0.608635263423501,0.,0.793450134613011));
#5101=DIRECTION('',(0.,-1.,0.));
#5102=DIRECTION('center_axis',(0.,-1.,0.));
#5103=DIRECTION('ref_axis',(1.,0.,3.91712146416972E-15));
#5104=DIRECTION('center_axis',(0.,-1.,0.));
#5105=DIRECTION('ref_axis',(-0.347608103729637,0.,-0.937639912877799));
#5106=DIRECTION('',(0.,-1.,0.));
#5107=DIRECTION('center_axis',(0.,1.,0.));
#5108=DIRECTION('ref_axis',(1.,0.,0.));
#5109=DIRECTION('center_axis',(0.,-1.,0.));
#5110=DIRECTION('ref_axis',(-0.347608103729637,0.,-0.937639912877799));
#5111=DIRECTION('',(0.,-1.,0.));
#5112=DIRECTION('center_axis',(0.,-1.,0.));
#5113=DIRECTION('ref_axis',(-0.347608103729637,0.,-0.937639912877799));
#5114=DIRECTION('',(0.,-1.,0.));
#5115=DIRECTION('center_axis',(0.,-1.,0.));
#5116=DIRECTION('ref_axis',(-0.347608103729637,0.,-0.937639912877799));
#5117=DIRECTION('',(0.,-1.,0.));
#5118=DIRECTION('center_axis',(0.,1.,0.));
#5119=DIRECTION('ref_axis',(1.,0.,0.));
#5120=DIRECTION('center_axis',(0.,-1.,0.));
#5121=DIRECTION('ref_axis',(-0.347608103729637,0.,-0.937639912877799));
#5122=DIRECTION('center_axis',(0.,-1.,0.));
#5123=DIRECTION('ref_axis',(-0.608635263423501,0.,0.793450134613011));
#5124=DIRECTION('center_axis',(0.,1.,0.));
#5125=DIRECTION('ref_axis',(1.,0.,0.));
#5126=DIRECTION('',(0.,0.,-1.));
#5127=DIRECTION('',(-0.866025403784439,0.,-0.5));
#5128=DIRECTION('',(-0.866025403784439,0.,0.5));
#5129=DIRECTION('',(0.,0.,1.));
#5130=DIRECTION('',(0.866025403784439,0.,0.5));
#5131=DIRECTION('',(0.866025403784439,0.,-0.5));
#5132=DIRECTION('center_axis',(0.5,0.,-0.866025403784439));
#5133=DIRECTION('ref_axis',(0.866025403784439,0.,0.5));
#5134=DIRECTION('',(0.,-1.,0.));
#5135=DIRECTION('',(0.866025403784439,0.,0.5));
#5136=DIRECTION('',(0.,-1.,0.));
#5137=DIRECTION('center_axis',(-0.5,0.,-0.866025403784439));
#5138=DIRECTION('ref_axis',(0.866025403784439,0.,-0.5));
#5139=DIRECTION('',(0.866025403784439,0.,-0.5));
#5140=DIRECTION('',(0.,-1.,0.));
#5141=DIRECTION('center_axis',(-1.,0.,0.));
#5142=DIRECTION('ref_axis',(0.,0.,-1.));
#5143=DIRECTION('',(0.,0.,-1.));
#5144=DIRECTION('',(0.,-1.,0.));
#5145=DIRECTION('center_axis',(-0.5,0.,0.866025403784439));
#5146=DIRECTION('ref_axis',(-0.866025403784439,0.,-0.5));
#5147=DIRECTION('',(-0.866025403784439,0.,-0.5));
#5148=DIRECTION('',(0.,-1.,0.));
#5149=DIRECTION('center_axis',(0.5,0.,0.866025403784439));
#5150=DIRECTION('ref_axis',(-0.866025403784439,0.,0.5));
#5151=DIRECTION('',(-0.866025403784439,0.,0.5));
#5152=DIRECTION('',(0.,-1.,0.));
#5153=DIRECTION('center_axis',(1.,0.,0.));
#5154=DIRECTION('ref_axis',(0.,0.,1.));
#5155=DIRECTION('',(0.,0.,1.));
#5156=DIRECTION('center_axis',(0.,1.,0.));
#5157=DIRECTION('ref_axis',(1.,0.,0.));
#28111=CARTESIAN_POINT('',(0.,0.,0.));
#28112=CARTESIAN_POINT('Origin',(370.834317853224,-8.23961502859548,0.));
#28113=CARTESIAN_POINT('',(373.320592904309,-15.4531286062585,-3.24124379989413));
#28114=CARTESIAN_POINT('',(373.320108995548,-15.5571531246989,-3.24059684932977));
#28115=CARTESIAN_POINT('',(373.320592904309,-8.23961502859548,-3.24124379989413));
#28116=CARTESIAN_POINT('',(371.892222276197,-16.,3.94563850749836));
#28117=CARTESIAN_POINT('Ctrl Pts',(373.320108995548,-15.5571531246989,-3.24059684932998));
#28118=CARTESIAN_POINT('Ctrl Pts',(373.632190344584,-15.5761639218313,-3.0053442006562));
#28119=CARTESIAN_POINT('Ctrl Pts',(374.850886074702,-15.6594771329477,-1.78563323199014));
#28120=CARTESIAN_POINT('Ctrl Pts',(375.341784615062,-15.8070927580481,1.59206573694299));
#28121=CARTESIAN_POINT('Ctrl Pts',(373.167528343663,-15.935697586016,3.60370350081893));
#28122=CARTESIAN_POINT('Ctrl Pts',(371.892222276197,-16.,3.94563850749836));
#28123=CARTESIAN_POINT('',(369.775300062574,-16.,3.94533982301726));
#28124=CARTESIAN_POINT('Origin',(370.834317853224,-16.,0.));
#28125=CARTESIAN_POINT('Ctrl Pts',(373.320592904309,-15.4531286062585,-3.2412437998941));
#28126=CARTESIAN_POINT('Ctrl Pts',(373.415273543652,-15.4589570255755,-3.16861670796533));
#28127=CARTESIAN_POINT('Ctrl Pts',(373.506888457287,-15.4647854448925,-3.09174615098767));
#28128=CARTESIAN_POINT('Ctrl Pts',(373.595037865624,-15.4706138642095,-3.01092178794732));
#28129=CARTESIAN_POINT('Ctrl Pts',(373.683101628257,-15.4764366206516,-2.93017595361797));
#28130=CARTESIAN_POINT('Ctrl Pts',(373.767706286925,-15.4822593770937,-2.84548422952368));
#28131=CARTESIAN_POINT('Ctrl Pts',(373.848484213075,-15.4880821335358,-2.75717720778772));
#28132=CARTESIAN_POINT('Ctrl Pts',(373.930386713752,-15.493985953257,-2.66764079292362));
#28133=CARTESIAN_POINT('Ctrl Pts',(374.008354785899,-15.4998897729783,-2.57438791056201));
#28134=CARTESIAN_POINT('Ctrl Pts',(374.082042785605,-15.5057935926996,-2.47780301145807));
#28135=CARTESIAN_POINT('Ctrl Pts',(374.154641056606,-15.511610104286,-2.38264644990447));
#28136=CARTESIAN_POINT('Ctrl Pts',(374.223084739107,-15.5174266158724,-2.28425609165628));
#28137=CARTESIAN_POINT('Ctrl Pts',(374.287083509277,-15.5232431274588,-2.18303328521979));
#28138=CARTESIAN_POINT('Ctrl Pts',(374.351073491281,-15.5290588403349,-2.08182437847084));
#28139=CARTESIAN_POINT('Ctrl Pts',(374.410619558004,-15.5348745532111,-1.97778414053954));
#28140=CARTESIAN_POINT('Ctrl Pts',(374.465475094,-15.5406902660872,-1.87134232377645));
#28141=CARTESIAN_POINT('Ctrl Pts',(374.520335880489,-15.5465065356138,-1.76489031894469));
#28142=CARTESIAN_POINT('Ctrl Pts',(374.570505057529,-15.5523228051403,-1.65603663942584));
#28143=CARTESIAN_POINT('Ctrl Pts',(374.615782577735,-15.5581390746669,-1.54523446029321));
#28144=CARTESIAN_POINT('Ctrl Pts',(374.662253415828,-15.5641086356818,-1.43151201914736));
#28145=CARTESIAN_POINT('Ctrl Pts',(374.703570979475,-15.5700781966968,-1.31573735489747));
#28146=CARTESIAN_POINT('Ctrl Pts',(374.739572660431,-15.5760477577118,-1.19841974732692));
#28147=CARTESIAN_POINT('Ctrl Pts',(374.774699352152,-15.5818722337892,-1.08395344116946));
#28148=CARTESIAN_POINT('Ctrl Pts',(374.80476554543,-15.5876967098667,-0.968018744102296));
#28149=CARTESIAN_POINT('Ctrl Pts',(374.829671745781,-15.5935211859442,-0.851100624619647));
#28150=CARTESIAN_POINT('Ctrl Pts',(374.855508548595,-15.5995632894279,-0.729813942756243));
#28151=CARTESIAN_POINT('Ctrl Pts',(374.875792168291,-15.6056053929116,-0.60746939833637));
#28152=CARTESIAN_POINT('Ctrl Pts',(374.890470404658,-15.6116474963953,-0.484614774322597));
#28153=CARTESIAN_POINT('Ctrl Pts',(374.905148641026,-15.617689599879,-0.361760150308814));
#28154=CARTESIAN_POINT('Ctrl Pts',(374.914221521336,-15.6237317033627,-0.238395931624845));
#28155=CARTESIAN_POINT('Ctrl Pts',(374.917696855934,-15.6297738068464,-0.115069197545622));
#28156=CARTESIAN_POINT('Ctrl Pts',(374.921059702466,-15.6356203422434,0.00426575230112755));
#28157=CARTESIAN_POINT('Ctrl Pts',(374.919191970017,-15.6414668776404,0.123925603645873));
#28158=CARTESIAN_POINT('Ctrl Pts',(374.912059029124,-15.6473134130375,0.243417136549867));
#28159=CARTESIAN_POINT('Ctrl Pts',(374.90493468769,-15.6531528998641,0.362764610721632));
#28160=CARTESIAN_POINT('Ctrl Pts',(374.892557790066,-15.6589923866908,0.48194376948902));
#28161=CARTESIAN_POINT('Ctrl Pts',(374.874945688179,-15.6648318735175,0.600459573481934));
#28162=CARTESIAN_POINT('Ctrl Pts',(374.857350341039,-15.6706658051229,0.718862631006505));
#28163=CARTESIAN_POINT('Ctrl Pts',(374.834529758843,-15.6764997367283,0.836603191362777));
#28164=CARTESIAN_POINT('Ctrl Pts',(374.806553203294,-15.6823336683337,0.953190077398779));
#28165=CARTESIAN_POINT('Ctrl Pts',(374.778510105951,-15.688181475853,1.07005426349758));
#28166=CARTESIAN_POINT('Ctrl Pts',(374.745286515245,-15.6940292833724,1.18575887267738));
#28167=CARTESIAN_POINT('Ctrl Pts',(374.707004094485,-15.6998770908917,1.29981778597958));
#28168=CARTESIAN_POINT('Ctrl Pts',(374.66885220236,-15.7057049595901,1.4134878013487));
#28169=CARTESIAN_POINT('Ctrl Pts',(374.625676053758,-15.7115328282884,1.52552294033343));
#28170=CARTESIAN_POINT('Ctrl Pts',(374.577646205178,-15.7173606969868,1.63545646516599));
#28171=CARTESIAN_POINT('Ctrl Pts',(374.529622648448,-15.7231878022419,1.74537558884905));
#28172=CARTESIAN_POINT('Ctrl Pts',(374.476746818621,-15.7290149074969,1.8531932755489));
#28173=CARTESIAN_POINT('Ctrl Pts',(374.419237275813,-15.734842012752,1.95846310497352));
#28174=CARTESIAN_POINT('Ctrl Pts',(374.361722022948,-15.7406696965738,2.06374338652139));
#28175=CARTESIAN_POINT('Ctrl Pts',(374.299572336272,-15.7464973803957,2.1664749528619));
#28176=CARTESIAN_POINT('Ctrl Pts',(374.233052264084,-15.7523250642175,2.26623683767535));
#28177=CARTESIAN_POINT('Ctrl Pts',(374.166129090197,-15.7581880629326,2.36660326460515));
#28178=CARTESIAN_POINT('Ctrl Pts',(374.094782607174,-15.7640510616476,2.46396354777857));
#28179=CARTESIAN_POINT('Ctrl Pts',(374.019324687262,-15.7699140603627,2.55792034026346));
#28180=CARTESIAN_POINT('Ctrl Pts',(373.944218004903,-15.7757497682999,2.65143978761619));
#28181=CARTESIAN_POINT('Ctrl Pts',(373.86503838664,-15.7815854762372,2.741587089664));
#28182=CARTESIAN_POINT('Ctrl Pts',(373.782131823879,-15.7874211841744,2.82800597496021));
#28183=CARTESIAN_POINT('Ctrl Pts',(373.698643690396,-15.7932978282784,2.91503106912336));
#28184=CARTESIAN_POINT('Ctrl Pts',(373.611376425383,-15.7991744723824,2.99827494940356));
#28185=CARTESIAN_POINT('Ctrl Pts',(373.520718043089,-15.8050511164864,3.07741433997664));
#28186=CARTESIAN_POINT('Ctrl Pts',(373.430059660795,-15.8109277605903,3.15655373054971));
#28187=CARTESIAN_POINT('Ctrl Pts',(373.336010517313,-15.8168044046943,3.23158841461434));
#28188=CARTESIAN_POINT('Ctrl Pts',(373.23898831715,-15.8226810487983,3.30223938561709));
#28189=CARTESIAN_POINT('Ctrl Pts',(373.14367593233,-15.8284541292206,3.37164527957541));
#28190=CARTESIAN_POINT('Ctrl Pts',(373.045197520102,-15.8342272096428,3.43703669014109));
#28191=CARTESIAN_POINT('Ctrl Pts',(372.943929058018,-15.8400002900651,3.49810885545434));
#28192=CARTESIAN_POINT('Ctrl Pts',(372.842781908308,-15.84576645475,3.55910786068212));
#28193=CARTESIAN_POINT('Ctrl Pts',(372.738851707931,-15.8515326194349,3.61579769575302));
#28194=CARTESIAN_POINT('Ctrl Pts',(372.632545764179,-15.8572987841198,3.66791512718899));
#28195=CARTESIAN_POINT('Ctrl Pts',(372.52292648619,-15.8632446681148,3.72165695011128));
#28196=CARTESIAN_POINT('Ctrl Pts',(372.410781293761,-15.8691905521098,3.77053639578871));
#28197=CARTESIAN_POINT('Ctrl Pts',(372.296587589712,-15.8751364361048,3.81431412153638));
#28198=CARTESIAN_POINT('Ctrl Pts',(372.186018218221,-15.8808936068855,3.85670240959074));
#28199=CARTESIAN_POINT('Ctrl Pts',(372.073528818251,-15.8866507776661,3.89430774825955));
#28200=CARTESIAN_POINT('Ctrl Pts',(371.959575171876,-15.8924079484468,3.92696077989325));
#28201=CARTESIAN_POINT('Ctrl Pts',(371.845655452231,-15.8981634051798,3.95960408993736));
#28202=CARTESIAN_POINT('Ctrl Pts',(371.730272752571,-15.9039188619129,3.98729790965033));
#28203=CARTESIAN_POINT('Ctrl Pts',(371.61389866535,-15.9096743186459,4.00992253757668));
#28204=CARTESIAN_POINT('Ctrl Pts',(371.497530543038,-15.9154294803753,4.03254600584747));
#28205=CARTESIAN_POINT('Ctrl Pts',(371.38017154287,-15.9211846421047,4.05010072040834));
#28206=CARTESIAN_POINT('Ctrl Pts',(371.262303377542,-15.9269398038341,4.06251810961796));
#28207=CARTESIAN_POINT('Ctrl Pts',(371.1444122023,-15.932696089071,4.07493792291771));
#28208=CARTESIAN_POINT('Ctrl Pts',(371.026012078188,-15.938452374308,4.08221837474753));
#28209=CARTESIAN_POINT('Ctrl Pts',(370.907589015783,-15.944208659545,4.08434282801249));
#28210=CARTESIAN_POINT('Ctrl Pts',(370.789055146843,-15.9499703308444,4.08646926909384));
#28211=CARTESIAN_POINT('Ctrl Pts',(370.670498713169,-15.9557320021439,4.08343007586418));
#28212=CARTESIAN_POINT('Ctrl Pts',(370.552404864861,-15.9614936734434,4.07526073607468));
#28213=CARTESIAN_POINT('Ctrl Pts',(370.434244414927,-15.9672585941643,4.06708678900614));
#28214=CARTESIAN_POINT('Ctrl Pts',(370.316547482495,-15.9730235148852,4.05377698180414));
#28215=CARTESIAN_POINT('Ctrl Pts',(370.199791598557,-15.9787884356061,4.03541837138828));
#28216=CARTESIAN_POINT('Ctrl Pts',(370.082884002566,-15.9845608472381,4.01703590587935));
#28217=CARTESIAN_POINT('Ctrl Pts',(369.966920301436,-15.9903332588702,3.9935916289543));
#28218=CARTESIAN_POINT('Ctrl Pts',(369.852365342942,-15.9961056705023,3.96522310438524));
#28219=CARTESIAN_POINT('Ctrl Pts',(369.826604027313,-15.9974037803348,3.9588435419032));
#28220=CARTESIAN_POINT('Ctrl Pts',(369.800913882548,-15.9987018901674,3.95221514738881));
#28221=CARTESIAN_POINT('Ctrl Pts',(369.775300062574,-16.,3.94533982301725));
#28222=CARTESIAN_POINT('Origin',(370.834317853224,-8.23961502859548,0.));
#28223=CARTESIAN_POINT('',(373.320592904309,-14.2030090365224,-3.2412437998941));
#28224=CARTESIAN_POINT('',(373.320592904309,-14.3073933031112,-3.24124379989411));
#28225=CARTESIAN_POINT('',(373.320592904309,-8.23961502859548,-3.24124379989413));
#28226=CARTESIAN_POINT('',(366.750998120586,-15.114615009128,0.00158342508104396));
#28227=CARTESIAN_POINT('Ctrl Pts',(373.320592904309,-14.3073933031112,-3.2412437998941));
#28228=CARTESIAN_POINT('Ctrl Pts',(373.4155069276,-14.3132174492802,-3.16843768511984));
#28229=CARTESIAN_POINT('Ctrl Pts',(373.507298072945,-14.3190415954492,-3.09139940002156));
#28230=CARTESIAN_POINT('Ctrl Pts',(373.59557351228,-14.3248657416181,-3.01043056477479));
#28231=CARTESIAN_POINT('Ctrl Pts',(373.683804553304,-14.3306869585209,-2.92950245296831));
#28232=CARTESIAN_POINT('Ctrl Pts',(373.76852310731,-14.3365081754237,-2.84464799703066));
#28233=CARTESIAN_POINT('Ctrl Pts',(373.849369841393,-14.3423293923265,-2.75620872007897));
#28234=CARTESIAN_POINT('Ctrl Pts',(373.93019681244,-14.3481491862292,-2.66779106216471));
#28235=CARTESIAN_POINT('Ctrl Pts',(374.007153572486,-14.3539689801318,-2.57579062537674));
#28236=CARTESIAN_POINT('Ctrl Pts',(374.079918454935,-14.3597887740345,-2.48058495806416));
#28237=CARTESIAN_POINT('Ctrl Pts',(374.152682438597,-14.3656084960515,-2.385380466724));
#28238=CARTESIAN_POINT('Ctrl Pts',(374.221254401612,-14.3714282180685,-2.28697114614182));
#28239=CARTESIAN_POINT('Ctrl Pts',(374.285354079822,-14.3772479400855,-2.18576621867654));
#28240=CARTESIAN_POINT('Ctrl Pts',(374.349467843428,-14.3830689409403,-2.08453905223224));
#28241=CARTESIAN_POINT('Ctrl Pts',(374.409107150774,-14.388889941795,-1.98051539983543));
#28242=CARTESIAN_POINT('Ctrl Pts',(374.464036361265,-14.3947109426497,-1.87413141278375));
#28243=CARTESIAN_POINT('Ctrl Pts',(374.519020910212,-14.4005378078742,-1.76764024914006));
#28244=CARTESIAN_POINT('Ctrl Pts',(374.569285700624,-14.4063646730986,-1.65878436344289));
#28245=CARTESIAN_POINT('Ctrl Pts',(374.614642079508,-14.4121915383231,-1.548022527023));
#28246=CARTESIAN_POINT('Ctrl Pts',(374.66002376523,-14.4180216546786,-1.43719889043583));
#28247=CARTESIAN_POINT('Ctrl Pts',(374.700491445895,-14.4238517710341,-1.32446756583434));
#28248=CARTESIAN_POINT('Ctrl Pts',(374.735905990116,-14.4296818873896,-1.21030368505693));
#28249=CARTESIAN_POINT('Ctrl Pts',(374.77137150327,-14.4355203945013,-1.09597549858901));
#28250=CARTESIAN_POINT('Ctrl Pts',(374.801769252405,-14.4413589016131,-0.980211030222186));
#28251=CARTESIAN_POINT('Ctrl Pts',(374.827010887024,-14.4471974087248,-0.863497155665468));
#28252=CARTESIAN_POINT('Ctrl Pts',(374.840765699463,-14.4503789606114,-0.799896779631017));
#28253=CARTESIAN_POINT('Ctrl Pts',(374.852990336374,-14.4535605124979,-0.73601461623384));
#28254=CARTESIAN_POINT('Ctrl Pts',(374.863676992061,-14.4567420643845,-0.671930003997587));
#28255=CARTESIAN_POINT('Ctrl Pts',(374.883288111445,-14.4625805414257,-0.554328107007071));
#28256=CARTESIAN_POINT('Ctrl Pts',(374.897776039763,-14.4684190184669,-0.435689439637863));
#28257=CARTESIAN_POINT('Ctrl Pts',(374.907038673679,-14.4742574955081,-0.31649663289538));
#28258=CARTESIAN_POINT('Ctrl Pts',(374.916290115743,-14.4800889180371,-0.197447844379272));
#28259=CARTESIAN_POINT('Ctrl Pts',(374.920328791936,-14.4859203405661,-0.0778466497980785));
#28260=CARTESIAN_POINT('Ctrl Pts',(374.919103830164,-14.4917517630952,0.0418153392558642));
#28261=CARTESIAN_POINT('Ctrl Pts',(374.917880034403,-14.4975776348342,0.161363424959726));
#28262=CARTESIAN_POINT('Ctrl Pts',(374.911402573918,-14.5034035065733,0.280971786323991));
#28263=CARTESIAN_POINT('Ctrl Pts',(374.899672523021,-14.5092293783124,0.400145484495215));
#28264=CARTESIAN_POINT('Ctrl Pts',(374.887892219456,-14.5150802086468,0.519829734259205));
#28265=CARTESIAN_POINT('Ctrl Pts',(374.870814186672,-14.5209310389811,0.639075174990034));
#28266=CARTESIAN_POINT('Ctrl Pts',(374.84849245484,-14.5267818693154,0.757381850679897));
#28267=CARTESIAN_POINT('Ctrl Pts',(374.826288831582,-14.5326017417821,0.875062543012515));
#28268=CARTESIAN_POINT('Ctrl Pts',(374.798896951249,-14.5384216142487,0.991813979705609));
#28269=CARTESIAN_POINT('Ctrl Pts',(374.766421677012,-14.5442414867153,1.10715153386956));
#28270=CARTESIAN_POINT('Ctrl Pts',(374.733950446182,-14.5500606345657,1.22247472767258));
#28271=CARTESIAN_POINT('Ctrl Pts',(374.696397190473,-14.555879782416,1.33638399867441));
#28272=CARTESIAN_POINT('Ctrl Pts',(374.653917103434,-14.5616989302664,1.44840828767009));
#28273=CARTESIAN_POINT('Ctrl Pts',(374.611432441427,-14.5675187048202,1.56044464132213));
#28274=CARTESIAN_POINT('Ctrl Pts',(374.564020036959,-14.5733384793741,1.6705952299558));
#28275=CARTESIAN_POINT('Ctrl Pts',(374.511883617558,-14.579158253928,1.77840800970994));
#28276=CARTESIAN_POINT('Ctrl Pts',(374.459259141037,-14.5850325082954,1.88723004163998));
#28277=CARTESIAN_POINT('Ctrl Pts',(374.401821921722,-14.5909067626628,1.9936698853835));
#28278=CARTESIAN_POINT('Ctrl Pts',(374.339828846594,-14.5967810170301,2.09728817174922));
#28279=CARTESIAN_POINT('Ctrl Pts',(374.278324033849,-14.6026090053037,2.20009035226406));
#28280=CARTESIAN_POINT('Ctrl Pts',(374.212335148662,-14.6084369935772,2.30011495408861));
#28281=CARTESIAN_POINT('Ctrl Pts',(374.142156033178,-14.6142649818508,2.39696298995966));
#28282=CARTESIAN_POINT('Ctrl Pts',(374.071141231333,-14.6201623692651,2.49496428320802));
#28283=CARTESIAN_POINT('Ctrl Pts',(373.995836024069,-14.6260597566794,2.58971253097699));
#28284=CARTESIAN_POINT('Ctrl Pts',(373.916585384865,-14.6319571440936,2.68083044286543));
#28285=CARTESIAN_POINT('Ctrl Pts',(373.83733474566,-14.6378545315079,2.77194835475387));
#28286=CARTESIAN_POINT('Ctrl Pts',(373.754139007523,-14.6437519189222,2.85943566124755));
#28287=CARTESIAN_POINT('Ctrl Pts',(373.667379174618,-14.6496493063365,2.94295575046901));
#28288=CARTESIAN_POINT('Ctrl Pts',(373.581470342212,-14.6554888480927,3.02565661684024));
#28289=CARTESIAN_POINT('Ctrl Pts',(373.491807866047,-14.6613283898488,3.10471728263915));
#28290=CARTESIAN_POINT('Ctrl Pts',(373.398732178978,-14.667167931605,3.1797805216506));
#28291=CARTESIAN_POINT('Ctrl Pts',(373.305768954703,-14.6730004174779,3.25475306220014));
#28292=CARTESIAN_POINT('Ctrl Pts',(373.209401037049,-14.6788329033507,3.32573753190801));
#28293=CARTESIAN_POINT('Ctrl Pts',(373.110005234208,-14.6846653892236,3.39241388159406));
#28294=CARTESIAN_POINT('Ctrl Pts',(373.010704073303,-14.6904923215645,3.45902674390221));
#28295=CARTESIAN_POINT('Ctrl Pts',(372.90838109884,-14.6963192539055,3.52133942339257));
#28296=CARTESIAN_POINT('Ctrl Pts',(372.803445237623,-14.7021461862465,3.57907283301245));
#28297=CARTESIAN_POINT('Ctrl Pts',(372.698086181016,-14.7079966179982,3.63703907545572));
#28298=CARTESIAN_POINT('Ctrl Pts',(372.590093440982,-14.71384704975,3.69038877569886));
#28299=CARTESIAN_POINT('Ctrl Pts',(372.479909696303,-14.7196974815017,3.73888385564343));
#28300=CARTESIAN_POINT('Ctrl Pts',(372.370281772821,-14.7255184007879,3.78713430246696));
#28301=CARTESIAN_POINT('Ctrl Pts',(372.258485276889,-14.731339320074,3.83057883712004));
#28302=CARTESIAN_POINT('Ctrl Pts',(372.144979320168,-14.7371602393601,3.8690297904084));
#28303=CARTESIAN_POINT('Ctrl Pts',(372.031487632652,-14.7429804268795,3.90747590990168));
#28304=CARTESIAN_POINT('Ctrl Pts',(371.916287295908,-14.7488006143988,3.94092956676532));
#28305=CARTESIAN_POINT('Ctrl Pts',(371.799854699615,-14.7546208019182,3.96925227193495));
#28306=CARTESIAN_POINT('Ctrl Pts',(371.683409733934,-14.7604416077537,3.99757798600882));
#28307=CARTESIAN_POINT('Ctrl Pts',(371.565732642494,-14.7662624135892,4.02077156872991));
#28308=CARTESIAN_POINT('Ctrl Pts',(371.447311586607,-14.7720832194248,4.03874531046862));
#28309=CARTESIAN_POINT('Ctrl Pts',(371.327833198053,-14.7779559968301,4.05687953231941));
#28310=CARTESIAN_POINT('Ctrl Pts',(371.207597908311,-14.7838287742354,4.06970016782488));
#28311=CARTESIAN_POINT('Ctrl Pts',(371.087112851483,-14.7897015516407,4.07717054939513));
#28312=CARTESIAN_POINT('Ctrl Pts',(370.967526141216,-14.7955305411314,4.08458523118182));
#28313=CARTESIAN_POINT('Ctrl Pts',(370.847693785369,-14.801359530622,4.0867292250632));
#28314=CARTESIAN_POINT('Ctrl Pts',(370.728111170366,-14.8071885201127,4.08361912285122));
#28315=CARTESIAN_POINT('Ctrl Pts',(370.607181081669,-14.8130831914753,4.08047397557087));
#28316=CARTESIAN_POINT('Ctrl Pts',(370.486506822828,-14.8189778628379,4.07195562526072));
#28317=CARTESIAN_POINT('Ctrl Pts',(370.366593871449,-14.8248725342006,4.05813495054967));
#28318=CARTESIAN_POINT('Ctrl Pts',(370.246680920071,-14.8307672055632,4.04431427583861));
#28319=CARTESIAN_POINT('Ctrl Pts',(370.127529685368,-14.8366618769258,4.0251913982745));
#28320=CARTESIAN_POINT('Ctrl Pts',(370.009632531657,-14.8425565482884,4.00088979108291));
#28321=CARTESIAN_POINT('Ctrl Pts',(369.892848406526,-14.848395569981,3.97681760743967));
#28322=CARTESIAN_POINT('Ctrl Pts',(369.776943225084,-14.8542345916736,3.9475916297344));
#28323=CARTESIAN_POINT('Ctrl Pts',(369.662404075483,-14.8600736133663,3.91329057157011));
#28324=CARTESIAN_POINT('Ctrl Pts',(369.548003167952,-14.8659055877004,3.87903091278187));
#28325=CARTESIAN_POINT('Ctrl Pts',(369.434965397991,-14.8717375620344,3.83970847421784));
#28326=CARTESIAN_POINT('Ctrl Pts',(369.323767765582,-14.8775695363685,3.79545299440327));
#28327=CARTESIAN_POINT('Ctrl Pts',(369.212675849584,-14.8833959662015,3.75123958860044));
#28328=CARTESIAN_POINT('Ctrl Pts',(369.103420965245,-14.8892223960345,3.70210262234209));
#28329=CARTESIAN_POINT('Ctrl Pts',(368.996464494536,-14.8950488258675,3.64822148888457));
#28330=CARTESIAN_POINT('Ctrl Pts',(368.889063897498,-14.900899449383,3.59411661926696));
#28331=CARTESIAN_POINT('Ctrl Pts',(368.783981240067,-14.9067500728986,3.53522821660625));
#28332=CARTESIAN_POINT('Ctrl Pts',(368.681663325772,-14.9126006964141,3.47178678571165));
#28333=CARTESIAN_POINT('Ctrl Pts',(368.579873241038,-14.9184211381959,3.40867263145132));
#28334=CARTESIAN_POINT('Ctrl Pts',(368.480819784953,-14.9242415799778,3.34105253733104));
#28335=CARTESIAN_POINT('Ctrl Pts',(368.384917322237,-14.9300620217596,3.26919899039507));
#28336=CARTESIAN_POINT('Ctrl Pts',(368.289026748465,-14.9358817419864,3.19735435108038));
#28337=CARTESIAN_POINT('Ctrl Pts',(368.196286715538,-14.9417014622132,3.12127754616099));
#28338=CARTESIAN_POINT('Ctrl Pts',(368.107080796817,-14.9475211824399,3.04128312364354));
#28339=CARTESIAN_POINT('Ctrl Pts',(368.01786523648,-14.9533415316777,2.9612800551141));
#28340=CARTESIAN_POINT('Ctrl Pts',(367.93218485183,-14.9591618809154,2.87735879789877));
#28341=CARTESIAN_POINT('Ctrl Pts',(367.850387991427,-14.9649822301532,2.78987232322122));
#28342=CARTESIAN_POINT('Ctrl Pts',(367.767844686665,-14.9708556934938,2.70158748311521));
#28343=CARTESIAN_POINT('Ctrl Pts',(367.689256437514,-14.9767291568344,2.60967232811506));
#28344=CARTESIAN_POINT('Ctrl Pts',(367.614940401454,-14.982602620175,2.51452457196921));
#28345=CARTESIAN_POINT('Ctrl Pts',(367.541192482523,-14.9884311831777,2.42010418333239));
#28346=CARTESIAN_POINT('Ctrl Pts',(367.471651872845,-14.9942597461804,2.32250081356489));
#28347=CARTESIAN_POINT('Ctrl Pts',(367.406584972693,-15.0000883091831,2.22213237673281));
#28348=CARTESIAN_POINT('Ctrl Pts',(367.340766208196,-15.0059842226927,2.12060415744903));
#28349=CARTESIAN_POINT('Ctrl Pts',(367.279525411764,-15.0118801362022,2.01624693487922));
#28350=CARTESIAN_POINT('Ctrl Pts',(367.223090097801,-15.0177760497117,1.90951802779171));
#28351=CARTESIAN_POINT('Ctrl Pts',(367.166654783838,-15.0236719632213,1.80278912070419));
#28352=CARTESIAN_POINT('Ctrl Pts',(367.115025083587,-15.0295678767308,1.69368893601282));
#28353=CARTESIAN_POINT('Ctrl Pts',(367.068377657378,-15.0354637902403,1.58269372947258));
#28354=CARTESIAN_POINT('Ctrl Pts',(367.016191792706,-15.04205972424,1.45852008692533));
#28355=CARTESIAN_POINT('Ctrl Pts',(366.970102395793,-15.0486556582397,1.33164564697758));
#28356=CARTESIAN_POINT('Ctrl Pts',(366.930366771184,-15.0552515922394,1.20265994738413));
#28357=CARTESIAN_POINT('Ctrl Pts',(366.891893348503,-15.061638006427,1.07777147792508));
#28358=CARTESIAN_POINT('Ctrl Pts',(366.859376354993,-15.0680244206146,0.950904109128813));
#28359=CARTESIAN_POINT('Ctrl Pts',(366.833002004882,-15.0744108348021,0.822615634308196));
#28360=CARTESIAN_POINT('Ctrl Pts',(366.805329755343,-15.0811115287079,0.688013997745671));
#28361=CARTESIAN_POINT('Ctrl Pts',(366.784420209559,-15.0878122226137,0.551848059732137));
#28362=CARTESIAN_POINT('Ctrl Pts',(366.770430667765,-15.0945129165194,0.414784213611038));
#28363=CARTESIAN_POINT('Ctrl Pts',(366.757179050395,-15.1008601602717,0.28495025116066));
#28364=CARTESIAN_POINT('Ctrl Pts',(366.750136314589,-15.107207404024,0.154311017285211));
#28365=CARTESIAN_POINT('Ctrl Pts',(366.749385149013,-15.1135546477762,0.0234478584639096));
#28366=CARTESIAN_POINT('Ctrl Pts',(366.749343319898,-15.1139080979298,0.0161606633633095));
#28367=CARTESIAN_POINT('Ctrl Pts',(366.749320987164,-15.1142615480833,0.0088727770423732));
#28368=CARTESIAN_POINT('Ctrl Pts',(366.749318160447,-15.1146149982368,0.00158430095624623));
#28369=CARTESIAN_POINT('Ctrl Pts',(366.75400096471,-15.1146150285955,0.001581859498241));
#28370=CARTESIAN_POINT('Ctrl Pts',(366.757058589183,-15.1525336964611,-0.779441855919802));
#28371=CARTESIAN_POINT('Ctrl Pts',(367.34239529069,-15.2547547783107,-2.88909145754122));
#28372=CARTESIAN_POINT('Ctrl Pts',(370.310628706842,-15.4022674770118,-4.56577064898819));
#28373=CARTESIAN_POINT('Ctrl Pts',(372.576601567184,-15.5118615078473,-3.80106639475913));
#28374=CARTESIAN_POINT('Ctrl Pts',(373.320108995548,-15.5571531246989,-3.24059684932998));
#28375=CARTESIAN_POINT('',(366.749319083349,-15.0103849713759,-0.00317019281932849));
#28376=CARTESIAN_POINT('Ctrl Pts',(366.74931908335,-15.0103849714045,-0.00317019340519376));
#28377=CARTESIAN_POINT('Ctrl Pts',(366.749445164018,-15.0183047899601,-0.165633270565317));
#28378=CARTESIAN_POINT('Ctrl Pts',(366.759266834899,-15.0262246085157,-0.327714073344508));
#28379=CARTESIAN_POINT('Ctrl Pts',(366.778625923479,-15.0341444270713,-0.488454676509938));
#28380=CARTESIAN_POINT('Ctrl Pts',(366.792402197418,-15.0397803117111,-0.602840566793434));
#28381=CARTESIAN_POINT('Ctrl Pts',(366.811007212665,-15.0454161963508,-0.716548464837123));
#28382=CARTESIAN_POINT('Ctrl Pts',(366.83436962688,-15.0510520809906,-0.829240125997579));
#28383=CARTESIAN_POINT('Ctrl Pts',(366.858576260292,-15.0568916227511,-0.946003988899151));
#28384=CARTESIAN_POINT('Ctrl Pts',(366.88793632571,-15.0627311645116,-1.06188295619786));
#28385=CARTESIAN_POINT('Ctrl Pts',(366.922370559218,-15.0685707062721,-1.17638997314475));
#28386=CARTESIAN_POINT('Ctrl Pts',(366.95676318605,-15.0744031921497,-1.29075863195777));
#28387=CARTESIAN_POINT('Ctrl Pts',(366.996217668377,-15.0802356780273,-1.40375825279818));
#28388=CARTESIAN_POINT('Ctrl Pts',(367.04060372864,-15.0860681639049,-1.51491192514104));
#28389=CARTESIAN_POINT('Ctrl Pts',(367.084947525727,-15.091895096251,-1.62595976003662));
#28390=CARTESIAN_POINT('Ctrl Pts',(367.134213407921,-15.0977220285972,-1.73516476894632));
#28391=CARTESIAN_POINT('Ctrl Pts',(367.188221459996,-15.1035489609433,-1.84206571307579));
#28392=CARTESIAN_POINT('Ctrl Pts',(367.242447320851,-15.1093993926933,-1.94939777744238));
#28393=CARTESIAN_POINT('Ctrl Pts',(367.301453561442,-15.1152498244432,-2.0544067577223));
#28394=CARTESIAN_POINT('Ctrl Pts',(367.365009254367,-15.1211002561932,-2.15664620322714));
#28395=CARTESIAN_POINT('Ctrl Pts',(367.428244341091,-15.1269211754856,-2.25836990264289));
#28396=CARTESIAN_POINT('Ctrl Pts',(367.495982863261,-15.1327420947781,-2.35735160143691));
#28397=CARTESIAN_POINT('Ctrl Pts',(367.567951867668,-15.1385630140705,-2.45317717427856));
#28398=CARTESIAN_POINT('Ctrl Pts',(367.63991182462,-15.1443832015965,-2.54899070058106));
#28399=CARTESIAN_POINT('Ctrl Pts',(367.716100962313,-15.1502033891226,-2.64164856601536));
#28400=CARTESIAN_POINT('Ctrl Pts',(367.796204298034,-15.1560235766486,-2.73076747925784));
#28401=CARTESIAN_POINT('Ctrl Pts',(367.876316143657,-15.1618443824913,-2.81989586018564));
#28402=CARTESIAN_POINT('Ctrl Pts',(367.960342742977,-15.1676651883339,-2.90548423976624));
#28403=CARTESIAN_POINT('Ctrl Pts',(368.047930725338,-15.1734859941766,-2.98718458980248));
#28404=CARTESIAN_POINT('Ctrl Pts',(368.136300744367,-15.1793587715737,-3.06961440828514));
#28405=CARTESIAN_POINT('Ctrl Pts',(368.228295756523,-15.1852315489709,-3.14808613079837));
#28406=CARTESIAN_POINT('Ctrl Pts',(368.323517911581,-15.1911043263681,-3.22228314290432));
#28407=CARTESIAN_POINT('Ctrl Pts',(368.41803008263,-15.1969333158669,-3.29592693614968));
#28408=CARTESIAN_POINT('Ctrl Pts',(368.515721068307,-15.2027623053658,-3.36535936023118));
#28409=CARTESIAN_POINT('Ctrl Pts',(368.616172641397,-15.2085912948646,-3.43031439072977));
#28410=CARTESIAN_POINT('Ctrl Pts',(368.717756116491,-15.2144859662109,-3.49600134335739));
#28411=CARTESIAN_POINT('Ctrl Pts',(368.822162406822,-15.2203806375573,-3.55710916142912));
#28412=CARTESIAN_POINT('Ctrl Pts',(368.928934303735,-15.2262753089036,-3.61341092727321));
#28413=CARTESIAN_POINT('Ctrl Pts',(369.035706200648,-15.2321699802499,-3.66971269311731));
#28414=CARTESIAN_POINT('Ctrl Pts',(369.144843297775,-15.2380646515962,-3.72120827599076));
#28415=CARTESIAN_POINT('Ctrl Pts',(369.255869511939,-15.2439593229425,-3.7677215706436));
#28416=CARTESIAN_POINT('Ctrl Pts',(369.365847566344,-15.2497983447529,-3.81379574950711));
#28417=CARTESIAN_POINT('Ctrl Pts',(369.478010271207,-15.2556373665633,-3.8551200400014));
#28418=CARTESIAN_POINT('Ctrl Pts',(369.59191117128,-15.2614763883737,-3.89148437445927));
#28419=CARTESIAN_POINT('Ctrl Pts',(369.705674599643,-15.267308362827,-3.92780481929679));
#28420=CARTESIAN_POINT('Ctrl Pts',(369.821171666416,-15.2731403372803,-3.95917709449356));
#28421=CARTESIAN_POINT('Ctrl Pts',(369.937935431409,-15.2789723117336,-3.98543894117845));
#28422=CARTESIAN_POINT('Ctrl Pts',(370.054588188257,-15.2847987416871,-4.01167582053797));
#28423=CARTESIAN_POINT('Ctrl Pts',(370.172504853425,-15.2906251716406,-4.03281184992711));
#28424=CARTESIAN_POINT('Ctrl Pts',(370.291203339413,-15.2964516015941,-4.0487345708119));
#28425=CARTESIAN_POINT('Ctrl Pts',(370.41039470593,-15.3023022250649,-4.0647234087919));
#28426=CARTESIAN_POINT('Ctrl Pts',(370.530374005577,-15.3081528485358,-4.07545542336444));
#28427=CARTESIAN_POINT('Ctrl Pts',(370.650642323011,-15.3140034720066,-4.0808685717137));
#28428=CARTESIAN_POINT('Ctrl Pts',(370.770290213208,-15.3198239139116,-4.08625379529655));
#28429=CARTESIAN_POINT('Ctrl Pts',(370.890223736736,-15.3256443558165,-4.08637489068034));
#28430=CARTESIAN_POINT('Ctrl Pts',(371.009947045905,-15.3314647977214,-4.08122278081925));
#28431=CARTESIAN_POINT('Ctrl Pts',(371.129655513096,-15.3372845180721,-4.07607130965999));
#28432=CARTESIAN_POINT('Ctrl Pts',(371.249153412593,-15.3431042384227,-4.06564795114866));
#28433=CARTESIAN_POINT('Ctrl Pts',(371.367946560254,-15.3489239587734,-4.0499957287673));
#28434=CARTESIAN_POINT('Ctrl Pts',(371.486752547411,-15.3547443081358,-4.03434181464989));
#28435=CARTESIAN_POINT('Ctrl Pts',(371.604853229119,-15.3605646574981,-4.01345796596198));
#28436=CARTESIAN_POINT('Ctrl Pts',(371.721761797892,-15.3663850068605,-3.9874388076899));
#28437=CARTESIAN_POINT('Ctrl Pts',(371.839737220009,-15.37225847003,-3.9611822106545));
#28438=CARTESIAN_POINT('Ctrl Pts',(371.956498249157,-15.3781319331995,-3.92969618757733));
#28439=CARTESIAN_POINT('Ctrl Pts',(372.071558557242,-15.3840053963689,-3.89312990283148));
#28440=CARTESIAN_POINT('Ctrl Pts',(372.185739279901,-15.389833959497,-3.85684315124237));
#28441=CARTESIAN_POINT('Ctrl Pts',(372.298244830831,-15.395662522625,-3.81555373822405));
#28442=CARTESIAN_POINT('Ctrl Pts',(372.408619367415,-15.4014910857531,-3.76945616003385));
#28443=CARTESIAN_POINT('Ctrl Pts',(372.520269300994,-15.4073869989433,-3.7228259162983));
#28444=CARTESIAN_POINT('Ctrl Pts',(372.629738273915,-15.4132829121335,-3.67127587025088));
#28445=CARTESIAN_POINT('Ctrl Pts',(372.736580287723,-15.4191788253238,-3.61505499685627));
#28446=CARTESIAN_POINT('Ctrl Pts',(372.84342230153,-15.425074738514,-3.55883412346166));
#28447=CARTESIAN_POINT('Ctrl Pts',(372.947637018142,-15.4309706517042,-3.49794268445248));
#28448=CARTESIAN_POINT('Ctrl Pts',(373.04880971793,-15.4368665648944,-3.43267399867086));
#28449=CARTESIAN_POINT('Ctrl Pts',(373.141827518327,-15.4422872453491,-3.37266621397225));
#28450=CARTESIAN_POINT('Ctrl Pts',(373.232535840599,-15.4477079258038,-3.30879011670646));
#28451=CARTESIAN_POINT('Ctrl Pts',(373.320592904309,-15.4531286062585,-3.2412437998941));
#28452=CARTESIAN_POINT('Ctrl Pts',(373.320592904309,-14.2030090365224,-3.2412437998941));
#28453=CARTESIAN_POINT('Ctrl Pts',(373.415661948684,-14.2088303493544,-3.16831877241942));
#28454=CARTESIAN_POINT('Ctrl Pts',(373.507490248051,-14.2146516621864,-3.09123034712973));
#28455=CARTESIAN_POINT('Ctrl Pts',(373.595707336677,-14.2204729750183,-3.01030781161584));
#28456=CARTESIAN_POINT('Ctrl Pts',(373.68401509969,-14.2263002713166,-2.9293020994593));
#28457=CARTESIAN_POINT('Ctrl Pts',(373.768703942294,-14.2321275676148,-2.84445468371928));
#28458=CARTESIAN_POINT('Ctrl Pts',(373.849439872622,-14.237954863913,-2.75613211006633));
#28459=CARTESIAN_POINT('Ctrl Pts',(373.930223816119,-14.243785625669,-2.66775701151394));
#28460=CARTESIAN_POINT('Ctrl Pts',(374.007049904298,-14.249616387425,-2.57590294867633));
#28461=CARTESIAN_POINT('Ctrl Pts',(374.079625113568,-14.255447149181,-2.48096871926246));
#28462=CARTESIAN_POINT('Ctrl Pts',(374.152301446089,-14.2612860352758,-2.38590221247615));
#28463=CARTESIAN_POINT('Ctrl Pts',(374.220714842523,-14.2671249213706,-2.28774730236853));
#28464=CARTESIAN_POINT('Ctrl Pts',(374.284616060351,-14.2729638074654,-2.18693101900744));
#28465=CARTESIAN_POINT('Ctrl Pts',(374.308179772959,-14.2751169093712,-2.14975479595475));
#28466=CARTESIAN_POINT('Ctrl Pts',(374.33113038291,-14.277270011277,-2.11221691717924));
#28467=CARTESIAN_POINT('Ctrl Pts',(374.353457011468,-14.2794231131828,-2.0743395539091));
#28468=CARTESIAN_POINT('Ctrl Pts',(374.414002743556,-14.2852619316506,-1.97162307422052));
#28469=CARTESIAN_POINT('Ctrl Pts',(374.470138951498,-14.2911007501185,-1.86609867768021));
#28470=CARTESIAN_POINT('Ctrl Pts',(374.521596995379,-14.2969395685863,-1.75818017501912));
#28471=CARTESIAN_POINT('Ctrl Pts',(374.572992873776,-14.3027713332887,-1.6503920466457));
#28472=CARTESIAN_POINT('Ctrl Pts',(374.61972165767,-14.3086030979912,-1.54021592911404));
#28473=CARTESIAN_POINT('Ctrl Pts',(374.66155929608,-14.3144348626936,-1.42809241230507));
#28474=CARTESIAN_POINT('Ctrl Pts',(374.703357114699,-14.3202610768998,-1.31607561124884));
#28475=CARTESIAN_POINT('Ctrl Pts',(374.740272909339,-14.326087291106,-1.20211547697434));
#28476=CARTESIAN_POINT('Ctrl Pts',(374.772129915253,-14.3319135053122,-1.08667435974978));
#28477=CARTESIAN_POINT('Ctrl Pts',(374.804120817757,-14.3377642073881,-0.970748037734786));
#28478=CARTESIAN_POINT('Ctrl Pts',(374.831010134972,-14.3436149094641,-0.853328630028726));
#28479=CARTESIAN_POINT('Ctrl Pts',(374.852668752218,-14.34946561154,-0.734902070040746));
#28480=CARTESIAN_POINT('Ctrl Pts',(374.874214503778,-14.3552858248963,-0.617092645251532));
#28481=CARTESIAN_POINT('Ctrl Pts',(374.890583876499,-14.3611060382526,-0.498286944619419));
#28482=CARTESIAN_POINT('Ctrl Pts',(374.901700669401,-14.3669262516088,-0.378974968389545));
#28483=CARTESIAN_POINT('Ctrl Pts',(374.912816075906,-14.372745739115,-0.259677871786943));
#28484=CARTESIAN_POINT('Ctrl Pts',(374.918680168094,-14.3785652266213,-0.139875029038302));
#28485=CARTESIAN_POINT('Ctrl Pts',(374.91926859001,-14.3843847141275,-0.0200618551361105));
#28486=CARTESIAN_POINT('Ctrl Pts',(374.919857075127,-14.3902048266986,0.0997641877711278));
#28487=CARTESIAN_POINT('Ctrl Pts',(374.91516876131,-14.3960249392698,0.219600158360798));
#28488=CARTESIAN_POINT('Ctrl Pts',(374.905231417739,-14.4018450518409,0.338950955513449));
#28489=CARTESIAN_POINT('Ctrl Pts',(374.895202449701,-14.4077188271154,0.459402192965573));
#28490=CARTESIAN_POINT('Ctrl Pts',(374.879827188809,-14.4135926023899,0.579358844228589));
#28491=CARTESIAN_POINT('Ctrl Pts',(374.859187531011,-14.4194663776644,0.698318750165522));
#28492=CARTESIAN_POINT('Ctrl Pts',(374.838707599901,-14.425294696823,0.816358046270801));
#28493=CARTESIAN_POINT('Ctrl Pts',(374.813044612295,-14.4311230159817,0.933415583774485));
#28494=CARTESIAN_POINT('Ctrl Pts',(374.782329488656,-14.4369513351403,1.04901340625064));
#28495=CARTESIAN_POINT('Ctrl Pts',(374.751255035805,-14.4428478384727,1.16596358123228));
#28496=CARTESIAN_POINT('Ctrl Pts',(374.715009612851,-14.4487443418051,1.28141926077883));
#28497=CARTESIAN_POINT('Ctrl Pts',(374.67377953316,-14.4546408451375,1.39490465921606));
#28498=CARTESIAN_POINT('Ctrl Pts',(374.632549453469,-14.4605373484699,1.50839005765328));
#28499=CARTESIAN_POINT('Ctrl Pts',(374.586334930723,-14.4664338518024,1.61990480424541));
#28500=CARTESIAN_POINT('Ctrl Pts',(374.535370478715,-14.4723303551348,1.72899810970076));
#28501=CARTESIAN_POINT('Ctrl Pts',(374.484903841064,-14.4781692621642,1.83702580546745));
#28502=CARTESIAN_POINT('Ctrl Pts',(374.429627465073,-14.4840081691935,1.943005024189));
#28503=CARTESIAN_POINT('Ctrl Pts',(374.369730689474,-14.4898470762229,2.04648016782015));
#28504=CARTESIAN_POINT('Ctrl Pts',(374.309906274741,-14.4956789293105,2.14983030387002));
#28505=CARTESIAN_POINT('Ctrl Pts',(374.245472766137,-14.501510782398,2.2506820344613));
#28506=CARTESIAN_POINT('Ctrl Pts',(374.176666805362,-14.5073426354855,2.34860138851618));
#28507=CARTESIAN_POINT('Ctrl Pts',(374.107926334413,-14.5131689377889,2.44642754248648));
#28508=CARTESIAN_POINT('Ctrl Pts',(374.034821923996,-14.5189952400923,2.54132654307397));
#28509=CARTESIAN_POINT('Ctrl Pts',(373.95763490541,-14.5248215423956,2.63289110893821));
#28510=CARTESIAN_POINT('Ctrl Pts',(373.880125076856,-14.5306722113411,2.72483861425343));
#28511=CARTESIAN_POINT('Ctrl Pts',(373.798498624598,-14.5365228802866,2.81342337494466));
#28512=CARTESIAN_POINT('Ctrl Pts',(373.713083257921,-14.542373549232,2.89826409161019));
#28513=CARTESIAN_POINT('Ctrl Pts',(373.628111252513,-14.548193849403,2.98266442981435));
#28514=CARTESIAN_POINT('Ctrl Pts',(373.539389870294,-14.554014149574,3.06335921760744));
#28515=CARTESIAN_POINT('Ctrl Pts',(373.447280121202,-14.5598344497451,3.14000846911619));
#28516=CARTESIAN_POINT('Ctrl Pts',(373.355181869303,-14.5656540234228,3.21664815322072));
#28517=CARTESIAN_POINT('Ctrl Pts',(373.259696403656,-14.5714735971006,3.28924304615679));
#28518=CARTESIAN_POINT('Ctrl Pts',(373.161218522421,-14.5772931707783,3.35749285564257));
#28519=CARTESIAN_POINT('Ctrl Pts',(373.062730076529,-14.583113368777,3.42574998693326));
#28520=CARTESIAN_POINT('Ctrl Pts',(372.961248910181,-14.5889335667757,3.48966087688044));
#28521=CARTESIAN_POINT('Ctrl Pts',(372.857199044004,-14.5947537647743,3.54896839771591));
#28522=CARTESIAN_POINT('Ctrl Pts',(372.752193548181,-14.600627417467,3.60882061915788));
#28523=CARTESIAN_POINT('Ctrl Pts',(372.644572289829,-14.6065010701597,3.6639842669187));
#28524=CARTESIAN_POINT('Ctrl Pts',(372.534795674837,-14.6123747228524,3.71424288088465));
#28525=CARTESIAN_POINT('Ctrl Pts',(372.425864780562,-14.6182031248351,3.76411430172139));
#28526=CARTESIAN_POINT('Ctrl Pts',(372.314812024559,-14.6240315268178,3.80915590334672));
#28527=CARTESIAN_POINT('Ctrl Pts',(372.20210562926,-14.6298599288005,3.84920532054668));
#28528=CARTESIAN_POINT('Ctrl Pts',(372.088086684375,-14.6357562068482,3.88972114292145));
#28529=CARTESIAN_POINT('Ctrl Pts',(371.972375749005,-14.6416524848959,3.92512764102816));
#28530=CARTESIAN_POINT('Ctrl Pts',(371.855470507816,-14.6475487629436,3.95530937551278));
#28531=CARTESIAN_POINT('Ctrl Pts',(371.738565266627,-14.6534450409913,3.98549110999739));
#28532=CARTESIAN_POINT('Ctrl Pts',(371.620466146087,-14.659341319039,4.01044804739018));
#28533=CARTESIAN_POINT('Ctrl Pts',(371.501677478411,-14.6652375970867,4.03011862488805));
#28534=CARTESIAN_POINT('Ctrl Pts',(371.384044436807,-14.6710765136641,4.04959783874287));
#28535=CARTESIAN_POINT('Ctrl Pts',(371.265380472658,-14.6769154302414,4.06395187513785));
#28536=CARTESIAN_POINT('Ctrl Pts',(371.146168404866,-14.6827543468188,4.07307920785252));
#28537=CARTESIAN_POINT('Ctrl Pts',(371.027100336288,-14.688586210424,4.08219551543557));
#28538=CARTESIAN_POINT('Ctrl Pts',(370.907485882455,-14.6944180740292,4.08609764807583));
#28539=CARTESIAN_POINT('Ctrl Pts',(370.787816779592,-14.7002499376343,4.08473532192122));
#28540=CARTESIAN_POINT('Ctrl Pts',(370.66826155876,-14.7060762513987,4.0833742922121));
#28541=CARTESIAN_POINT('Ctrl Pts',(370.548652195972,-14.7119025651631,4.07675877654074));
#28542=CARTESIAN_POINT('Ctrl Pts',(370.429483691496,-14.7177288789274,4.06489044151223));
#28543=CARTESIAN_POINT('Ctrl Pts',(370.309817118944,-14.7235795439321,4.05297250244768));
#28544=CARTESIAN_POINT('Ctrl Pts',(370.190595510944,-14.7294302089367,4.03575770788277));
#28545=CARTESIAN_POINT('Ctrl Pts',(370.072318666318,-14.7352808739413,4.0133006664283));
#28546=CARTESIAN_POINT('Ctrl Pts',(369.95465539979,-14.7411011877819,3.99096012409794));
#28547=CARTESIAN_POINT('Ctrl Pts',(369.837927518439,-14.7469215016226,3.96343168110069));
#28548=CARTESIAN_POINT('Ctrl Pts',(369.72261958799,-14.7527418154632,3.93082077524223));
#28549=CARTESIAN_POINT('Ctrl Pts',(369.607326034435,-14.7585614036119,3.89821393539673));
#28550=CARTESIAN_POINT('Ctrl Pts',(369.493452469857,-14.7643809917605,3.86052600369593));
#28551=CARTESIAN_POINT('Ctrl Pts',(369.381469834352,-14.7702005799092,3.81791273264077));
#28552=CARTESIAN_POINT('Ctrl Pts',(369.269475170411,-14.7760207931597,3.7752948843487));
#28553=CARTESIAN_POINT('Ctrl Pts',(369.159372218528,-14.7818410064102,3.72775078908034));
#28554=CARTESIAN_POINT('Ctrl Pts',(369.051612848481,-14.7876612196608,3.67548471171662));
#28555=CARTESIAN_POINT('Ctrl Pts',(368.942864392941,-14.7935348546089,3.62273890234619));
#28556=CARTESIAN_POINT('Ctrl Pts',(368.836503142544,-14.7994084895571,3.56518416254497));
#28557=CARTESIAN_POINT('Ctrl Pts',(368.732967999565,-14.8052821245052,3.50307775998863));
#28558=CARTESIAN_POINT('Ctrl Pts',(368.63022988261,-14.8111105435028,3.44144946001386));
#28559=CARTESIAN_POINT('Ctrl Pts',(368.530274821467,-14.8169389625003,3.37533960636082));
#28560=CARTESIAN_POINT('Ctrl Pts',(368.433501534976,-14.8227673814978,3.30504251198595));
#28561=CARTESIAN_POINT('Ctrl Pts',(368.335602120762,-14.8286636244213,3.23392738703963));
#28562=CARTESIAN_POINT('Ctrl Pts',(368.240959337544,-14.8345598673448,3.15852721721278));
#28563=CARTESIAN_POINT('Ctrl Pts',(368.149949857687,-14.8404561102682,3.07918714347423));
#28564=CARTESIAN_POINT('Ctrl Pts',(368.05894037783,-14.8463523531917,2.99984706973568));
#28565=CARTESIAN_POINT('Ctrl Pts',(367.971564470121,-14.8522485961152,2.91656742484888));
#28566=CARTESIAN_POINT('Ctrl Pts',(367.888158136163,-14.8581448390387,2.82972930181761));
#28567=CARTESIAN_POINT('Ctrl Pts',(367.806660262009,-14.863906167237,2.74487816298118));
#28568=CARTESIAN_POINT('Ctrl Pts',(367.728691228059,-14.8696674954354,2.6563575941899));
#28569=CARTESIAN_POINT('Ctrl Pts',(367.654603693653,-14.8754288236337,2.56449661014033));
#28570=CARTESIAN_POINT('Ctrl Pts',(367.580625533572,-14.8811816464689,2.4727712390961));
#28571=CARTESIAN_POINT('Ctrl Pts',(367.510517729518,-14.8869344693041,2.37771558942559));
#28572=CARTESIAN_POINT('Ctrl Pts',(367.44459590751,-14.8926872921393,2.27969518373436));
#28573=CARTESIAN_POINT('Ctrl Pts',(367.37872953369,-14.8984352761579,2.18175722500505));
#28574=CARTESIAN_POINT('Ctrl Pts',(367.317042376498,-14.9041832601765,2.08085981096543));
#28575=CARTESIAN_POINT('Ctrl Pts',(367.259809457048,-14.909931244195,1.9774010027479));
#28576=CARTESIAN_POINT('Ctrl Pts',(367.202610438528,-14.9156758234947,1.87400347656646));
#28577=CARTESIAN_POINT('Ctrl Pts',(367.149860614512,-14.9214204027943,1.76804793698009));
#28578=CARTESIAN_POINT('Ctrl Pts',(367.101790944581,-14.927164982094,1.65996020321443));
#28579=CARTESIAN_POINT('Ctrl Pts',(367.053737790816,-14.9329075876247,1.55190960710544));
#28580=CARTESIAN_POINT('Ctrl Pts',(367.010361762391,-14.9386501931554,1.4417286554423));
#28581=CARTESIAN_POINT('Ctrl Pts',(366.971846879343,-14.944392798686,1.32986577364936));
#28582=CARTESIAN_POINT('Ctrl Pts',(366.933322274463,-14.9501368537509,1.21797465570625));
#28583=CARTESIAN_POINT('Ctrl Pts',(366.899661410976,-14.9558809088158,1.10440115207591));
#28584=CARTESIAN_POINT('Ctrl Pts',(366.870999241777,-14.9616249638807,0.989611329846685));
#28585=CARTESIAN_POINT('Ctrl Pts',(366.842334210192,-14.9673695925835,0.87481004397493));
#28586=CARTESIAN_POINT('Ctrl Pts',(366.818668959252,-14.9731142212863,0.758792605684265));
#28587=CARTESIAN_POINT('Ctrl Pts',(366.800087550079,-14.9788588499891,0.642036495215628));
#28588=CARTESIAN_POINT('Ctrl Pts',(366.781489033254,-14.9846087676939,0.525172888972658));
#28589=CARTESIAN_POINT('Ctrl Pts',(366.767983764793,-14.9903586853988,0.407569666818465));
#28590=CARTESIAN_POINT('Ctrl Pts',(366.759604034958,-14.9961086031037,0.289710716467365));
#28591=CARTESIAN_POINT('Ctrl Pts',(366.752668740967,-15.0008673925278,0.192167420153659));
#28592=CARTESIAN_POINT('Ctrl Pts',(366.749243325144,-15.0056261819518,0.0944491614589898));
#28593=CARTESIAN_POINT('Ctrl Pts',(366.749319083349,-15.0103849713759,-0.00317019281933907));
#28594=CARTESIAN_POINT('Origin',(370.834317853224,-8.23961502859548,0.));
#28595=CARTESIAN_POINT('',(373.320592904309,-12.9531485432512,-3.24124379989409));
#28596=CARTESIAN_POINT('',(373.320592904309,-13.0571931311057,-3.2412437998941));
#28597=CARTESIAN_POINT('',(373.320592904309,-8.23961502859548,-3.24124379989413));
#28598=CARTESIAN_POINT('',(366.749318109676,-13.864615028561,-0.00144748442786206));
#28599=CARTESIAN_POINT('Ctrl Pts',(373.320592904309,-13.0571931311057,-3.2412437998941));
#28600=CARTESIAN_POINT('Ctrl Pts',(373.415634712958,-13.0630222050237,-3.16833966424664));
#28601=CARTESIAN_POINT('Ctrl Pts',(373.507397375535,-13.0688512789417,-3.09130541218824));
#28602=CARTESIAN_POINT('Ctrl Pts',(373.595519638687,-13.0746803528596,-3.01047997833458));
#28603=CARTESIAN_POINT('Ctrl Pts',(373.683775086311,-13.0805182366072,-2.92953238814687));
#28604=CARTESIAN_POINT('Ctrl Pts',(373.76837885436,-13.0863561203548,-2.84478245481835));
#28605=CARTESIAN_POINT('Ctrl Pts',(373.849007325584,-13.0921940041024,-2.75660522839973));
#28606=CARTESIAN_POINT('Ctrl Pts',(373.9143684516,-13.0969264596419,-2.68512473620953));
#28607=CARTESIAN_POINT('Ctrl Pts',(373.977117920218,-13.1016589151815,-2.61139273980695));
#28608=CARTESIAN_POINT('Ctrl Pts',(374.03710392341,-13.106391370721,-2.53562347138149));
#28609=CARTESIAN_POINT('Ctrl Pts',(374.111114034853,-13.1122302255079,-2.44214013023974));
#28610=CARTESIAN_POINT('Ctrl Pts',(374.181139475934,-13.1180690802947,-2.34527280419094));
#28611=CARTESIAN_POINT('Ctrl Pts',(374.246857595481,-13.1239079350815,-2.24539473311907));
#28612=CARTESIAN_POINT('Ctrl Pts',(374.312496322541,-13.1297397360878,-2.14563732235193));
#28613=CARTESIAN_POINT('Ctrl Pts',(374.373837858353,-13.1355715370941,-2.04287673835842));
#28614=CARTESIAN_POINT('Ctrl Pts',(374.43060006475,-13.1414033381003,-1.9375188399243));
#28615=CARTESIAN_POINT('Ctrl Pts',(374.487308246335,-13.1472295885481,-1.83226121843365));
#28616=CARTESIAN_POINT('Ctrl Pts',(374.539445579219,-13.1530558389958,-1.72441155653902));
#28617=CARTESIAN_POINT('Ctrl Pts',(374.586773795764,-13.1588820894436,-1.61440372871605));
#28618=CARTESIAN_POINT('Ctrl Pts',(374.634300528992,-13.1647327779115,-1.50393447659702));
#28619=CARTESIAN_POINT('Ctrl Pts',(374.676977486266,-13.1705834663794,-1.39128926017079));
#28620=CARTESIAN_POINT('Ctrl Pts',(374.714610386602,-13.1764341548473,-1.27693181313962));
#28621=CARTESIAN_POINT('Ctrl Pts',(374.752047494974,-13.1822544040512,-1.16316933139164));
#28622=CARTESIAN_POINT('Ctrl Pts',(374.784492787487,-13.188074653255,-1.04771278505638));
#28623=CARTESIAN_POINT('Ctrl Pts',(374.811803840143,-13.1938949024589,-0.931037176413037));
#28624=CARTESIAN_POINT('Ctrl Pts',(374.839111485795,-13.1997144255973,-0.814376122839463));
#28625=CARTESIAN_POINT('Ctrl Pts',(374.861286073291,-13.2055339487357,-0.696496704403742));
#28626=CARTESIAN_POINT('Ctrl Pts',(374.878235797962,-13.2113534718741,-0.57788636965012));
#28627=CARTESIAN_POINT('Ctrl Pts',(374.895187342422,-13.2171736198197,-0.459263300418008));
#28628=CARTESIAN_POINT('Ctrl Pts',(374.906912851315,-13.2229937677653,-0.33990956043577));
#28629=CARTESIAN_POINT('Ctrl Pts',(374.91337219933,-13.2288139157109,-0.220319407936235));
#28630=CARTESIAN_POINT('Ctrl Pts',(374.91989100824,-13.2346876404578,-0.0996283800139154));
#28631=CARTESIAN_POINT('Ctrl Pts',(374.921046175616,-13.2405613652046,0.0213030153844473));
#28632=CARTESIAN_POINT('Ctrl Pts',(374.916850230376,-13.2464350899514,0.141966156199758));
#28633=CARTESIAN_POINT('Ctrl Pts',(374.912686696418,-13.2522634435269,0.261697243117249));
#28634=CARTESIAN_POINT('Ctrl Pts',(374.903254520544,-13.2580917971023,0.381163802454329));
#28635=CARTESIAN_POINT('Ctrl Pts',(374.888618103044,-13.2639201506777,0.499874468553034));
#28636=CARTESIAN_POINT('Ctrl Pts',(374.873810778426,-13.2698165610103,0.619971300206968));
#28637=CARTESIAN_POINT('Ctrl Pts',(374.853676970586,-13.2757129713428,0.73929405099517));
#28638=CARTESIAN_POINT('Ctrl Pts',(374.828336241694,-13.2816093816754,0.857345970167816));
#28639=CARTESIAN_POINT('Ctrl Pts',(374.802995512802,-13.2875057920079,0.975397889340462));
#28640=CARTESIAN_POINT('Ctrl Pts',(374.772448023863,-13.2934022023404,1.09217858049311));
#28641=CARTESIAN_POINT('Ctrl Pts',(374.73686449609,-13.299298612673,1.20720946825777));
#28642=CARTESIAN_POINT('Ctrl Pts',(374.701628305141,-13.3051374671486,1.3211175201024));
#28643=CARTESIAN_POINT('Ctrl Pts',(374.661347710689,-13.3109763216242,1.4336533651992));
#28644=CARTESIAN_POINT('Ctrl Pts',(374.61614803537,-13.3168151760998,1.54433981798324));
#28645=CARTESIAN_POINT('Ctrl Pts',(374.571002964228,-13.3226469768556,1.6548925542618));
#28646=CARTESIAN_POINT('Ctrl Pts',(374.520950786023,-13.3284787776115,1.7635999700876));
#28647=CARTESIAN_POINT('Ctrl Pts',(374.466166637357,-13.3343105783674,1.86999984203066));
#28648=CARTESIAN_POINT('Ctrl Pts',(374.411434630269,-13.3401368286253,1.97629844640786));
#28649=CARTESIAN_POINT('Ctrl Pts',(374.351979798616,-13.3459630788833,2.08029351793484));
#28650=CARTESIAN_POINT('Ctrl Pts',(374.288025195678,-13.3517893291412,2.1815431677319));
#28651=CARTESIAN_POINT('Ctrl Pts',(374.223802334092,-13.357640017703,2.28321751087358));
#28652=CARTESIAN_POINT('Ctrl Pts',(374.155042026257,-13.3634907062649,2.38212296678474));
#28653=CARTESIAN_POINT('Ctrl Pts',(374.082016828196,-13.3693413948267,2.47783703418227));
#28654=CARTESIAN_POINT('Ctrl Pts',(374.009371558597,-13.3751616439899,2.57305312965482));
#28655=CARTESIAN_POINT('Ctrl Pts',(373.932505926946,-13.3809818931532,2.66511064520723));
#28656=CARTESIAN_POINT('Ctrl Pts',(373.851731111693,-13.3868021423164,2.75362347237566));
#28657=CARTESIAN_POINT('Ctrl Pts',(373.770966372169,-13.3926216654705,2.84212525858524));
#28658=CARTESIAN_POINT('Ctrl Pts',(373.686293692495,-13.3984411886245,2.92708293641963));
#28659=CARTESIAN_POINT('Ctrl Pts',(373.598063144806,-13.4042607117785,3.00814510342507));
#28660=CARTESIAN_POINT('Ctrl Pts',(373.509823123481,-13.4100808597958,3.08921597437034));
#28661=CARTESIAN_POINT('Ctrl Pts',(373.418024773309,-13.4159010078132,3.16639022837159));
#28662=CARTESIAN_POINT('Ctrl Pts',(373.323053011204,-13.4217211558306,3.23935523112764));
#28663=CARTESIAN_POINT('Ctrl Pts',(373.227206994545,-13.4275948807301,3.31299190706824));
#28664=CARTESIAN_POINT('Ctrl Pts',(373.128129170963,-13.4334686056296,3.38234117696181));
#28665=CARTESIAN_POINT('Ctrl Pts',(373.02624608336,-13.4393423305292,3.44712570614027));
#28666=CARTESIAN_POINT('Ctrl Pts',(372.925149983459,-13.4451706843139,3.51140981244237));
#28667=CARTESIAN_POINT('Ctrl Pts',(372.821292189772,-13.4509990380987,3.57119929880891));
#28668=CARTESIAN_POINT('Ctrl Pts',(372.715114351455,-13.4568273918834,3.62626936840638));
#28669=CARTESIAN_POINT('Ctrl Pts',(372.60769669301,-13.4627238023403,3.68198248161638));
#28670=CARTESIAN_POINT('Ctrl Pts',(372.497904851588,-13.4686202127972,3.73286507992408));
#28671=CARTESIAN_POINT('Ctrl Pts',(372.386216115876,-13.4745166232542,3.77873481239129));
#28672=CARTESIAN_POINT('Ctrl Pts',(372.274527380164,-13.4804130337111,3.82460454485849));
#28673=CARTESIAN_POINT('Ctrl Pts',(372.160942168137,-13.486309444168,3.86546132006785));
#28674=CARTESIAN_POINT('Ctrl Pts',(372.045951713958,-13.4922058546249,3.90117525721697));
#28675=CARTESIAN_POINT('Ctrl Pts',(371.932083590863,-13.4980447148722,3.93654061880763));
#28676=CARTESIAN_POINT('Ctrl Pts',(371.816494090411,-13.5038835751196,3.96696979634805));
#28677=CARTESIAN_POINT('Ctrl Pts',(371.699647624774,-13.5097224353669,3.99229625484738));
#28678=CARTESIAN_POINT('Ctrl Pts',(371.582942317908,-13.5155542418593,4.01759211719896));
#28679=CARTESIAN_POINT('Ctrl Pts',(371.46498346001,-13.5213860483518,4.03779743825467));
#28680=CARTESIAN_POINT('Ctrl Pts',(371.346251297956,-13.5272178548442,4.05279522652758));
#28681=CARTESIAN_POINT('Ctrl Pts',(371.227632141643,-13.5330441107966,4.06777874035151));
#28682=CARTESIAN_POINT('Ctrl Pts',(371.108241546071,-13.538870366749,4.07756453259185));
#28683=CARTESIAN_POINT('Ctrl Pts',(370.988570089168,-13.5446966227014,4.08208662912804));
#28684=CARTESIAN_POINT('Ctrl Pts',(370.868396829967,-13.5505473091129,4.08662768756622));
#28685=CARTESIAN_POINT('Ctrl Pts',(370.747940753732,-13.5563979955243,4.08586072260642));
#28686=CARTESIAN_POINT('Ctrl Pts',(370.627704445442,-13.5622486819358,4.07977154994303));
#28687=CARTESIAN_POINT('Ctrl Pts',(370.508093532916,-13.5680689366537,4.07371404943293));
#28688=CARTESIAN_POINT('Ctrl Pts',(370.388700516253,-13.5738891913715,4.06238960520887));
#28689=CARTESIAN_POINT('Ctrl Pts',(370.270019813719,-13.5797094460894,4.04583646760595));
#28690=CARTESIAN_POINT('Ctrl Pts',(370.151353916506,-13.5855289747351,4.02928539499355));
#28691=CARTESIAN_POINT('Ctrl Pts',(370.033400558351,-13.5913485033809,4.00750698262282));
#28692=CARTESIAN_POINT('Ctrl Pts',(369.916647533344,-13.5971680320267,3.98059118524009));
#28693=CARTESIAN_POINT('Ctrl Pts',(369.799881973539,-13.6029881854667,3.95367249813293));
#28694=CARTESIAN_POINT('Ctrl Pts',(369.684317398419,-13.6088083389067,3.92161542049096));
#28695=CARTESIAN_POINT('Ctrl Pts',(369.570429337899,-13.6146284923467,3.88456056984963));
#28696=CARTESIAN_POINT('Ctrl Pts',(369.455493151723,-13.6205022093658,3.84716469891608));
#28697=CARTESIAN_POINT('Ctrl Pts',(369.342264898922,-13.626375926385,3.80467871715061));
#28698=CARTESIAN_POINT('Ctrl Pts',(369.231214537902,-13.6322496434042,3.75729753418646));
#28699=CARTESIAN_POINT('Ctrl Pts',(369.121021730229,-13.6380780023927,3.71028223829959));
#28700=CARTESIAN_POINT('Ctrl Pts',(369.012973638525,-13.6439063613811,3.65844731053448));
#28701=CARTESIAN_POINT('Ctrl Pts',(368.907505440725,-13.6497347203696,3.60202983427953));
#28702=CARTESIAN_POINT('Ctrl Pts',(368.800806065393,-13.6556311164041,3.54495377154423));
#28703=CARTESIAN_POINT('Ctrl Pts',(368.696747568476,-13.6615275124386,3.48318770888157));
#28704=CARTESIAN_POINT('Ctrl Pts',(368.595750276169,-13.6674239084732,3.4170221250319));
#28705=CARTESIAN_POINT('Ctrl Pts',(368.494752983861,-13.6733203045077,3.35085654118224));
#28706=CARTESIAN_POINT('Ctrl Pts',(368.396817207948,-13.6792167005423,3.28029172913517));
#28707=CARTESIAN_POINT('Ctrl Pts',(368.302327890809,-13.6851130965768,3.20565934407081));
#28708=CARTESIAN_POINT('Ctrl Pts',(368.209633776792,-13.6908974669465,3.13244490015359));
#28709=CARTESIAN_POINT('Ctrl Pts',(368.119964495517,-13.6966818373162,3.05508541895734));
#28710=CARTESIAN_POINT('Ctrl Pts',(368.03371601442,-13.7024662076859,2.97386185632225));
#28711=CARTESIAN_POINT('Ctrl Pts',(367.947572413299,-13.7082435441389,2.89273706325591));
#28712=CARTESIAN_POINT('Ctrl Pts',(367.864841639667,-13.714020880592,2.80775781424708));
#28713=CARTESIAN_POINT('Ctrl Pts',(367.785888110422,-13.719798217045,2.71924642193395));
#28714=CARTESIAN_POINT('Ctrl Pts',(367.703426535092,-13.7258322508582,2.62680231063686));
#28715=CARTESIAN_POINT('Ctrl Pts',(367.625085979366,-13.7318662846714,2.53050519941724));
#28716=CARTESIAN_POINT('Ctrl Pts',(367.551240700248,-13.7379003184845,2.43076724669488));
#28717=CARTESIAN_POINT('Ctrl Pts',(367.480651420613,-13.7436682985808,2.33542695793263));
#28718=CARTESIAN_POINT('Ctrl Pts',(367.414169730435,-13.7494362786771,2.2369431626848));
#28719=CARTESIAN_POINT('Ctrl Pts',(367.352082186995,-13.7552042587734,2.13571059950636));
#28720=CARTESIAN_POINT('Ctrl Pts',(367.290014383364,-13.7609704050264,2.03451022171223));
#28721=CARTESIAN_POINT('Ctrl Pts',(367.232338165302,-13.7667365512794,1.9305631664438));
#28722=CARTESIAN_POINT('Ctrl Pts',(367.179296528996,-13.7725026975325,1.82429277240197));
#28723=CARTESIAN_POINT('Ctrl Pts',(367.126258799186,-13.7782684191111,1.71803020513293));
#28724=CARTESIAN_POINT('Ctrl Pts',(367.077855156735,-13.7840341406897,1.60944501046251));
#28725=CARTESIAN_POINT('Ctrl Pts',(367.034282094525,-13.7897998622683,1.49898406682881));
#28726=CARTESIAN_POINT('Ctrl Pts',(366.990701597061,-13.7955665677025,1.38850427427539));
#28727=CARTESIAN_POINT('Ctrl Pts',(366.951953469599,-13.8013332731368,1.27614848225212));
#28728=CARTESIAN_POINT('Ctrl Pts',(366.918185362683,-13.8070999785711,1.1623817430307));
#28729=CARTESIAN_POINT('Ctrl Pts',(366.884386361119,-13.8128719599997,1.04851091791767));
#28730=CARTESIAN_POINT('Ctrl Pts',(366.855576592803,-13.8186439414283,0.933226966533934));
#28731=CARTESIAN_POINT('Ctrl Pts',(366.831853294486,-13.824415922857,0.817008234991934));
#28732=CARTESIAN_POINT('Ctrl Pts',(366.808117223194,-13.8301910120057,0.700726929567399));
#28733=CARTESIAN_POINT('Ctrl Pts',(366.789473140479,-13.8359661011544,0.583510250425359));
#28734=CARTESIAN_POINT('Ctrl Pts',(366.775966572866,-13.8417411903032,0.465843198103686));
#28735=CARTESIAN_POINT('Ctrl Pts',(366.762442319589,-13.8475238414239,0.348022071111352));
#28736=CARTESIAN_POINT('Ctrl Pts',(366.7540690373,-13.8533064925447,0.229749806177949));
#28737=CARTESIAN_POINT('Ctrl Pts',(366.750840186333,-13.8590891436655,0.11151297683367));
#28738=CARTESIAN_POINT('Ctrl Pts',(366.749811692746,-13.8609311052973,0.0738507180229249));
#28739=CARTESIAN_POINT('Ctrl Pts',(366.74930477244,-13.8627730669292,0.0361920264922796));
#28740=CARTESIAN_POINT('Ctrl Pts',(366.749318109676,-13.864615028561,-0.00144748442786197));
#28741=CARTESIAN_POINT('Ctrl Pts',(366.749318109676,-13.8646150285955,-0.00144748513296822));
#28742=CARTESIAN_POINT('Ctrl Pts',(366.749350464652,-13.8690834652399,-0.0927576226328301));
#28743=CARTESIAN_POINT('Ctrl Pts',(366.752444184748,-13.8735519018843,-0.184007250062436));
#28744=CARTESIAN_POINT('Ctrl Pts',(366.75858808408,-13.8780203385288,-0.275048811866955));
#28745=CARTESIAN_POINT('Ctrl Pts',(366.766616196763,-13.8838591569996,-0.394011034000072));
#28746=CARTESIAN_POINT('Ctrl Pts',(366.779869115059,-13.8896979754705,-0.51280090005843));
#28747=CARTESIAN_POINT('Ctrl Pts',(366.798334899559,-13.8955367939414,-0.630925191859141));
#28748=CARTESIAN_POINT('Ctrl Pts',(366.816778375896,-13.9013685586469,-0.748906779952974));
#28749=CARTESIAN_POINT('Ctrl Pts',(366.840422128447,-13.9072003233524,-0.866223995644971));
#28750=CARTESIAN_POINT('Ctrl Pts',(366.869202296336,-13.9130320880579,-0.982386696024231));
#28751=CARTESIAN_POINT('Ctrl Pts',(366.897955072137,-13.9188583022672,-1.09843883627878));
#28752=CARTESIAN_POINT('Ctrl Pts',(366.931834439113,-13.9246845164764,-1.21333825579321));
#28753=CARTESIAN_POINT('Ctrl Pts',(366.97072522258,-13.9305107306857,-1.32660355209665));
#28754=CARTESIAN_POINT('Ctrl Pts',(367.009779465928,-13.9363614327605,-1.44034490802412));
#28755=CARTESIAN_POINT('Ctrl Pts',(367.053887280941,-13.9422121348353,-1.55243796460567));
#28756=CARTESIAN_POINT('Ctrl Pts',(367.102880849631,-13.9480628369101,-1.66240876087073));
#28757=CARTESIAN_POINT('Ctrl Pts',(367.151619106916,-13.9538830502694,-1.77180648602832));
#28758=CARTESIAN_POINT('Ctrl Pts',(367.205192143526,-13.9597032636287,-1.879103646418));
#28759=CARTESIAN_POINT('Ctrl Pts',(367.263386173736,-13.965523476988,-1.9838528021074));
#28760=CARTESIAN_POINT('Ctrl Pts',(367.321572946456,-13.9713429644973,-2.0885888943268));
#28761=CARTESIAN_POINT('Ctrl Pts',(367.38437936936,-13.9771624520065,-2.19077725943343));
#28762=CARTESIAN_POINT('Ctrl Pts',(367.451545809899,-13.9829819395158,-2.28999526263686));
#28763=CARTESIAN_POINT('Ctrl Pts',(367.518719464713,-13.9888020520899,-2.38922392273988));
#28764=CARTESIAN_POINT('Ctrl Pts',(367.590253840866,-13.9946221646641,-2.4854812506462));
#28765=CARTESIAN_POINT('Ctrl Pts',(367.665846462443,-14.0004422772383,-2.57837430288916));
#28766=CARTESIAN_POINT('Ctrl Pts',(367.742136064331,-14.0063160525085,-2.67212384915385));
#28767=CARTESIAN_POINT('Ctrl Pts',(367.822558871191,-14.0121898277787,-2.76244643184495));
#28768=CARTESIAN_POINT('Ctrl Pts',(367.906763749228,-14.0180636030489,-2.84897384476831));
#28769=CARTESIAN_POINT('Ctrl Pts',(367.990316980597,-14.0238919222105,-2.93483163733683));
#28770=CARTESIAN_POINT('Ctrl Pts',(368.077593612437,-14.029720241372,-3.01695255774001));
#28771=CARTESIAN_POINT('Ctrl Pts',(368.168215715381,-14.0355485605336,-3.09501605659609));
#28772=CARTESIAN_POINT('Ctrl Pts',(368.259897985426,-14.0414450638581,-3.1739928023382));
#28773=CARTESIAN_POINT('Ctrl Pts',(368.355004165594,-14.0473415671826,-3.24881632189692));
#28774=CARTESIAN_POINT('Ctrl Pts',(368.453111834642,-14.0532380705072,-3.31919913489236));
#28775=CARTESIAN_POINT('Ctrl Pts',(368.55121950369,-14.0591345738317,-3.3895819478878));
#28776=CARTESIAN_POINT('Ctrl Pts',(368.652328275925,-14.0650310771562,-3.45552386899358));
#28777=CARTESIAN_POINT('Ctrl Pts',(368.755990062825,-14.0709275804807,-3.51678526436531));
#28778=CARTESIAN_POINT('Ctrl Pts',(368.858639294538,-14.0767664875085,-3.57744826619613));
#28779=CARTESIAN_POINT('Ctrl Pts',(368.964101496172,-14.0826053945363,-3.63370479082797));
#28780=CARTESIAN_POINT('Ctrl Pts',(369.071963148423,-14.0884443015642,-3.68528572765585));
#28781=CARTESIAN_POINT('Ctrl Pts',(369.179694493783,-14.0942761546502,-3.73680434992329));
#28782=CARTESIAN_POINT('Ctrl Pts',(369.2898191601,-14.1001080077363,-3.78365844746453));
#28783=CARTESIAN_POINT('Ctrl Pts',(369.401896798964,-14.1059398608223,-3.82562346857523));
#28784=CARTESIAN_POINT('Ctrl Pts',(369.513867761825,-14.1117661631242,-3.86754854718911));
#28785=CARTESIAN_POINT('Ctrl Pts',(369.627787620653,-14.1175924654262,-3.90459366688072));
#28786=CARTESIAN_POINT('Ctrl Pts',(369.743194213509,-14.1234187677281,-3.93658153768663));
#28787=CARTESIAN_POINT('Ctrl Pts',(369.859083457493,-14.1292694366741,-3.96870318752134));
#28788=CARTESIAN_POINT('Ctrl Pts',(369.976471524561,-14.1351201056201,-3.99572501662337));
#28789=CARTESIAN_POINT('Ctrl Pts',(370.094872646103,-14.1409707745661,-4.01751736594451));
#28790=CARTESIAN_POINT('Ctrl Pts',(370.212659188833,-14.1467910747359,-4.03919659880189));
#28791=CARTESIAN_POINT('Ctrl Pts',(370.331447889633,-14.1526113749056,-4.05570044669782));
#28792=CARTESIAN_POINT('Ctrl Pts',(370.450748823307,-14.1584316750753,-4.06695215109405));
#28793=CARTESIAN_POINT('Ctrl Pts',(370.570034865771,-14.1642512487518,-4.07820245104606));
#28794=CARTESIAN_POINT('Ctrl Pts',(370.689832610125,-14.1700708224283,-4.08420187357412));
#28795=CARTESIAN_POINT('Ctrl Pts',(370.809646657491,-14.1758903961048,-4.08492549896578));
#28796=CARTESIAN_POINT('Ctrl Pts',(370.929473558449,-14.1817105941023,-4.08564920198762));
#28797=CARTESIAN_POINT('Ctrl Pts',(371.049316360235,-14.1875307920998,-4.08109598008354));
#28798=CARTESIAN_POINT('Ctrl Pts',(371.168679918398,-14.1933509900972,-4.0712930389954));
#28799=CARTESIAN_POINT('Ctrl Pts',(371.28913975247,-14.1992246427919,-4.06140006432988));
#28800=CARTESIAN_POINT('Ctrl Pts',(371.409111074852,-14.2050982954865,-4.0461604745554));
#28801=CARTESIAN_POINT('Ctrl Pts',(371.528091673987,-14.2109719481811,-4.02565558457548));
#28802=CARTESIAN_POINT('Ctrl Pts',(371.646155644711,-14.2168003501627,-4.00530866459122));
#28803=CARTESIAN_POINT('Ctrl Pts',(371.763243717384,-14.2226287521444,-3.97977743425995));
#28804=CARTESIAN_POINT('Ctrl Pts',(371.878877773692,-14.228457154126,-3.94919226836981));
#28805=CARTESIAN_POINT('Ctrl Pts',(371.995858474459,-14.2343534321771,-3.91825091550933));
#28806=CARTESIAN_POINT('Ctrl Pts',(372.111350668757,-14.2402497102282,-3.88213729285527));
#28807=CARTESIAN_POINT('Ctrl Pts',(372.224878418643,-14.2461459882793,-3.84103714039612));
#28808=CARTESIAN_POINT('Ctrl Pts',(372.338406168528,-14.2520422663304,-3.79993698793697));
#28809=CARTESIAN_POINT('Ctrl Pts',(372.449969103123,-14.2579385443815,-3.75385051885361));
#28810=CARTESIAN_POINT('Ctrl Pts',(372.559116219245,-14.2638348224326,-3.70301169274025));
#28811=CARTESIAN_POINT('Ctrl Pts',(372.667208109033,-14.2696740956988,-3.65266437267868));
#28812=CARTESIAN_POINT('Ctrl Pts',(372.773256689999,-14.2755133689651,-3.59750437989767));
#28813=CARTESIAN_POINT('Ctrl Pts',(372.876806066402,-14.2813526422313,-3.53772057955799));
#28814=CARTESIAN_POINT('Ctrl Pts',(372.980216768418,-14.2871840954829,-3.47801684229699));
#28815=CARTESIAN_POINT('Ctrl Pts',(373.081134578619,-14.2930155487344,-3.41370182303264));
#28816=CARTESIAN_POINT('Ctrl Pts',(373.179125350556,-14.298847001986,-3.34501162934537));
#28817=CARTESIAN_POINT('Ctrl Pts',(373.226995558795,-14.3016957690278,-3.31145526673294));
#28818=CARTESIAN_POINT('Ctrl Pts',(373.274167568559,-14.3045445360695,-3.27685548514191));
#28819=CARTESIAN_POINT('Ctrl Pts',(373.320592904309,-14.3073933031112,-3.2412437998941));
#28820=CARTESIAN_POINT('',(366.749318910897,-13.7603849713562,0.00293958966507201));
#28821=CARTESIAN_POINT('Ctrl Pts',(366.749318910896,-13.7603849714045,0.00293958867138478));
#28822=CARTESIAN_POINT('Ctrl Pts',(366.749233092332,-13.7661811969052,-0.116318166152711));
#28823=CARTESIAN_POINT('Ctrl Pts',(366.754373994896,-13.7719774224059,-0.235652147899815));
#28824=CARTESIAN_POINT('Ctrl Pts',(366.764734942895,-13.7777736479066,-0.354570072003375));
#28825=CARTESIAN_POINT('Ctrl Pts',(366.775093077567,-13.7835682995473,-0.47345570609983));
#28826=CARTESIAN_POINT('Ctrl Pts',(366.790668403739,-13.789362951188,-0.591925099556149));
#28827=CARTESIAN_POINT('Ctrl Pts',(366.811402223152,-13.7951576028288,-0.709489135451252));
#28828=CARTESIAN_POINT('Ctrl Pts',(366.832135340407,-13.8009520582315,-0.827049189997007));
#28829=CARTESIAN_POINT('Ctrl Pts',(366.858026532062,-13.8067465136342,-0.943703544737596));
#28830=CARTESIAN_POINT('Ctrl Pts',(366.888965739009,-13.8125409690369,-1.05897199909083));
#28831=CARTESIAN_POINT('Ctrl Pts',(366.919911251373,-13.818336605351,-1.17426394518391));
#28832=CARTESIAN_POINT('Ctrl Pts',(366.955906718432,-13.8241322416652,-1.28816903385626));
#28833=CARTESIAN_POINT('Ctrl Pts',(366.996792032616,-13.8299278779794,-1.40022161680409));
#28834=CARTESIAN_POINT('Ctrl Pts',(367.037719238015,-13.8357294525199,-1.51238900916566));
#28835=CARTESIAN_POINT('Ctrl Pts',(367.08354615477,-13.8415310270605,-1.62269972028456));
#28836=CARTESIAN_POINT('Ctrl Pts',(367.134064194678,-13.8473326016011,-1.73070733008778));
#28837=CARTESIAN_POINT('Ctrl Pts',(367.184610154335,-13.8531373824913,-1.8387746323355));
#28838=CARTESIAN_POINT('Ctrl Pts',(367.239852212216,-13.8589421633816,-1.94453593504841));
#28839=CARTESIAN_POINT('Ctrl Pts',(367.299536225143,-13.8647469442719,-2.04757022877807));
#28840=CARTESIAN_POINT('Ctrl Pts',(367.359310356431,-13.8705604899438,-2.15076009652668));
#28841=CARTESIAN_POINT('Ctrl Pts',(367.423539618352,-13.8763740356158,-2.25121438642522));
#28842=CARTESIAN_POINT('Ctrl Pts',(367.491926831069,-13.8821875812877,-2.3485415165621));
#28843=CARTESIAN_POINT('Ctrl Pts',(367.536710380988,-13.8859945972848,-2.41227644912965));
#28844=CARTESIAN_POINT('Ctrl Pts',(367.583276142426,-13.8898016132819,-2.47467100927438));
#28845=CARTESIAN_POINT('Ctrl Pts',(367.631531783043,-13.893608629279,-2.53562347138825));
#28846=CARTESIAN_POINT('Ctrl Pts',(367.7055419637,-13.8994474895263,-2.62910689995473));
#28847=CARTESIAN_POINT('Ctrl Pts',(367.78376005255,-13.9052863497737,-2.7194883031148));
#28848=CARTESIAN_POINT('Ctrl Pts',(367.865896788345,-13.911125210021,-2.80636800537333));
#28849=CARTESIAN_POINT('Ctrl Pts',(367.947934297171,-13.9169570165134,-2.89314275082489));
#28850=CARTESIAN_POINT('Ctrl Pts',(368.03388075901,-13.9227888230059,-2.97642391827985));
#28851=CARTESIAN_POINT('Ctrl Pts',(368.12340586915,-13.9286206294983,-3.05584378111874));
#28852=CARTESIAN_POINT('Ctrl Pts',(368.212845771952,-13.9344468854507,-3.13518805449391));
#28853=CARTESIAN_POINT('Ctrl Pts',(368.305857244036,-13.9402731414031,-3.21067806775095));
#28854=CARTESIAN_POINT('Ctrl Pts',(368.402072647356,-13.9460993973555,-3.28198236718782));
#28855=CARTESIAN_POINT('Ctrl Pts',(368.498691497845,-13.951950083767,-3.35358565739715));
#28856=CARTESIAN_POINT('Ctrl Pts',(368.598540923152,-13.9578007701785,-3.42096775296308));
#28857=CARTESIAN_POINT('Ctrl Pts',(368.701214132483,-13.96365145659,-3.4838331642831));
#28858=CARTESIAN_POINT('Ctrl Pts',(368.803353298552,-13.9694717113078,-3.54637158816914));
#28859=CARTESIAN_POINT('Ctrl Pts',(368.908286589121,-13.9752919660257,-3.60443999606237));
#28860=CARTESIAN_POINT('Ctrl Pts',(369.015584346616,-13.9811122207435,-3.65779078569854));
#28861=CARTESIAN_POINT('Ctrl Pts',(369.122868718803,-13.9869317493893,-3.71113491986678));
#28862=CARTESIAN_POINT('Ctrl Pts',(369.232516607959,-13.9927512780351,-3.75976242596029));
#28863=CARTESIAN_POINT('Ctrl Pts',(369.344074628949,-13.9985708066808,-3.80347211538398));
#28864=CARTESIAN_POINT('Ctrl Pts',(369.455644626994,-14.0043909601208,-3.8471864975522));
#28865=CARTESIAN_POINT('Ctrl Pts',(369.569124786904,-14.0102111135608,-3.88598186527154));
#28866=CARTESIAN_POINT('Ctrl Pts',(369.684043239005,-14.0160312670008,-3.91970576853471));
#28867=CARTESIAN_POINT('Ctrl Pts',(369.800019299583,-14.02190498402,-3.95374003697664));
#28868=CARTESIAN_POINT('Ctrl Pts',(369.917459859636,-14.0277787010391,-3.98260889101293));
#28869=CARTESIAN_POINT('Ctrl Pts',(370.035866992001,-14.0336524180583,-4.00620783562352));
#28870=CARTESIAN_POINT('Ctrl Pts',(370.153359760542,-14.0394807770468,-4.02962454441117));
#28871=CARTESIAN_POINT('Ctrl Pts',(370.271803812536,-14.0453091360352,-4.04785244622414));
#28872=CARTESIAN_POINT('Ctrl Pts',(370.390706113024,-14.0511374950237,-4.06084149209945));
#28873=CARTESIAN_POINT('Ctrl Pts',(370.510996413344,-14.0570338910582,-4.07398216492748));
#28874=CARTESIAN_POINT('Ctrl Pts',(370.631755301709,-14.0629302870927,-4.08176086392417));
#28875=CARTESIAN_POINT('Ctrl Pts',(370.752471851296,-14.0688266831273,-4.08417999505018));
#28876=CARTESIAN_POINT('Ctrl Pts',(370.873188400882,-14.0747230791618,-4.08659912617619));
#28877=CARTESIAN_POINT('Ctrl Pts',(370.993862188928,-14.0806194751964,-4.08365875519713));
#28878=CARTESIAN_POINT('Ctrl Pts',(371.113988241904,-14.0865158712309,-4.07541525168848));
#28879=CARTESIAN_POINT('Ctrl Pts',(371.232928481495,-14.0923540615293,-4.06725312317356));
#28880=CARTESIAN_POINT('Ctrl Pts',(371.351690459257,-14.0981922518276,-4.05386751480068));
#28881=CARTESIAN_POINT('Ctrl Pts',(371.46978113535,-14.104030442126,-4.03527092238788));
#28882=CARTESIAN_POINT('Ctrl Pts',(371.587736952339,-14.1098619652332,-4.01669556721319));
#28883=CARTESIAN_POINT('Ctrl Pts',(371.70502259486,-14.1156934883403,-3.99292112540638));
#28884=CARTESIAN_POINT('Ctrl Pts',(371.821148058735,-14.1215250114475,-3.96401200117885));
#28885=CARTESIAN_POINT('Ctrl Pts',(371.937167875275,-14.1273512292163,-3.93512917757356));
#28886=CARTESIAN_POINT('Ctrl Pts',(372.052029221206,-14.1331774469851,-3.90112106157912));
#28887=CARTESIAN_POINT('Ctrl Pts',(372.165250828261,-14.1390036647538,-3.86210336681422));
#28888=CARTESIAN_POINT('Ctrl Pts',(372.278394693045,-14.1448258820194,-3.82311246308595));
#28889=CARTESIAN_POINT('Ctrl Pts',(372.389900677209,-14.150648099285,-3.77911895777986));
#28890=CARTESIAN_POINT('Ctrl Pts',(372.49930185826,-14.1564703165505,-3.73028862998216));
#28891=CARTESIAN_POINT('Ctrl Pts',(372.608658062249,-14.1622901401835,-3.68147837733061));
#28892=CARTESIAN_POINT('Ctrl Pts',(372.715910815491,-14.1681099638165,-3.62783542500394));
#28893=CARTESIAN_POINT('Ctrl Pts',(372.820612903843,-14.1739297874495,-3.5695737801434));
#28894=CARTESIAN_POINT('Ctrl Pts',(372.925315203698,-14.1797496228389,-3.51131201759125));
#28895=CARTESIAN_POINT('Ctrl Pts',(373.027466470007,-14.1855694582282,-3.44843173395799));
#28896=CARTESIAN_POINT('Ctrl Pts',(373.126644151864,-14.1913892936176,-3.38119285764115));
#28897=CARTESIAN_POINT('Ctrl Pts',(373.192649407338,-14.1952625412525,-3.33644368498476));
#28898=CARTESIAN_POINT('Ctrl Pts',(373.257338109058,-14.1991357888874,-3.28976493221356));
#28899=CARTESIAN_POINT('Ctrl Pts',(373.320592904309,-14.2030090365224,-3.2412437998941));
#28900=CARTESIAN_POINT('Ctrl Pts',(373.320592904309,-12.9531485432512,-3.2412437998941));
#28901=CARTESIAN_POINT('Ctrl Pts',(373.415389105552,-12.9589780536625,-3.16852806339356));
#28902=CARTESIAN_POINT('Ctrl Pts',(373.507099306673,-12.9648075640739,-3.09156831113415));
#28903=CARTESIAN_POINT('Ctrl Pts',(373.595325455516,-12.9706370744852,-3.01065807093533));
#28904=CARTESIAN_POINT('Ctrl Pts',(373.683476099339,-12.9764615959301,-2.92981707471166));
#28905=CARTESIAN_POINT('Ctrl Pts',(373.768148326379,-12.982286117375,-2.84503259115645));
#28906=CARTESIAN_POINT('Ctrl Pts',(373.848976665281,-12.9881106388198,-2.75663875886719));
#28907=CARTESIAN_POINT('Ctrl Pts',(373.929761206976,-12.993932004221,-2.66829282318176));
#28908=CARTESIAN_POINT('Ctrl Pts',(374.006705730902,-12.9997533696222,-2.57634172817591));
#28909=CARTESIAN_POINT('Ctrl Pts',(374.079481548501,-13.0055747350234,-2.48115650269327));
#28910=CARTESIAN_POINT('Ctrl Pts',(374.152237640405,-13.0113945225588,-2.3859970769167));
#28911=CARTESIAN_POINT('Ctrl Pts',(374.220827027024,-13.0172143100941,-2.28760558614071));
#28912=CARTESIAN_POINT('Ctrl Pts',(374.284961616153,-13.0230340976295,-2.18638574395216));
#28913=CARTESIAN_POINT('Ctrl Pts',(374.34909370896,-13.0288536586401,-2.08516984156239));
#28914=CARTESIAN_POINT('Ctrl Pts',(374.408771132333,-13.0346732196508,-1.98112614958709));
#28915=CARTESIAN_POINT('Ctrl Pts',(374.46374974405,-13.0404927806615,-1.87468641373873));
#28916=CARTESIAN_POINT('Ctrl Pts',(374.518738977417,-13.0463134659884,-1.76822611415268));
#28917=CARTESIAN_POINT('Ctrl Pts',(374.569027407677,-13.0521341513154,-1.65936921051655));
#28918=CARTESIAN_POINT('Ctrl Pts',(374.614417649656,-13.0579548366423,-1.54857047918815));
#28919=CARTESIAN_POINT('Ctrl Pts',(374.659853002979,-13.0637813068896,-1.43766162992624));
#28920=CARTESIAN_POINT('Ctrl Pts',(374.700380292053,-13.069607777137,-1.32480747475849));
#28921=CARTESIAN_POINT('Ctrl Pts',(374.735850874107,-13.0754342473843,-1.2104813451526));
#28922=CARTESIAN_POINT('Ctrl Pts',(374.771340403745,-13.0812638300007,-1.09609414510564));
#28923=CARTESIAN_POINT('Ctrl Pts',(374.801767741011,-13.087093412617,-0.980233796070421));
#28924=CARTESIAN_POINT('Ctrl Pts',(374.827034985985,-13.0929229952334,-0.863385717831531));
#28925=CARTESIAN_POINT('Ctrl Pts',(374.852339369046,-13.0987611462372,-0.746365894946289));
#28926=CARTESIAN_POINT('Ctrl Pts',(374.87246844124,-13.104599297241,-0.628355842638248));
#28927=CARTESIAN_POINT('Ctrl Pts',(374.887375904404,-13.1104374482449,-0.509848441956565));
#28928=CARTESIAN_POINT('Ctrl Pts',(374.897200083234,-13.1142848526537,-0.431750788168268));
#28929=CARTESIAN_POINT('Ctrl Pts',(374.904757614425,-13.1181322570625,-0.353437235778988));
#28930=CARTESIAN_POINT('Ctrl Pts',(374.910047622374,-13.1219796614713,-0.275048811783993));
#28931=CARTESIAN_POINT('Ctrl Pts',(374.918075800169,-13.127818527299,-0.156085624782912));
#28932=CARTESIAN_POINT('Ctrl Pts',(374.920903302936,-13.1336573931267,-0.0365912520044337));
#28933=CARTESIAN_POINT('Ctrl Pts',(374.918475698036,-13.1394962589545,0.082943948910298));
#28934=CARTESIAN_POINT('Ctrl Pts',(374.916051025807,-13.1453280711314,0.202334745143395));
#28935=CARTESIAN_POINT('Ctrl Pts',(374.90838388312,-13.1511598833084,0.32176586896938));
#28936=CARTESIAN_POINT('Ctrl Pts',(374.89547170126,-13.1569916954854,0.440743034634737));
#28937=CARTESIAN_POINT('Ctrl Pts',(374.882571808608,-13.1628179572177,0.559606963427308));
#28938=CARTESIAN_POINT('Ctrl Pts',(374.864436852962,-13.16864421895,0.678017392453952));
#28939=CARTESIAN_POINT('Ctrl Pts',(374.841116288482,-13.1744704806823,0.795481803196109));
#28940=CARTESIAN_POINT('Ctrl Pts',(374.817697968761,-13.1803211649632,0.913438601751774));
#28941=CARTESIAN_POINT('Ctrl Pts',(374.789050479173,-13.1861718492441,1.03044101940979));
#28942=CARTESIAN_POINT('Ctrl Pts',(374.755276435948,-13.1920225335249,1.14599685538825));
#28943=CARTESIAN_POINT('Ctrl Pts',(374.721678017938,-13.1978427942147,1.26095180037127));
#28944=CARTESIAN_POINT('Ctrl Pts',(374.683006359508,-13.2036630549045,1.37447478173989));
#28945=CARTESIAN_POINT('Ctrl Pts',(374.639413194194,-13.2094833155943,1.48609368686157));
#28946=CARTESIAN_POINT('Ctrl Pts',(374.595825466632,-13.2153028502725,1.59769866879066));
#28947=CARTESIAN_POINT('Ctrl Pts',(374.547317600993,-13.2211223849508,1.70739966916459));
#28948=CARTESIAN_POINT('Ctrl Pts',(374.494090094668,-13.2269419196291,1.81474299578722));
#28949=CARTESIAN_POINT('Ctrl Pts',(374.44085687327,-13.2327620791546,1.92209784793244));
#28950=CARTESIAN_POINT('Ctrl Pts',(374.382903183838,-13.23858223868,2.02709415955572));
#28951=CARTESIAN_POINT('Ctrl Pts',(374.320475967924,-13.2444023982055,2.12930190421862));
#28952=CARTESIAN_POINT('Ctrl Pts',(374.257474381133,-13.2502761069737,2.2324500264256));
#28953=CARTESIAN_POINT('Ctrl Pts',(374.189916741048,-13.2561498157418,2.33275764285162));
#28954=CARTESIAN_POINT('Ctrl Pts',(374.118101511986,-13.2620235245099,2.42981272579799));
#28955=CARTESIAN_POINT('Ctrl Pts',(374.046840679252,-13.2678518896564,2.52611856680229));
#28956=CARTESIAN_POINT('Ctrl Pts',(373.971388066244,-13.2736802548028,2.61922163617767));
#28957=CARTESIAN_POINT('Ctrl Pts',(373.892075109945,-13.2795086199493,2.7087535064988));
#28958=CARTESIAN_POINT('Ctrl Pts',(373.811836593065,-13.2854050005283,2.79933018934163));
#28959=CARTESIAN_POINT('Ctrl Pts',(373.727647358567,-13.2913013811073,2.88625148480409));
#28960=CARTESIAN_POINT('Ctrl Pts',(373.639887342266,-13.2971977616862,2.96917578498761));
#28961=CARTESIAN_POINT('Ctrl Pts',(373.552127325965,-13.3030941422652,3.05210008517112));
#28962=CARTESIAN_POINT('Ctrl Pts',(373.460796885094,-13.3089905228442,3.13102715464025));
#28963=CARTESIAN_POINT('Ctrl Pts',(373.366307815629,-13.3148869034232,3.20565934407867));
#28964=CARTESIAN_POINT('Ctrl Pts',(373.272740512783,-13.320725763203,3.27956347617355));
#28965=CARTESIAN_POINT('Ctrl Pts',(373.175793742295,-13.3265646229828,3.34947909213848));
#28966=CARTESIAN_POINT('Ctrl Pts',(373.075841111034,-13.3324034827626,3.41508396451658));
#28967=CARTESIAN_POINT('Ctrl Pts',(372.976009228044,-13.3382352888789,3.48060958260274));
#28968=CARTESIAN_POINT('Ctrl Pts',(372.873179044464,-13.3440670949951,3.54183459581339));
#28969=CARTESIAN_POINT('Ctrl Pts',(372.767756739998,-13.3498989011114,3.59847732674655));
#28970=CARTESIAN_POINT('Ctrl Pts',(372.662434771708,-13.3557251567786,3.65506614769307));
#28971=CARTESIAN_POINT('Ctrl Pts',(372.554525946849,-13.3615514124459,3.70708117289297));
#28972=CARTESIAN_POINT('Ctrl Pts',(372.444464410948,-13.3673776681131,3.75428462728229));
#28973=CARTESIAN_POINT('Ctrl Pts',(372.333941360669,-13.3732283546657,3.80168601706065));
#28974=CARTESIAN_POINT('Ctrl Pts',(372.221247852402,-13.3790790412183,3.84423516805264));
#28975=CARTESIAN_POINT('Ctrl Pts',(372.106847839179,-13.3849297277708,3.88173832642591));
#28976=CARTESIAN_POINT('Ctrl Pts',(371.99304286882,-13.3907499824277,3.91904641500757));
#28977=CARTESIAN_POINT('Ctrl Pts',(371.877549495946,-13.3965702370845,3.95136075995291));
#28978=CARTESIAN_POINT('Ctrl Pts',(371.760842884978,-13.4023904917413,3.97853947643273));
#28979=CARTESIAN_POINT('Ctrl Pts',(371.644150831371,-13.4082100204105,4.00571480278401));
#28980=CARTESIAN_POINT('Ctrl Pts',(371.526246235741,-13.4140295490797,4.02775568302582));
#28981=CARTESIAN_POINT('Ctrl Pts',(371.407616651283,-13.4198490777489,4.04457086575872));
#28982=CARTESIAN_POINT('Ctrl Pts',(371.288974328835,-13.4256692312968,4.06138785404145));
#28983=CARTESIAN_POINT('Ctrl Pts',(371.169607264439,-13.4314893848447,4.07297797222377));
#28984=CARTESIAN_POINT('Ctrl Pts',(371.050009762303,-13.4373095383925,4.07930165596487));
#28985=CARTESIAN_POINT('Ctrl Pts',(370.929311587348,-13.4431832556411,4.08568353746661));
#28986=CARTESIAN_POINT('Ctrl Pts',(370.808379131339,-13.4490569728896,4.08670152332728));
#28987=CARTESIAN_POINT('Ctrl Pts',(370.687720999121,-13.4549306901382,4.08236871955081));
#28988=CARTESIAN_POINT('Ctrl Pts',(370.567994611619,-13.4607590494411,4.07806937449732));
#28989=CARTESIAN_POINT('Ctrl Pts',(370.448538728588,-13.4665874087439,4.06850168216696));
#28990=CARTESIAN_POINT('Ctrl Pts',(370.329844643048,-13.4724157680468,4.05373060035005));
#28991=CARTESIAN_POINT('Ctrl Pts',(370.209764990935,-13.4783121642682,4.03878708940899));
#28992=CARTESIAN_POINT('Ctrl Pts',(370.090465457346,-13.4842085604896,4.01851800387922));
#28993=CARTESIAN_POINT('Ctrl Pts',(369.972442652823,-13.490104956711,3.99304346819986));
#28994=CARTESIAN_POINT('Ctrl Pts',(369.8544198483,-13.4960013529323,3.96756893252049));
#28995=CARTESIAN_POINT('Ctrl Pts',(369.737674169058,-13.5018977491537,3.93688910814501));
#28996=CARTESIAN_POINT('Ctrl Pts',(369.622683992498,-13.5077941453751,3.90117525721957));
#28997=CARTESIAN_POINT('Ctrl Pts',(369.508815975897,-13.5136330001618,3.86580992870413));
#28998=CARTESIAN_POINT('Ctrl Pts',(369.396325883695,-13.5194718549485,3.8254017561411));
#28999=CARTESIAN_POINT('Ctrl Pts',(369.285690759097,-13.5253107097351,3.78007660283948));
#29000=CARTESIAN_POINT('Ctrl Pts',(369.175189290142,-13.5311425107412,3.73480620576969));
#29001=CARTESIAN_POINT('Ctrl Pts',(369.06653870332,-13.5369743117473,3.68463079724408));
#29002=CARTESIAN_POINT('Ctrl Pts',(368.960201023265,-13.5428061127534,3.62972603754946));
#29003=CARTESIAN_POINT('Ctrl Pts',(368.853964552685,-13.548632363201,3.57487353479583));
#29004=CARTESIAN_POINT('Ctrl Pts',(368.750036967426,-13.5544586136486,3.51530082231403));
#29005=CARTESIAN_POINT('Ctrl Pts',(368.648859903293,-13.5602848640961,3.45123145400047));
#29006=CARTESIAN_POINT('Ctrl Pts',(368.547258455213,-13.5661355525641,3.38689334877934));
#29007=CARTESIAN_POINT('Ctrl Pts',(368.448431036185,-13.5719862410321,3.31802093983099));
#29008=CARTESIAN_POINT('Ctrl Pts',(368.352799838286,-13.5778369295,3.24488726176098));
#29009=CARTESIAN_POINT('Ctrl Pts',(368.25766617898,-13.5836571787037,3.17213407486989));
#29010=CARTESIAN_POINT('Ctrl Pts',(368.1656958819,-13.5894774279074,3.0951641096098));
#29011=CARTESIAN_POINT('Ctrl Pts',(368.077274702612,-13.5952976771111,3.01428898177723));
#29012=CARTESIAN_POINT('Ctrl Pts',(367.988864553705,-13.6011172002493,2.93342394296956));
#29013=CARTESIAN_POINT('Ctrl Pts',(367.904002941103,-13.6069367233875,2.84865498445783));
#29014=CARTESIAN_POINT('Ctrl Pts',(367.823040870314,-13.6127562465257,2.76033257637481));
#29015=CARTESIAN_POINT('Ctrl Pts',(367.742070107115,-13.6185763944711,2.6720006856465));
#29016=CARTESIAN_POINT('Ctrl Pts',(367.664999992291,-13.6243965424165,2.58011488583731));
#29017=CARTESIAN_POINT('Ctrl Pts',(367.59214272374,-13.6302166903619,2.48506044790789));
#29018=CARTESIAN_POINT('Ctrl Pts',(367.518614774742,-13.636090415109,2.38913099566252));
#29019=CARTESIAN_POINT('Ctrl Pts',(367.449377892856,-13.6419641398561,2.28997459903167));
#29020=CARTESIAN_POINT('Ctrl Pts',(367.3847089292,-13.6478378646032,2.18801811493667));
#29021=CARTESIAN_POINT('Ctrl Pts',(367.320539496385,-13.6536662181784,2.08684918650043));
#29022=CARTESIAN_POINT('Ctrl Pts',(367.260867811579,-13.6594945717536,1.98292366137199));
#29023=CARTESIAN_POINT('Ctrl Pts',(367.205918170984,-13.6653229253289,1.87668344318415));
#29024=CARTESIAN_POINT('Ctrl Pts',(367.150326892175,-13.6712193356619,1.76920267486424));
#29025=CARTESIAN_POINT('Ctrl Pts',(367.099568817166,-13.6771157459949,1.65935320104759));
#29026=CARTESIAN_POINT('Ctrl Pts',(367.05382575592,-13.683012156328,1.54761251682033));
#29027=CARTESIAN_POINT('Ctrl Pts',(367.008082694673,-13.688908566661,1.43587183259306));
#29028=CARTESIAN_POINT('Ctrl Pts',(366.967354738134,-13.694804976994,1.32224035603285));
#29029=CARTESIAN_POINT('Ctrl Pts',(366.931771210358,-13.7007013873271,1.20720946825787));
#29030=CARTESIAN_POINT('Ctrl Pts',(366.889874249855,-13.7076439724576,1.07176914339708));
#29031=CARTESIAN_POINT('Ctrl Pts',(366.855006217274,-13.7145865575881,0.934062471553731));
#29032=CARTESIAN_POINT('Ctrl Pts',(366.827376047162,-13.7215291427186,0.794759311258914));
#29033=CARTESIAN_POINT('Ctrl Pts',(366.800005672858,-13.728406449405,0.65676596472998));
#29034=CARTESIAN_POINT('Ctrl Pts',(366.779737729344,-13.7352837560913,0.517206071648502));
#29035=CARTESIAN_POINT('Ctrl Pts',(366.766728357886,-13.7421610627776,0.376750179056597));
#29036=CARTESIAN_POINT('Ctrl Pts',(366.755237348061,-13.7482356989705,0.252687302766028));
#29037=CARTESIAN_POINT('Ctrl Pts',(366.749408851624,-13.7543103351634,0.127925664420039));
#29038=CARTESIAN_POINT('Ctrl Pts',(366.749318910897,-13.7603849713562,0.00293958966506929));
#29039=CARTESIAN_POINT('Origin',(370.834317853224,-8.23961502859548,0.));
#29040=CARTESIAN_POINT('',(373.320592904309,-11.7029891890582,-3.24124379989411));
#29041=CARTESIAN_POINT('',(373.320592904309,-11.8073874696441,-3.24124379989412));
#29042=CARTESIAN_POINT('',(373.320592904309,-8.23961502859548,-3.24124379989413));
#29043=CARTESIAN_POINT('',(366.749318160251,-11.2603849713631,0.00158379706420307));
#29044=CARTESIAN_POINT('Ctrl Pts',(366.749318160251,-11.2603849714045,0.00158379621223467));
#29045=CARTESIAN_POINT('Ctrl Pts',(366.749271660382,-11.2662079034056,-0.118350794889082));
#29046=CARTESIAN_POINT('Ctrl Pts',(366.754511367077,-11.2720308354067,-0.23832601982146));
#29047=CARTESIAN_POINT('Ctrl Pts',(366.765021606588,-11.2778537674077,-0.357845018286969));
#29048=CARTESIAN_POINT('Ctrl Pts',(366.775531340107,-11.283676419077,-0.477358262781803));
#29049=CARTESIAN_POINT('Ctrl Pts',(366.791311066522,-11.2894990707462,-0.59641492158895));
#29050=CARTESIAN_POINT('Ctrl Pts',(366.812293155352,-11.2953217224155,-0.714522448705577));
#29051=CARTESIAN_POINT('Ctrl Pts',(366.833279063491,-11.3011454339655,-0.832651474600536));
#29052=CARTESIAN_POINT('Ctrl Pts',(366.859469147176,-11.3069691455155,-0.949830626889041));
#29053=CARTESIAN_POINT('Ctrl Pts',(366.890744608621,-11.3127928570656,-1.06557733855915));
#29054=CARTESIAN_POINT('Ctrl Pts',(366.923424012687,-11.3188779926354,-1.18651987258203));
#29055=CARTESIAN_POINT('Ctrl Pts',(366.961655862029,-11.3249631282053,-1.3058978956442));
#29056=CARTESIAN_POINT('Ctrl Pts',(367.005246895972,-11.3310482637751,-1.4231797512366));
#29057=CARTESIAN_POINT('Ctrl Pts',(367.047033600812,-11.3368815221535,-1.53560705197797));
#29058=CARTESIAN_POINT('Ctrl Pts',(367.093744473723,-11.3427147805319,-1.64610789774426));
#29059=CARTESIAN_POINT('Ctrl Pts',(367.145160824468,-11.3485480389102,-1.75423641997932));
#29060=CARTESIAN_POINT('Ctrl Pts',(367.19661482878,-11.3543855691395,-1.86244412761821));
#29061=CARTESIAN_POINT('Ctrl Pts',(367.252780985196,-11.3602230993687,-1.96827569535019));
#29062=CARTESIAN_POINT('Ctrl Pts',(367.313395671236,-11.3660606295979,-2.07131165892109));
#29063=CARTESIAN_POINT('Ctrl Pts',(367.374098204497,-11.3719066200014,-2.1744969497207));
#29064=CARTESIAN_POINT('Ctrl Pts',(367.439261914381,-11.377752610405,-2.2748782131449));
#29065=CARTESIAN_POINT('Ctrl Pts',(367.508581043213,-11.3835986008085,-2.37206654007454));
#29066=CARTESIAN_POINT('Ctrl Pts',(367.517339358752,-11.384337228507,-2.38434606591743));
#29067=CARTESIAN_POINT('Ctrl Pts',(367.526163959873,-11.3850758562054,-2.39657466641323));
#29068=CARTESIAN_POINT('Ctrl Pts',(367.535054186773,-11.3858144839039,-2.40875159766206));
#29069=CARTESIAN_POINT('Ctrl Pts',(367.605317058358,-11.3916521417843,-2.50499055378519));
#29070=CARTESIAN_POINT('Ctrl Pts',(367.679902869804,-11.3974897996647,-2.59830131414769));
#29071=CARTESIAN_POINT('Ctrl Pts',(367.758539379142,-11.403327457545,-2.68827301038714));
#29072=CARTESIAN_POINT('Ctrl Pts',(367.837078657014,-11.4091578973528,-2.77813345957347));
#29073=CARTESIAN_POINT('Ctrl Pts',(367.919658404463,-11.4149883371606,-2.86466275422529));
#29074=CARTESIAN_POINT('Ctrl Pts',(368.005964041971,-11.4208187769684,-2.94748023205755));
#29075=CARTESIAN_POINT('Ctrl Pts',(368.092185149825,-11.4266435063142,-3.03021659661654));
#29076=CARTESIAN_POINT('Ctrl Pts',(368.182124595608,-11.43246823566,-3.10924809789295));
#29077=CARTESIAN_POINT('Ctrl Pts',(368.275428991747,-11.4382929650058,-3.18422875977987));
#29078=CARTESIAN_POINT('Ctrl Pts',(368.369157386334,-11.4441441633745,-3.25955015249597));
#29079=CARTESIAN_POINT('Ctrl Pts',(368.46628111593,-11.4499953617433,-3.33078348678459));
#29080=CARTESIAN_POINT('Ctrl Pts',(368.566405734061,-11.4558465601121,-3.39761675586779));
#29081=CARTESIAN_POINT('Ctrl Pts',(368.665968312269,-11.461664913341,-3.46407486281691));
#29082=CARTESIAN_POINT('Ctrl Pts',(368.76849782855,-11.4674832665699,-3.52618195619947));
#29083=CARTESIAN_POINT('Ctrl Pts',(368.873575460687,-11.4733016197989,-3.58367329288085));
#29084=CARTESIAN_POINT('Ctrl Pts',(368.978637520203,-11.4791191107415,-3.64115610928314));
#29085=CARTESIAN_POINT('Ctrl Pts',(369.086246588171,-11.4849366016841,-3.69402433492965));
#29086=CARTESIAN_POINT('Ctrl Pts',(369.195958220374,-11.4907540926267,-3.74205861972375));
#29087=CARTESIAN_POINT('Ctrl Pts',(369.30567913085,-11.4965720755524,-3.79009696675955));
#29088=CARTESIAN_POINT('Ctrl Pts',(369.417502586998,-11.5023900584781,-3.83330039746001));
#29089=CARTESIAN_POINT('Ctrl Pts',(369.530963669884,-11.5082080414038,-3.87149749745121));
#29090=CARTESIAN_POINT('Ctrl Pts',(369.645558927073,-11.5140841817748,-3.91007642148396));
#29091=CARTESIAN_POINT('Ctrl Pts',(369.761824334618,-11.5199603221458,-3.94354822893277));
#29092=CARTESIAN_POINT('Ctrl Pts',(369.879265776766,-11.5258364625168,-3.9717880773341));
#29093=CARTESIAN_POINT('Ctrl Pts',(369.99570284113,-11.5316623492061,-3.99978641408623));
#29094=CARTESIAN_POINT('Ctrl Pts',(370.113295489678,-11.5374882358954,-4.02264191374151));
#29095=CARTESIAN_POINT('Ctrl Pts',(370.231553464511,-11.5433141225848,-4.04028465478602));
#29096=CARTESIAN_POINT('Ctrl Pts',(370.351341566586,-11.5492153897966,-4.05815567336308));
#29097=CARTESIAN_POINT('Ctrl Pts',(370.471811904407,-11.5551166570084,-4.07067804364192));
#29098=CARTESIAN_POINT('Ctrl Pts',(370.592452268245,-11.5610179242203,-4.0778334981706));
#29099=CARTESIAN_POINT('Ctrl Pts',(370.713092632082,-11.5669191914321,-4.08498895269929));
#29100=CARTESIAN_POINT('Ctrl Pts',(370.833902593644,-11.572820458644,-4.08677753983674));
#29101=CARTESIAN_POINT('Ctrl Pts',(370.954373694032,-11.5787217258558,-4.08323543223847));
#29102=CARTESIAN_POINT('Ctrl Pts',(371.073698652196,-11.5845668493826,-4.07972702366896));
#29103=CARTESIAN_POINT('Ctrl Pts',(371.193044864443,-11.5904119729093,-4.07097858147516));
#29104=CARTESIAN_POINT('Ctrl Pts',(371.311918092408,-11.5962570964361,-4.05698447267567));
#29105=CARTESIAN_POINT('Ctrl Pts',(371.430658839178,-11.6020957057211,-4.04300595995514));
#29106=CARTESIAN_POINT('Ctrl Pts',(371.548927251579,-11.6079343150061,-4.02379345434519));
#29107=CARTESIAN_POINT('Ctrl Pts',(371.666230227338,-11.613772924291,-3.99939330421453));
#29108=CARTESIAN_POINT('Ctrl Pts',(371.783429498612,-11.6196063718147,-3.97501472561675));
#29109=CARTESIAN_POINT('Ctrl Pts',(371.899664637159,-11.6254398193383,-3.94545770783133));
#29110=CARTESIAN_POINT('Ctrl Pts',(372.014449378726,-11.6312732668619,-3.91082019306902));
#29111=CARTESIAN_POINT('Ctrl Pts',(372.132045556661,-11.6372495937116,-3.87533429752578));
#29112=CARTESIAN_POINT('Ctrl Pts',(372.248118935508,-11.6432259205613,-3.83451584958903));
#29113=CARTESIAN_POINT('Ctrl Pts',(372.362159242034,-11.649202247411,-3.78852552989119));
#29114=CARTESIAN_POINT('Ctrl Pts',(372.473359808257,-11.6550297565598,-3.74368042427057));
#29115=CARTESIAN_POINT('Ctrl Pts',(372.582626971052,-11.6608572657087,-3.69391815786364));
#29116=CARTESIAN_POINT('Ctrl Pts',(372.689505290836,-11.6666847748575,-3.63943739763784));
#29117=CARTESIAN_POINT('Ctrl Pts',(372.800477654598,-11.6727355105577,-3.58286971624134));
#29118=CARTESIAN_POINT('Ctrl Pts',(372.908874080937,-11.6787862462578,-3.52121500301371));
#29119=CARTESIAN_POINT('Ctrl Pts',(373.014211161153,-11.6848369819579,-3.45474892952387));
#29120=CARTESIAN_POINT('Ctrl Pts',(373.119548241369,-11.690887717658,-3.38828285603403));
#29121=CARTESIAN_POINT('Ctrl Pts',(373.221825568593,-11.6969384533581,-3.3170056918752));
#29122=CARTESIAN_POINT('Ctrl Pts',(373.320592904309,-11.7029891890582,-3.2412437998941));
#29123=CARTESIAN_POINT('',(369.776413430251,-11.,3.94563850749837));
#29124=CARTESIAN_POINT('Ctrl Pts',(369.776413430251,-11.,3.94563850749839));
#29125=CARTESIAN_POINT('Ctrl Pts',(369.658555082909,-11.0059425548389,3.91403833259629));
#29126=CARTESIAN_POINT('Ctrl Pts',(369.54203182805,-11.0118851096777,3.87713126827553));
#29127=CARTESIAN_POINT('Ctrl Pts',(369.427338766957,-11.0178276645166,3.83505343519563));
#29128=CARTESIAN_POINT('Ctrl Pts',(369.312716174018,-11.0237665682116,3.79300145500712));
#29129=CARTESIAN_POINT('Ctrl Pts',(369.199921894619,-11.0297054719065,3.74578516541319));
#29130=CARTESIAN_POINT('Ctrl Pts',(369.089435035688,-11.0356443756014,3.69359025245994));
#29131=CARTESIAN_POINT('Ctrl Pts',(368.978992730761,-11.0415808844239,3.64141638718932));
#29132=CARTESIAN_POINT('Ctrl Pts',(368.870856339153,-11.0475173932464,3.58426806167526));
#29133=CARTESIAN_POINT('Ctrl Pts',(368.765483899815,-11.0534539020689,3.5223786101474));
#29134=CARTESIAN_POINT('Ctrl Pts',(368.660107526221,-11.0593906325409,3.46048684787291));
#29135=CARTESIAN_POINT('Ctrl Pts',(368.557495646737,-11.0653273630128,3.39385379192271));
#29136=CARTESIAN_POINT('Ctrl Pts',(368.458080684342,-11.0712640934848,3.32275817916765));
#29137=CARTESIAN_POINT('Ctrl Pts',(368.358660266531,-11.0772011497362,3.2516586650261));
#29138=CARTESIAN_POINT('Ctrl Pts',(368.262437427882,-11.0831382059875,3.17609632917323));
#29139=CARTESIAN_POINT('Ctrl Pts',(368.169814137957,-11.0890752622388,3.09639224765349));
#29140=CARTESIAN_POINT('Ctrl Pts',(368.077167996229,-11.0950137832669,3.01666850172726));
#29141=CARTESIAN_POINT('Ctrl Pts',(367.988123463082,-11.100952304295,2.9328012252537));
#29142=CARTESIAN_POINT('Ctrl Pts',(367.90304779981,-11.1068908253231,2.84515041324005));
#29143=CARTESIAN_POINT('Ctrl Pts',(367.817934820676,-11.1128319511035,2.75746115585251));
#29144=CARTESIAN_POINT('Ctrl Pts',(367.736794445859,-11.118773076884,2.6659853329638));
#29145=CARTESIAN_POINT('Ctrl Pts',(367.659955363951,-11.1247142026645,2.57111800326221));
#29146=CARTESIAN_POINT('Ctrl Pts',(367.583016261277,-11.1306630619568,2.47612718558003));
#29147=CARTESIAN_POINT('Ctrl Pts',(367.510389879206,-11.1366119212492,2.37773634013093));
#29148=CARTESIAN_POINT('Ctrl Pts',(367.442363466651,-11.1425607805416,2.27637221020805));
#29149=CARTESIAN_POINT('Ctrl Pts',(367.374291336794,-11.1485136377782,2.17493995829567));
#29150=CARTESIAN_POINT('Ctrl Pts',(367.310825540233,-11.1544664950147,2.07053076535526));
#29151=CARTESIAN_POINT('Ctrl Pts',(367.252208140915,-11.1604193522512,1.96359746612641));
#29152=CARTESIAN_POINT('Ctrl Pts',(367.193491815945,-11.166382255827,1.85648370092013));
#29153=CARTESIAN_POINT('Ctrl Pts',(367.139640412308,-11.1723451594028,1.74683766006762));
#29154=CARTESIAN_POINT('Ctrl Pts',(367.090848866821,-11.1783080629785,1.63513453508797));
#29155=CARTESIAN_POINT('Ctrl Pts',(367.051029535186,-11.1831744559697,1.54397235250682));
#29156=CARTESIAN_POINT('Ctrl Pts',(367.014579378245,-11.1880408489608,1.45144053637299));
#29157=CARTESIAN_POINT('Ctrl Pts',(366.981579687489,-11.1929072419519,1.35780470844867));
#29158=CARTESIAN_POINT('Ctrl Pts',(366.93694994957,-11.1994886928329,1.23116890174215));
#29159=CARTESIAN_POINT('Ctrl Pts',(366.898524370235,-11.2060701437139,1.10220791307046));
#29160=CARTESIAN_POINT('Ctrl Pts',(366.86652191129,-11.2126515945948,0.971504175580758));
#29161=CARTESIAN_POINT('Ctrl Pts',(366.834629314539,-11.2192104518171,0.84124913484363));
#29162=CARTESIAN_POINT('Ctrl Pts',(366.809115930347,-11.2257693090393,0.709263473234092));
#29163=CARTESIAN_POINT('Ctrl Pts',(366.79015143706,-11.2323281662616,0.576144945624114));
#29164=CARTESIAN_POINT('Ctrl Pts',(366.771298075538,-11.2388485886377,0.44380649142543));
#29165=CARTESIAN_POINT('Ctrl Pts',(366.758917173706,-11.2453690110138,0.310348606542818));
#29166=CARTESIAN_POINT('Ctrl Pts',(366.753127314955,-11.2518894333899,0.176376841858498));
#29167=CARTESIAN_POINT('Ctrl Pts',(366.750612755721,-11.254721279381,0.118192358882813));
#29168=CARTESIAN_POINT('Ctrl Pts',(366.749340774381,-11.2575531253721,0.0599111639190462));
#29169=CARTESIAN_POINT('Ctrl Pts',(366.749318160251,-11.2603849713631,0.00158379706420297));
#29170=CARTESIAN_POINT('',(371.893335409592,-11.,3.94533988590394));
#29171=CARTESIAN_POINT('Origin',(370.834317853224,-11.,0.));
#29172=CARTESIAN_POINT('',(366.749317884331,-11.3646150285611,-0.000504124207611034));
#29173=CARTESIAN_POINT('Ctrl Pts',(371.893335409592,-11.,3.94533988590394));
#29174=CARTESIAN_POINT('Ctrl Pts',(371.779439084971,-11.0057722725029,3.9759122094216));
#29175=CARTESIAN_POINT('Ctrl Pts',(371.664032071455,-11.0115445450058,4.00159818186356));
#29176=CARTESIAN_POINT('Ctrl Pts',(371.547575100626,-11.0173168175087,4.02224925868946));
#29177=CARTESIAN_POINT('Ctrl Pts',(371.431254230685,-11.0230823440745,4.04287620102291));
#29178=CARTESIAN_POINT('Ctrl Pts',(371.313886249872,-11.0288478706402,4.05847987589247));
#29179=CARTESIAN_POINT('Ctrl Pts',(371.195946097017,-11.0346133972059,4.06896178567588));
#29180=CARTESIAN_POINT('Ctrl Pts',(371.074312838115,-11.0405594619557,4.07977191959225));
#29181=CARTESIAN_POINT('Ctrl Pts',(370.952071411611,-11.0465055267056,4.08513411645457));
#29182=CARTESIAN_POINT('Ctrl Pts',(370.829753664507,-11.0524515914554,4.08499745020497));
#29183=CARTESIAN_POINT('Ctrl Pts',(370.711326098722,-11.0582085481604,4.08486513047502));
#29184=CARTESIAN_POINT('Ctrl Pts',(370.592827443816,-11.0639655048653,4.07957840674844));
#29185=CARTESIAN_POINT('Ctrl Pts',(370.474743937419,-11.0697224615703,4.06914384103981));
#29186=CARTESIAN_POINT('Ctrl Pts',(370.356692365384,-11.0754778613708,4.05871209724262));
#29187=CARTESIAN_POINT('Ctrl Pts',(370.239056132905,-11.0812332611713,4.04313531578104));
#29188=CARTESIAN_POINT('Ctrl Pts',(370.122318273177,-11.0869886609718,4.02247207547947));
#29189=CARTESIAN_POINT('Ctrl Pts',(370.005583211736,-11.0927439228114,4.00180933049004));
#29190=CARTESIAN_POINT('Ctrl Pts',(369.889746889886,-11.098499184651,3.97606044244825));
#29191=CARTESIAN_POINT('Ctrl Pts',(369.775283298204,-11.1042544464906,3.94533532304586));
#29192=CARTESIAN_POINT('Ctrl Pts',(369.660794237774,-11.1100109889061,3.91460336714373));
#29193=CARTESIAN_POINT('Ctrl Pts',(369.547678916266,-11.1157675313215,3.87889308758316));
#29194=CARTESIAN_POINT('Ctrl Pts',(369.436396562165,-11.121524073737,3.83836437353257));
#29195=CARTESIAN_POINT('Ctrl Pts',(369.32500564356,-11.1272862321027,3.79779612060125));
#29196=CARTESIAN_POINT('Ctrl Pts',(369.215451652393,-11.1330483904685,3.75240019435146));
#29197=CARTESIAN_POINT('Ctrl Pts',(369.108174193521,-11.1388105488342,3.70238478093063));
#29198=CARTESIAN_POINT('Ctrl Pts',(369.000833722416,-11.1445760917551,3.65233998964304));
#29199=CARTESIAN_POINT('Ctrl Pts',(368.895772814035,-11.1503416346759,3.59767050111718));
#29200=CARTESIAN_POINT('Ctrl Pts',(368.793405326633,-11.1561071775967,3.53862982788566));
#29201=CARTESIAN_POINT('Ctrl Pts',(368.690901453063,-11.1618804020609,3.4795104936326));
#29202=CARTESIAN_POINT('Ctrl Pts',(368.591098510422,-11.1676536265252,3.41600857687091));
#29203=CARTESIAN_POINT('Ctrl Pts',(368.494380284798,-11.1734268509894,3.34842010146105));
#29204=CARTESIAN_POINT('Ctrl Pts',(368.472645635539,-11.1747242177269,3.33323152870201));
#29205=CARTESIAN_POINT('Ctrl Pts',(368.451066625825,-11.1760215844643,3.31783674250088));
#29206=CARTESIAN_POINT('Ctrl Pts',(368.429647365639,-11.1773189512017,3.30223936838908));
#29207=CARTESIAN_POINT('Ctrl Pts',(368.33357121294,-11.1831382934053,3.23227730229304));
#29208=CARTESIAN_POINT('Ctrl Pts',(368.240402810823,-11.1889576356089,3.15801106487821));
#29209=CARTESIAN_POINT('Ctrl Pts',(368.150551312676,-11.1947769778125,3.07971137541123));
#29210=CARTESIAN_POINT('Ctrl Pts',(368.060807061285,-11.2005893740488,3.00150514445892));
#29211=CARTESIAN_POINT('Ctrl Pts',(367.974372144894,-11.2064017702852,2.91927530397612));
#29212=CARTESIAN_POINT('Ctrl Pts',(367.891625510157,-11.2122141665215,2.83333492091153));
#29213=CARTESIAN_POINT('Ctrl Pts',(367.808956003466,-11.2180211450299,2.74747464278148));
#29214=CARTESIAN_POINT('Ctrl Pts',(367.729968221061,-11.2238281235382,2.65791099598431));
#29215=CARTESIAN_POINT('Ctrl Pts',(367.655006396492,-11.2296351020466,2.56499584036495));
#29216=CARTESIAN_POINT('Ctrl Pts',(367.580092479708,-11.2354383693394,2.47214006642955));
#29217=CARTESIAN_POINT('Ctrl Pts',(367.509199657806,-11.2412416366323,2.37593736242979));
#29218=CARTESIAN_POINT('Ctrl Pts',(367.442633400948,-11.2470449039252,2.27677437972832));
#29219=CARTESIAN_POINT('Ctrl Pts',(367.376089151854,-11.2528462525742,2.17764418173846));
#29220=CARTESIAN_POINT('Ctrl Pts',(367.313868851014,-11.2586476012233,2.07555599032896));
#29221=CARTESIAN_POINT('Ctrl Pts',(367.256235632751,-11.2644489498723,1.97092684378053));
#29222=CARTESIAN_POINT('Ctrl Pts',(367.198607821631,-11.2702497542395,1.86630751352781));
#29223=CARTESIAN_POINT('Ctrl Pts',(367.145566434097,-11.2760505586066,1.75914806051596));
#29224=CARTESIAN_POINT('Ctrl Pts',(367.097329153327,-11.2818513629737,1.64989104393092));
#29225=CARTESIAN_POINT('Ctrl Pts',(367.049084975963,-11.2876529966951,1.54061840662022));
#29226=CARTESIAN_POINT('Ctrl Pts',(367.005646435884,-11.2934546304165,1.42924798358644));
#29227=CARTESIAN_POINT('Ctrl Pts',(366.967183223484,-11.2992562641379,1.31624266587345));
#29228=CARTESIAN_POINT('Ctrl Pts',(366.928683436374,-11.305063414639,1.2031298912836));
#29229=CARTESIAN_POINT('Ctrl Pts',(366.895168557871,-11.31087056514,1.08837950474184));
#29230=CARTESIAN_POINT('Ctrl Pts',(366.866758541716,-11.3166777156411,0.972470107339642));
#29231=CARTESIAN_POINT('Ctrl Pts',(366.838334371929,-11.322487759216,0.856502964844621));
#29232=CARTESIAN_POINT('Ctrl Pts',(366.815020211601,-11.3282978027909,0.739376061951449));
#29233=CARTESIAN_POINT('Ctrl Pts',(366.796884646067,-11.3341078463658,0.621577105232758));
#29234=CARTESIAN_POINT('Ctrl Pts',(366.778722266324,-11.3399264803387,0.50360397771694));
#29235=CARTESIAN_POINT('Ctrl Pts',(366.765753822078,-11.3457451143116,0.384957217836436));
#29236=CARTESIAN_POINT('Ctrl Pts',(366.757995936781,-11.3515637482845,0.266128979116804));
#29237=CARTESIAN_POINT('Ctrl Pts',(366.752195587086,-11.3559141750434,0.177284492275928));
#29238=CARTESIAN_POINT('Ctrl Pts',(366.749306920368,-11.3602646018023,0.0883386385946549));
#29239=CARTESIAN_POINT('Ctrl Pts',(366.749317884331,-11.3646150285611,-0.000504124207612033));
#29240=CARTESIAN_POINT('Ctrl Pts',(366.749317884331,-11.3646150285955,-0.000504124909455006));
#29241=CARTESIAN_POINT('Ctrl Pts',(366.749322598097,-11.3664854167815,-0.0387004819959074));
#29242=CARTESIAN_POINT('Ctrl Pts',(366.749863028343,-11.3683558049676,-0.0768922472437367));
#29243=CARTESIAN_POINT('Ctrl Pts',(366.750938849501,-11.3702261931536,-0.115069161598965));
#29244=CARTESIAN_POINT('Ctrl Pts',(366.75429518582,-11.3760614119119,-0.234173125385912));
#29245=CARTESIAN_POINT('Ctrl Pts',(366.762871991954,-11.3818966306702,-0.353312031471976));
#29246=CARTESIAN_POINT('Ctrl Pts',(366.776677225411,-11.3877318494285,-0.471993151986081));
#29247=CARTESIAN_POINT('Ctrl Pts',(366.790465659685,-11.3935599674804,-0.590529852928814));
#29248=CARTESIAN_POINT('Ctrl Pts',(366.809469818492,-11.3993880855323,-0.708609476083606));
#29249=CARTESIAN_POINT('Ctrl Pts',(366.833645657319,-11.4052162035842,-0.825740262378583));
#29250=CARTESIAN_POINT('Ctrl Pts',(366.857798298364,-11.4110387293002,-0.942758656527254));
#29251=CARTESIAN_POINT('Ctrl Pts',(366.88711266417,-11.4168612550162,-1.05882962943746));
#29252=CARTESIAN_POINT('Ctrl Pts',(366.921493086368,-11.4226837807323,-1.17346808387846));
#29253=CARTESIAN_POINT('Ctrl Pts',(366.95604795318,-11.4285358496645,-1.28868820833842));
#29254=CARTESIAN_POINT('Ctrl Pts',(366.995720380752,-11.4343879185967,-1.40246082410072));
#29255=CARTESIAN_POINT('Ctrl Pts',(367.040361389904,-11.440239987529,-1.51430490801364));
#29256=CARTESIAN_POINT('Ctrl Pts',(367.08473066592,-11.4460564344832,-1.62546818868625));
#29257=CARTESIAN_POINT('Ctrl Pts',(367.13400804007,-11.4518728814375,-1.73472597299548));
#29258=CARTESIAN_POINT('Ctrl Pts',(367.187997909219,-11.4576893283918,-1.84162316067947));
#29259=CARTESIAN_POINT('Ctrl Pts',(367.241980833302,-11.4635050271389,-1.94850659748858));
#29260=CARTESIAN_POINT('Ctrl Pts',(367.300674863371,-11.4693207258861,-2.05302967914904));
#29261=CARTESIAN_POINT('Ctrl Pts',(367.363837598286,-11.4751364246333,-2.15476026510718));
#29262=CARTESIAN_POINT('Ctrl Pts',(367.427006927125,-11.480952730515,-2.25650147131213));
#29263=CARTESIAN_POINT('Ctrl Pts',(367.494645674013,-11.4867690363968,-2.35544925703979));
#29264=CARTESIAN_POINT('Ctrl Pts',(367.566467450474,-11.4925853422785,-2.45119945032005));
#29265=CARTESIAN_POINT('Ctrl Pts',(367.639063491327,-11.4984643500141,-2.54798186486703));
#29266=CARTESIAN_POINT('Ctrl Pts',(367.715933039427,-11.5043433577497,-2.64149699004699));
#29267=CARTESIAN_POINT('Ctrl Pts',(367.796738524552,-11.5102223654853,-2.73136171570656));
#29268=CARTESIAN_POINT('Ctrl Pts',(367.87679485592,-11.516046868496,-2.82039329870493));
#29269=CARTESIAN_POINT('Ctrl Pts',(367.960714120322,-11.5218713715067,-2.90584163408582));
#29270=CARTESIAN_POINT('Ctrl Pts',(368.048131624811,-11.5276958745174,-2.98737197225236));
#29271=CARTESIAN_POINT('Ctrl Pts',(368.136776186875,-11.5336021346154,-3.07004673131913));
#29272=CARTESIAN_POINT('Ctrl Pts',(368.229017613753,-11.5395083947134,-3.14869238285008));
#29273=CARTESIAN_POINT('Ctrl Pts',(368.324442591822,-11.5454146548115,-3.22300343968169));
#29274=CARTESIAN_POINT('Ctrl Pts',(368.41986756989,-11.5513209149095,-3.2973144965133));
#29275=CARTESIAN_POINT('Ctrl Pts',(368.518475715946,-11.5572271750076,-3.36729075595378));
#29276=CARTESIAN_POINT('Ctrl Pts',(368.619825966729,-11.5631334351056,-3.43267398461454));
#29277=CARTESIAN_POINT('Ctrl Pts',(368.720023213455,-11.5689725030476,-3.4973133855354));
#29278=CARTESIAN_POINT('Ctrl Pts',(368.823204048632,-11.5748115709897,-3.55765960597024));
#29279=CARTESIAN_POINT('Ctrl Pts',(368.928965788806,-11.5806506389317,-3.61342752945438));
#29280=CARTESIAN_POINT('Ctrl Pts',(369.03459971804,-11.5864826504773,-3.66912805852182));
#29281=CARTESIAN_POINT('Ctrl Pts',(369.14280799164,-11.5923146620229,-3.7202611093649));
#29282=CARTESIAN_POINT('Ctrl Pts',(369.253159372267,-11.5981466735684,-3.76658503927602));
#29283=CARTESIAN_POINT('Ctrl Pts',(369.363405671341,-11.60397313161,-3.81286485745531));
#29284=CARTESIAN_POINT('Ctrl Pts',(369.475790644761,-11.6097995896516,-3.85434451033228));
#29285=CARTESIAN_POINT('Ctrl Pts',(369.589859406784,-11.6156260476932,-3.89082872600213));
#29286=CARTESIAN_POINT('Ctrl Pts',(369.704401000401,-11.6214766572501,-3.92746417404763));
#29287=CARTESIAN_POINT('Ctrl Pts',(369.82064000553,-11.6273272668069,-3.95906248855058));
#29288=CARTESIAN_POINT('Ctrl Pts',(369.938096133759,-11.6331778763638,-3.98547508203966));
#29289=CARTESIAN_POINT('Ctrl Pts',(370.054946738593,-11.6389983241827,-4.01175151027708));
#29290=CARTESIAN_POINT('Ctrl Pts',(370.173001545222,-11.6448187720016,-4.03289547844079));
#29291=CARTESIAN_POINT('Ctrl Pts',(370.291773986964,-11.6506392198205,-4.04881107896914));
#29292=CARTESIAN_POINT('Ctrl Pts',(370.410531534084,-11.656458937728,-4.06472468360656));
#29293=CARTESIAN_POINT('Ctrl Pts',(370.53000613533,-11.6622786556355,-4.07541117107995));
#29294=CARTESIAN_POINT('Ctrl Pts',(370.649703722092,-11.668098373543,-4.08082621813109));
#29295=CARTESIAN_POINT('Ctrl Pts',(370.769414074254,-11.6739187121065,-4.08624184268128));
#29296=CARTESIAN_POINT('Ctrl Pts',(370.889347053994,-11.67973905067,-4.08638489069963));
#29297=CARTESIAN_POINT('Ctrl Pts',(371.00900680281,-11.6855593892335,-4.08126313423826));
#29298=CARTESIAN_POINT('Ctrl Pts',(371.129758272065,-11.6914328298855,-4.07609464922975));
#29299=CARTESIAN_POINT('Ctrl Pts',(371.250231078803,-11.6973062705375,-4.06556481543231));
#29300=CARTESIAN_POINT('Ctrl Pts',(371.369920269737,-11.7031797111895,-4.04973518287613));
#29301=CARTESIAN_POINT('Ctrl Pts',(371.488694308412,-11.709008243087,-4.03402658484183));
#29302=CARTESIAN_POINT('Ctrl Pts',(371.606696280947,-11.7148367749846,-4.01309908232749));
#29303=CARTESIAN_POINT('Ctrl Pts',(371.723443294561,-11.7206653068822,-3.98706420183666));
#29304=CARTESIAN_POINT('Ctrl Pts',(371.841539609265,-11.7265612019114,-3.96072842377636));
#29305=CARTESIAN_POINT('Ctrl Pts',(371.958351360577,-11.7324570969406,-3.92916657745507));
#29306=CARTESIAN_POINT('Ctrl Pts',(372.073395784961,-11.7383529919699,-3.89254555260209));
#29307=CARTESIAN_POINT('Ctrl Pts',(372.188440209345,-11.7442488869991,-3.85592452774911));
#29308=CARTESIAN_POINT('Ctrl Pts',(372.30171692802,-11.7501447820283,-3.81424452269664));
#29309=CARTESIAN_POINT('Ctrl Pts',(372.4127661906,-11.7560406770575,-3.76772157228141));
#29310=CARTESIAN_POINT('Ctrl Pts',(372.522748452178,-11.7618799222202,-3.72164563100016));
#29311=CARTESIAN_POINT('Ctrl Pts',(372.630876980634,-11.7677191673829,-3.67068073444835));
#29312=CARTESIAN_POINT('Ctrl Pts',(372.736688921398,-11.7735584125456,-3.61499783111619));
#29313=CARTESIAN_POINT('Ctrl Pts',(372.842360004958,-11.7793898844859,-3.55938905304787));
#29314=CARTESIAN_POINT('Ctrl Pts',(372.945720282467,-11.7852213564263,-3.49907495555428));
#29315=CARTESIAN_POINT('Ctrl Pts',(373.046326778446,-11.7910528283666,-3.43427452524351));
#29316=CARTESIAN_POINT('Ctrl Pts',(373.140263668869,-11.7964977087924,-3.37376997370112));
#29317=CARTESIAN_POINT('Ctrl Pts',(373.231799722461,-11.8019425892183,-3.30935477406498));
#29318=CARTESIAN_POINT('Ctrl Pts',(373.320592904309,-11.8073874696441,-3.2412437998941));
#29319=CARTESIAN_POINT('Origin',(370.834317853224,-11.,0.));
#29320=CARTESIAN_POINT('',(372.012622422822,-15.1306250182556,3.17836489468462));
#29321=CARTESIAN_POINT('',(372.012622422842,-15.4759533536068,3.17836489467751));
#29322=CARTESIAN_POINT('',(372.012622422842,-11.,3.17836489467752));
#29323=CARTESIAN_POINT('',(367.444571657931,-15.8589799862073,0.00507877902897487));
#29324=CARTESIAN_POINT('Ctrl Pts',(372.012622422842,-15.4759533536068,3.17836489467751));
#29325=CARTESIAN_POINT('Ctrl Pts',(371.915085677486,-15.4820510309549,3.21452436552715));
#29326=CARTESIAN_POINT('Ctrl Pts',(371.815818975043,-15.4881487083029,3.24621370971365));
#29327=CARTESIAN_POINT('Ctrl Pts',(371.715267978533,-15.494246385651,3.27327541450729));
#29328=CARTESIAN_POINT('Ctrl Pts',(371.614748749664,-15.5003421365256,3.30032856954439));
#29329=CARTESIAN_POINT('Ctrl Pts',(371.512946443811,-15.5064378874003,3.32275688102416));
#29330=CARTESIAN_POINT('Ctrl Pts',(371.410321653924,-15.5125336382749,3.34045276632958));
#29331=CARTESIAN_POINT('Ctrl Pts',(371.307703062513,-15.5186290209697,3.358147582814));
#29332=CARTESIAN_POINT('Ctrl Pts',(371.204262505207,-15.5247244036646,3.37111046963088));
#29333=CARTESIAN_POINT('Ctrl Pts',(371.100469655214,-15.5308197863594,3.37928517305025));
#29334=CARTESIAN_POINT('Ctrl Pts',(370.996656552083,-15.5369163584487,3.38746147160269));
#29335=CARTESIAN_POINT('Ctrl Pts',(370.892491443781,-15.543012930538,3.39084769666992));
#29336=CARTESIAN_POINT('Ctrl Pts',(370.788447109625,-15.5491095026272,3.389439619964));
#29337=CARTESIAN_POINT('Ctrl Pts',(370.684294576641,-15.5552124147249,3.38803007895681));
#29338=CARTESIAN_POINT('Ctrl Pts',(370.580263494632,-15.5613153268226,3.38181628746154));
#29339=CARTESIAN_POINT('Ctrl Pts',(370.476824564169,-15.5674182389203,3.3708461268323));
#29340=CARTESIAN_POINT('Ctrl Pts',(370.373326239876,-15.5735246552626,3.35986966722219));
#29341=CARTESIAN_POINT('Ctrl Pts',(370.270421164752,-15.5796310716049,3.34413146283107));
#29342=CARTESIAN_POINT('Ctrl Pts',(370.168570958071,-15.5857374879472,3.32373075535515));
#29343=CARTESIAN_POINT('Ctrl Pts',(370.066565210115,-15.5918532297472,3.30329889279225));
#29344=CARTESIAN_POINT('Ctrl Pts',(369.965617960256,-15.5979689715471,3.2781904104684));
#29345=CARTESIAN_POINT('Ctrl Pts',(369.866176836464,-15.604084713347,3.24855476083871));
#29346=CARTESIAN_POINT('Ctrl Pts',(369.811430946844,-15.6074516475967,3.23223927744915));
#29347=CARTESIAN_POINT('Ctrl Pts',(369.757141228761,-15.6108185818464,3.21455252186698));
#29348=CARTESIAN_POINT('Ctrl Pts',(369.703379629996,-15.6141855160962,3.19552559021866));
#29349=CARTESIAN_POINT('Ctrl Pts',(369.606165004131,-15.6202737884117,3.16112006501042));
#29350=CARTESIAN_POINT('Ctrl Pts',(369.51035770414,-15.6263620607272,3.12221617440523));
#29351=CARTESIAN_POINT('Ctrl Pts',(369.416404507066,-15.6324503330427,3.07894897737639));
#29352=CARTESIAN_POINT('Ctrl Pts',(369.322571621384,-15.6385308090454,3.03573718598441));
#29353=CARTESIAN_POINT('Ctrl Pts',(369.2305885063,-15.644611285048,2.98817337365492));
#29354=CARTESIAN_POINT('Ctrl Pts',(369.140885049192,-15.6506917610507,2.93644179249781));
#29355=CARTESIAN_POINT('Ctrl Pts',(369.051270458902,-15.6567662132882,2.88476146043614));
#29356=CARTESIAN_POINT('Ctrl Pts',(368.963931406737,-15.6628406655257,2.82892178304921));
#29357=CARTESIAN_POINT('Ctrl Pts',(368.879275289204,-15.6689151177632,2.76915395660295));
#29358=CARTESIAN_POINT('Ctrl Pts',(368.794674436653,-15.674985604493,2.70942514763024));
#29359=CARTESIAN_POINT('Ctrl Pts',(368.712753386944,-15.6810560912227,2.64577353530503));
#29360=CARTESIAN_POINT('Ctrl Pts',(368.633891803325,-15.6871265779525,2.57847440581156));
#29361=CARTESIAN_POINT('Ctrl Pts',(368.555056086467,-15.6931950735501,2.51119735057105));
#29362=CARTESIAN_POINT('Ctrl Pts',(368.479278168274,-15.6992635691477,2.4402754346612));
#29363=CARTESIAN_POINT('Ctrl Pts',(368.40690508613,-15.7053320647453,2.36602458158218));
#29364=CARTESIAN_POINT('Ctrl Pts',(368.334536748511,-15.7114001625138,2.29177859612659));
#29365=CARTESIAN_POINT('Ctrl Pts',(368.265573103118,-15.7174682602823,2.21420441559934));
#29366=CARTESIAN_POINT('Ctrl Pts',(368.200324044597,-15.7235363580508,2.13365453591159));
#29367=CARTESIAN_POINT('Ctrl Pts',(368.135062139283,-15.7296056505583,2.05308879687357));
#29368=CARTESIAN_POINT('Ctrl Pts',(368.073516544506,-15.7356749430659,1.96954652887919));
#29369=CARTESIAN_POINT('Ctrl Pts',(368.015956014002,-15.7417442355735,1.883412224055));
#29370=CARTESIAN_POINT('Ctrl Pts',(367.958333931101,-15.7478200182837,1.79718581144496));
#29371=CARTESIAN_POINT('Ctrl Pts',(367.904705659556,-15.7538958009939,1.70836218635213));
#29372=CARTESIAN_POINT('Ctrl Pts',(367.855295787055,-15.7599715837041,1.61735357661238));
#29373=CARTESIAN_POINT('Ctrl Pts',(367.805856909444,-15.7660509330852,1.52629154202677));
#29374=CARTESIAN_POINT('Ctrl Pts',(367.760641549194,-15.7721302824663,1.43304235549025));
#29375=CARTESIAN_POINT('Ctrl Pts',(367.719826751698,-15.7782096318473,1.33803970083583));
#29376=CARTESIAN_POINT('Ctrl Pts',(367.678947355797,-15.7842986031374,1.24288668356181));
#29377=CARTESIAN_POINT('Ctrl Pts',(367.642482581195,-15.7903875744275,1.14597505873585));
#29378=CARTESIAN_POINT('Ctrl Pts',(367.610560106106,-15.7964765457175,1.04775524355367));
#29379=CARTESIAN_POINT('Ctrl Pts',(367.592007668837,-15.800015283161,0.990672672274866));
#29380=CARTESIAN_POINT('Ctrl Pts',(367.574988493561,-15.8035540206046,0.933148487401219));
#29381=CARTESIAN_POINT('Ctrl Pts',(367.559519679585,-15.8070927580481,0.875272520092086));
#29382=CARTESIAN_POINT('Ctrl Pts',(367.524528649451,-15.8150975132095,0.744354938486314));
#29383=CARTESIAN_POINT('Ctrl Pts',(367.497384183701,-15.823102268371,0.611307366002712));
#29384=CARTESIAN_POINT('Ctrl Pts',(367.478289125932,-15.8311070235325,0.476944697096577));
#29385=CARTESIAN_POINT('Ctrl Pts',(367.45956976824,-15.8389542831173,0.345225647588131));
#29386=CARTESIAN_POINT('Ctrl Pts',(367.44858613634,-15.8468015427021,0.212242435105983));
#29387=CARTESIAN_POINT('Ctrl Pts',(367.445483495871,-15.8546488022869,0.0787829989611029));
#29388=CARTESIAN_POINT('Ctrl Pts',(367.444912676366,-15.8560925302603,0.0542293163407381));
#29389=CARTESIAN_POINT('Ctrl Pts',(367.444608486778,-15.8575362582338,0.0296595777462121));
#29390=CARTESIAN_POINT('Ctrl Pts',(367.444571657931,-15.8589799862073,0.00507877902897487));
#29391=CARTESIAN_POINT('',(368.26108342621,-16.,-2.20655152809223));
#29392=CARTESIAN_POINT('Ctrl Pts',(367.444571791084,-15.8604132225308,0.00516688582735295));
#29393=CARTESIAN_POINT('Ctrl Pts',(367.444368925066,-15.8689596753995,-0.127923782203768));
#29394=CARTESIAN_POINT('Ctrl Pts',(367.452004419869,-15.8774239806517,-0.260919577064219));
#29395=CARTESIAN_POINT('Ctrl Pts',(367.479606817387,-15.8922327881285,-0.497313792977768));
#29396=CARTESIAN_POINT('Ctrl Pts',(367.496601528192,-15.8986398126175,-0.60088279544555));
#29397=CARTESIAN_POINT('Ctrl Pts',(367.533806436283,-15.9093613893647,-0.776246727587198));
#29398=CARTESIAN_POINT('Ctrl Pts',(367.551629335393,-15.9137397185277,-0.848464409357345));
#29399=CARTESIAN_POINT('Ctrl Pts',(367.595944192492,-15.9232110648643,-1.00560666487732));
#29400=CARTESIAN_POINT('Ctrl Pts',(367.623431929418,-15.9282724154365,-1.09019356338717));
#29401=CARTESIAN_POINT('Ctrl Pts',(367.690219426018,-15.9390944475785,-1.27116653976022));
#29402=CARTESIAN_POINT('Ctrl Pts',(367.730695232446,-15.9448218038598,-1.36702142877395));
#29403=CARTESIAN_POINT('Ctrl Pts',(367.877191286025,-15.9633925603866,-1.6737587249561));
#29404=CARTESIAN_POINT('Ctrl Pts',(368.000806589721,-15.9759676173899,-1.87543678879479));
#29405=CARTESIAN_POINT('Ctrl Pts',(368.165052549216,-15.9912516825638,-2.08963778707627));
#29406=CARTESIAN_POINT('Ctrl Pts',(368.186166578252,-15.993194783547,-2.11633126665893));
#29407=CARTESIAN_POINT('Ctrl Pts',(368.225218517582,-15.9967580887144,-2.16420324926291));
#29408=CARTESIAN_POINT('Ctrl Pts',(368.243021585248,-15.9983715362902,-2.18548818541282));
#29409=CARTESIAN_POINT('Ctrl Pts',(368.261083426209,-16.0000000000003,-2.2065515280925));
#29410=CARTESIAN_POINT('',(373.376670596656,-16.,-2.24206324408181));
#29411=CARTESIAN_POINT('Origin',(370.834317853224,-16.,0.));
#29412=CARTESIAN_POINT('Ctrl Pts',(373.376670596656,-16.,-2.24206324408178));
#29413=CARTESIAN_POINT('Ctrl Pts',(373.181129850895,-15.9815073064942,-2.46379363137158));
#29414=CARTESIAN_POINT('Ctrl Pts',(372.957360744741,-15.9621520677859,-2.65906379107586));
#29415=CARTESIAN_POINT('Ctrl Pts',(372.624823145168,-15.9373252245759,-2.88013923328604));
#29416=CARTESIAN_POINT('Ctrl Pts',(372.536073584592,-15.9310067923377,-2.93345220247366));
#29417=CARTESIAN_POINT('Ctrl Pts',(372.382793677882,-15.9205976093272,-3.01622752956713));
#29418=CARTESIAN_POINT('Ctrl Pts',(372.319531307382,-15.9164369440155,-3.04787597287237));
#29419=CARTESIAN_POINT('Ctrl Pts',(372.181961182041,-15.9076570415518,-3.11139705929018));
#29420=CARTESIAN_POINT('Ctrl Pts',(372.107409577823,-15.903060053103,-3.14263791780728));
#29421=CARTESIAN_POINT('Ctrl Pts',(371.829792649048,-15.8864392827796,-3.24747049345628));
#29422=CARTESIAN_POINT('Ctrl Pts',(371.620948274416,-15.8749254565236,-3.3042783361045));
#29423=CARTESIAN_POINT('Ctrl Pts',(371.294039411643,-15.8571425492,-3.36042503244688));
#29424=CARTESIAN_POINT('Ctrl Pts',(371.1790482447,-15.8509221310753,-3.3741604633309));
#29425=CARTESIAN_POINT('Ctrl Pts',(370.987595630786,-15.8403343195617,-3.38713921303782));
#29426=CARTESIAN_POINT('Ctrl Pts',(370.911458383628,-15.836062878099,-3.38972769808728));
#29427=CARTESIAN_POINT('Ctrl Pts',(370.793483966147,-15.8292657561943,-3.38976202483508));
#29428=CARTESIAN_POINT('Ctrl Pts',(370.751668630722,-15.8268212488625,-3.38900029485282));
#29429=CARTESIAN_POINT('Ctrl Pts',(370.659661419984,-15.8213480916324,-3.38562036872409));
#29430=CARTESIAN_POINT('Ctrl Pts',(370.60949513568,-15.8183049363756,-3.38265935375856));
#29431=CARTESIAN_POINT('Ctrl Pts',(370.308538621423,-15.7997639362016,-3.35817175643423));
#29432=CARTESIAN_POINT('Ctrl Pts',(370.060724557639,-15.7833721310607,-3.30988069002626));
#29433=CARTESIAN_POINT('Ctrl Pts',(369.671815573573,-15.7574845746523,-3.18799112169855));
#29434=CARTESIAN_POINT('Ctrl Pts',(369.526463382616,-15.7477541465874,-3.13116995294513));
#29435=CARTESIAN_POINT('Ctrl Pts',(369.317224026491,-15.7337521781211,-3.03224980723153));
#29436=CARTESIAN_POINT('Ctrl Pts',(369.250019055329,-15.7292534396165,-2.99768430518787));
#29437=CARTESIAN_POINT('Ctrl Pts',(369.120795446843,-15.7205873274601,-2.92565981991112));
#29438=CARTESIAN_POINT('Ctrl Pts',(369.058711579588,-15.7164161902242,-2.88840230383671));
#29439=CARTESIAN_POINT('Ctrl Pts',(368.895611415357,-15.7054018723884,-2.78327541581863));
#29440=CARTESIAN_POINT('Ctrl Pts',(368.796974851988,-15.6986831471059,-2.71190744469673));
#29441=CARTESIAN_POINT('Ctrl Pts',(368.512214597918,-15.6787819523762,-2.48154622506456));
#29442=CARTESIAN_POINT('Ctrl Pts',(368.339269910257,-15.6660283890105,-2.30758724485276));
#29443=CARTESIAN_POINT('Ctrl Pts',(368.136792464523,-15.6481987742494,-2.05429158960542));
#29444=CARTESIAN_POINT('Ctrl Pts',(368.089242598258,-15.6437435333288,-1.99030580620531));
#29445=CARTESIAN_POINT('Ctrl Pts',(368.020127289003,-15.6367444247644,-1.89010674556755));
#29446=CARTESIAN_POINT('Ctrl Pts',(367.996905841995,-15.6342923527546,-1.85506468777503));
#29447=CARTESIAN_POINT('Ctrl Pts',(367.948509069746,-15.6289422105522,-1.77899655050264));
#29448=CARTESIAN_POINT('Ctrl Pts',(367.923544980871,-15.626034023493,-1.73784976699607));
#29449=CARTESIAN_POINT('Ctrl Pts',(367.788875678473,-15.6095448407672,-1.50483647351955));
#29450=CARTESIAN_POINT('Ctrl Pts',(367.697269890652,-15.5952341464205,-1.30313907047644));
#29451=CARTESIAN_POINT('Ctrl Pts',(367.585313285836,-15.5730710283633,-0.974796926929378));
#29452=CARTESIAN_POINT('Ctrl Pts',(367.551346176506,-15.5650970921987,-0.853440525345097));
#29453=CARTESIAN_POINT('Ctrl Pts',(367.502936543691,-15.5511694015422,-0.634072694639167));
#29454=CARTESIAN_POINT('Ctrl Pts',(367.485883754585,-15.5451568403413,-0.536788145642456));
#29455=CARTESIAN_POINT('Ctrl Pts',(367.464094627573,-15.5351197794893,-0.36991737839074));
#29456=CARTESIAN_POINT('Ctrl Pts',(367.457213189075,-15.5310346384404,-0.300680169648971));
#29457=CARTESIAN_POINT('Ctrl Pts',(367.44694727203,-15.5223316747026,-0.150566255261707));
#29458=CARTESIAN_POINT('Ctrl Pts',(367.444318485203,-15.5177385953621,-0.0696805304459789));
#29459=CARTESIAN_POINT('Ctrl Pts',(367.445415315348,-15.4992324152054,0.261494802441862));
#29460=CARTESIAN_POINT('Ctrl Pts',(367.473956208093,-15.4860609706456,0.510897509708436));
#29461=CARTESIAN_POINT('Ctrl Pts',(367.561438832565,-15.4650019222951,0.893860808524713));
#29462=CARTESIAN_POINT('Ctrl Pts',(367.601914910565,-15.4572839725652,1.03067359573983));
#29463=CARTESIAN_POINT('Ctrl Pts',(367.667227884636,-15.4464920090718,1.20921946241856));
#29464=CARTESIAN_POINT('Ctrl Pts',(367.684518334353,-15.4437495089187,1.25356813036079));
#29465=CARTESIAN_POINT('Ctrl Pts',(367.718818462732,-15.4384872562773,1.33635096595479));
#29466=CARTESIAN_POINT('Ctrl Pts',(367.735619858271,-15.4359779786288,1.37486015810798));
#29467=CARTESIAN_POINT('Ctrl Pts',(367.785713281397,-15.4287013156099,1.48409043161024));
#29468=CARTESIAN_POINT('Ctrl Pts',(367.82074077183,-15.4238521825269,1.55398381326585));
#29469=CARTESIAN_POINT('Ctrl Pts',(367.955245838918,-15.4061800543025,1.80069278290662));
#29470=CARTESIAN_POINT('Ctrl Pts',(368.068130614859,-15.3930403856624,1.96971054294453));
#29471=CARTESIAN_POINT('Ctrl Pts',(368.290250308091,-15.3705880698647,2.245203272554));
#29472=CARTESIAN_POINT('Ctrl Pts',(368.3928117271,-15.3611728460088,2.35632640979305));
#29473=CARTESIAN_POINT('Ctrl Pts',(368.556872201341,-15.347506755999,2.51182560962108));
#29474=CARTESIAN_POINT('Ctrl Pts',(368.612988702248,-15.3430449324642,2.56158635832513));
#29475=CARTESIAN_POINT('Ctrl Pts',(368.726365910705,-15.3344226245516,2.65559225676189));
#29476=CARTESIAN_POINT('Ctrl Pts',(368.783483518159,-15.3302592822766,2.69994652608585));
#29477=CARTESIAN_POINT('Ctrl Pts',(368.941226536833,-15.319199642174,2.81454419418131));
#29478=CARTESIAN_POINT('Ctrl Pts',(369.044319700471,-15.3124315283819,2.88120881749646));
#29479=CARTESIAN_POINT('Ctrl Pts',(369.361922022979,-15.2925699548962,3.06294263369627));
#29480=CARTESIAN_POINT('Ctrl Pts',(369.585409599288,-15.2798939253938,3.16066181787488));
#29481=CARTESIAN_POINT('Ctrl Pts',(369.893163928145,-15.2621618525088,3.25744373128031));
#29482=CARTESIAN_POINT('Ctrl Pts',(369.969720993533,-15.2577242499199,3.27859434104151));
#29483=CARTESIAN_POINT('Ctrl Pts',(370.087724318164,-15.2507499141775,3.30677501825687));
#29484=CARTESIAN_POINT('Ctrl Pts',(370.128680391649,-15.2483045801731,3.31575611149422));
#29485=CARTESIAN_POINT('Ctrl Pts',(370.217159029718,-15.2429513328119,3.33344466156055));
#29486=CARTESIAN_POINT('Ctrl Pts',(370.264719933196,-15.2400329123458,3.34190005784656));
#29487=CARTESIAN_POINT('Ctrl Pts',(370.440641079645,-15.2291267817304,3.36931114247035));
#29488=CARTESIAN_POINT('Ctrl Pts',(370.569871638207,-15.2209017652042,3.38190805200113));
#29489=CARTESIAN_POINT('Ctrl Pts',(370.878679489492,-15.201155567086,3.39420021505435));
#29490=CARTESIAN_POINT('Ctrl Pts',(371.058159037159,-15.1896181542278,3.38710274522967));
#29491=CARTESIAN_POINT('Ctrl Pts',(371.354384885678,-15.1709103792875,3.35172981177866));
#29492=CARTESIAN_POINT('Ctrl Pts',(371.471714152433,-15.1635847541056,3.33141007565144));
#29493=CARTESIAN_POINT('Ctrl Pts',(371.657823241952,-15.1521187011189,3.28898321264146));
#29494=CARTESIAN_POINT('Ctrl Pts',(371.727382122338,-15.147867585696,3.27078110476225));
#29495=CARTESIAN_POINT('Ctrl Pts',(371.868732958214,-15.1392852872532,3.2289463313005));
#29496=CARTESIAN_POINT('Ctrl Pts',(371.940419163311,-15.1349634594056,3.20509752148028));
#29497=CARTESIAN_POINT('Ctrl Pts',(372.011709388664,-15.1306798775974,3.17870326891439));
#29498=CARTESIAN_POINT('Ctrl Pts',(372.012165924805,-15.1306524464985,3.17853413066531));
#29499=CARTESIAN_POINT('Ctrl Pts',(372.012622422822,-15.1306250182556,3.1783648946846));
#29500=CARTESIAN_POINT('Origin',(370.834317853224,-11.,0.));
#29501=CARTESIAN_POINT('',(372.012622418493,-13.8856567889318,3.1783648962896));
#29502=CARTESIAN_POINT('',(372.012622422842,-14.2257519494217,3.17836489467751));
#29503=CARTESIAN_POINT('',(372.012622422842,-11.,3.17836489467752));
#29504=CARTESIAN_POINT('',(367.444568873987,-14.6089821967165,-0.00263063910416286));
#29505=CARTESIAN_POINT('Ctrl Pts',(372.012622422842,-14.2257519494217,3.17836489467751));
#29506=CARTESIAN_POINT('Ctrl Pts',(371.91124658596,-14.2320990949235,3.21594761906723));
#29507=CARTESIAN_POINT('Ctrl Pts',(371.808171373033,-14.2384462404253,3.24863824573331));
#29508=CARTESIAN_POINT('Ctrl Pts',(371.703910693242,-14.2447933859271,3.27631093687543));
#29509=CARTESIAN_POINT('Ctrl Pts',(371.599650013451,-14.2511405314289,3.30398362801756));
#29510=CARTESIAN_POINT('Ctrl Pts',(371.494204378047,-14.2574876769308,3.32663833846832));
#29511=CARTESIAN_POINT('Ctrl Pts',(371.388095647466,-14.2638348224326,3.34420920653966));
#29512=CARTESIAN_POINT('Ctrl Pts',(371.285822638614,-14.2699525251375,3.3611449057602));
#29513=CARTESIAN_POINT('Ctrl Pts',(371.182610429071,-14.2760702278424,3.3734115222908));
#29514=CARTESIAN_POINT('Ctrl Pts',(371.078920131339,-14.2821879305474,3.38091330679169));
#29515=CARTESIAN_POINT('Ctrl Pts',(370.975360398977,-14.2882979299267,3.38840564515063));
#29516=CARTESIAN_POINT('Ctrl Pts',(370.871324196144,-14.2944079293061,3.39114505110587));
#29517=CARTESIAN_POINT('Ctrl Pts',(370.767281275843,-14.3005179286855,3.38908706878312));
#29518=CARTESIAN_POINT('Ctrl Pts',(370.663340093026,-14.3066219534539,3.3870310988409));
#29519=CARTESIAN_POINT('Ctrl Pts',(370.559392628715,-14.3127259782223,3.38018707898977));
#29520=CARTESIAN_POINT('Ctrl Pts',(370.45591134727,-14.3188300029908,3.36856253894029));
#29521=CARTESIAN_POINT('Ctrl Pts',(370.352498257132,-14.3249300053755,3.35694565914164));
#29522=CARTESIAN_POINT('Ctrl Pts',(370.249551160134,-14.3310300077602,3.34055457182891));
#29523=CARTESIAN_POINT('Ctrl Pts',(370.147539315721,-14.3371300101448,3.31944879504494));
#29524=CARTESIAN_POINT('Ctrl Pts',(370.04556157806,-14.343227973048,3.29835007478964));
#29525=CARTESIAN_POINT('Ctrl Pts',(369.944518887154,-14.3493259359512,3.27253988471554));
#29526=CARTESIAN_POINT('Ctrl Pts',(369.844871427421,-14.3554238988543,3.24212905865364));
#29527=CARTESIAN_POINT('Ctrl Pts',(369.745231894195,-14.361521376692,3.21172065163599));
#29528=CARTESIAN_POINT('Ctrl Pts',(369.64698777777,-14.3676188545297,3.17671246085942));
#29529=CARTESIAN_POINT('Ctrl Pts',(369.550584338613,-14.3737163323674,3.13726526228891));
#29530=CARTESIAN_POINT('Ctrl Pts',(369.454164005467,-14.3798148787429,3.09781115088893));
#29531=CARTESIAN_POINT('Ctrl Pts',(369.359585383833,-14.3859134251184,3.05391664693505));
#29532=CARTESIAN_POINT('Ctrl Pts',(369.267273164675,-14.392011971494,3.00579041295133));
#29533=CARTESIAN_POINT('Ctrl Pts',(369.174868353328,-14.3981166349119,2.95761590677372));
#29534=CARTESIAN_POINT('Ctrl Pts',(369.084734860711,-14.4042212983298,2.90520139258086));
#29535=CARTESIAN_POINT('Ctrl Pts',(368.997272123444,-14.4103259617477,2.84880115999623));
#29536=CARTESIAN_POINT('Ctrl Pts',(368.909760749328,-14.4164340198866,2.79236956400288));
#29537=CARTESIAN_POINT('Ctrl Pts',(368.824923435153,-14.4225420780255,2.73194808084853));
#29538=CARTESIAN_POINT('Ctrl Pts',(368.743128469909,-14.4286501361644,2.66783283314581));
#29539=CARTESIAN_POINT('Ctrl Pts',(368.661211980528,-14.4347672691466,2.60362232835576));
#29540=CARTESIAN_POINT('Ctrl Pts',(368.582347188466,-14.4408844021289,2.53570737689277));
#29541=CARTESIAN_POINT('Ctrl Pts',(368.506867344009,-14.4470015351111,2.46442268891778));
#29542=CARTESIAN_POINT('Ctrl Pts',(368.466804260173,-14.4502483782022,2.42658630423728));
#29543=CARTESIAN_POINT('Ctrl Pts',(368.427694157088,-14.4534952212934,2.38780117871283));
#29544=CARTESIAN_POINT('Ctrl Pts',(368.389582259366,-14.4567420643846,2.34812115075559));
#29545=CARTESIAN_POINT('Ctrl Pts',(368.315123261944,-14.4630854032317,2.27059850622654));
#29546=CARTESIAN_POINT('Ctrl Pts',(368.244214620814,-14.4694287420789,2.1893839797476));
#29547=CARTESIAN_POINT('Ctrl Pts',(368.177245026862,-14.4757720809261,2.10484418851099));
#29548=CARTESIAN_POINT('Ctrl Pts',(368.113616044009,-14.481798998142,2.02452145382602));
#29549=CARTESIAN_POINT('Ctrl Pts',(368.053542963847,-14.487825915358,1.94119757354517));
#29550=CARTESIAN_POINT('Ctrl Pts',(367.997322392813,-14.493852832574,1.85522554426817));
#29551=CARTESIAN_POINT('Ctrl Pts',(367.941149535837,-14.4998746347817,1.76932647893339));
#29552=CARTESIAN_POINT('Ctrl Pts',(367.888822931825,-14.5058964369894,1.68078409341299));
#29553=CARTESIAN_POINT('Ctrl Pts',(367.840598028115,-14.5119182391971,1.5899832298651));
#29554=CARTESIAN_POINT('Ctrl Pts',(367.792400881935,-14.517936575346,1.49923462992842));
#29555=CARTESIAN_POINT('Ctrl Pts',(367.748300949639,-14.523954911495,1.40623052089193));
#29556=CARTESIAN_POINT('Ctrl Pts',(367.708509001295,-14.5299732476439,1.31138250853956));
#29557=CARTESIAN_POINT('Ctrl Pts',(367.668729090899,-14.5359897631126,1.2165631898157));
#29558=CARTESIAN_POINT('Ctrl Pts',(367.633254741903,-14.5420062785813,1.11990148061017));
#29559=CARTESIAN_POINT('Ctrl Pts',(367.602249173642,-14.54802279405,1.02183027600718));
#29560=CARTESIAN_POINT('Ctrl Pts',(367.571234157724,-14.5540411428015,0.923729188283593));
#29561=CARTESIAN_POINT('Ctrl Pts',(367.544690779183,-14.5600594915531,0.824218163703193));
#29562=CARTESIAN_POINT('Ctrl Pts',(367.522732626955,-14.5660778403046,0.723746054672887));
#29563=CARTESIAN_POINT('Ctrl Pts',(367.500770556816,-14.5720972628875,0.623256018781771));
#29564=CARTESIAN_POINT('Ctrl Pts',(367.483395422998,-14.5781166854704,0.521804987559546));
#29565=CARTESIAN_POINT('Ctrl Pts',(367.470669535808,-14.5841361080533,0.419851234659084));
#29566=CARTESIAN_POINT('Ctrl Pts',(367.457932447937,-14.5901608286269,0.317807747233233));
#29567=CARTESIAN_POINT('Ctrl Pts',(367.449852814453,-14.5961855492004,0.215261091024579));
#29568=CARTESIAN_POINT('Ctrl Pts',(367.446440971499,-14.6022102697739,0.112673407565595));
#29569=CARTESIAN_POINT('Ctrl Pts',(367.445162641052,-14.6044675787548,0.0742364217549553));
#29570=CARTESIAN_POINT('Ctrl Pts',(367.444539054526,-14.6067248877357,0.0357936694278519));
#29571=CARTESIAN_POINT('Ctrl Pts',(367.444568873987,-14.6089821967165,-0.00263063910417031));
#29572=CARTESIAN_POINT('Ctrl Pts',(367.444568873987,-14.6089821967504,-0.00263063968060246));
#29573=CARTESIAN_POINT('Ctrl Pts',(367.444678491567,-14.6172801566126,-0.143879964709788));
#29574=CARTESIAN_POINT('Ctrl Pts',(367.453620519671,-14.6255781164748,-0.284780872301649));
#29575=CARTESIAN_POINT('Ctrl Pts',(367.471242920486,-14.633876076337,-0.424419673543423));
#29576=CARTESIAN_POINT('Ctrl Pts',(367.482408804865,-14.6391338196701,-0.512897442594087));
#29577=CARTESIAN_POINT('Ctrl Pts',(367.497058665012,-14.6443915630033,-0.600869113347477));
#29578=CARTESIAN_POINT('Ctrl Pts',(367.515144168952,-14.6496493063364,-0.688106907490654));
#29579=CARTESIAN_POINT('Ctrl Pts',(367.536190000969,-14.6557676640746,-0.789624231375929));
#29580=CARTESIAN_POINT('Ctrl Pts',(367.56193066331,-14.6618860218127,-0.890335427005092));
#29581=CARTESIAN_POINT('Ctrl Pts',(367.592289324518,-14.6680043795509,-0.989775773373781));
#29582=CARTESIAN_POINT('Ctrl Pts',(367.622609746661,-14.6741150307476,-1.08909086698887));
#29583=CARTESIAN_POINT('Ctrl Pts',(367.657536478472,-14.6802256819443,-1.18713789094678));
#29584=CARTESIAN_POINT('Ctrl Pts',(367.69694172691,-14.686336333141,-1.28346254504481));
#29585=CARTESIAN_POINT('Ctrl Pts',(367.736308420847,-14.6924410056138,-1.37969295411159));
#29586=CARTESIAN_POINT('Ctrl Pts',(367.780144756326,-14.6985456780865,-1.47420395355472));
#29587=CARTESIAN_POINT('Ctrl Pts',(367.828273468945,-14.7046503505593,-1.56655744300817));
#29588=CARTESIAN_POINT('Ctrl Pts',(367.876370399687,-14.7107509918013,-1.65884994667818));
#29589=CARTESIAN_POINT('Ctrl Pts',(367.928753874277,-14.7168516330433,-1.7489873981159));
#29590=CARTESIAN_POINT('Ctrl Pts',(367.98519928576,-14.7229522742852,-1.83655341633011));
#29591=CARTESIAN_POINT('Ctrl Pts',(368.041625773511,-14.729050870243,-1.92409007740244));
#29592=CARTESIAN_POINT('Ctrl Pts',(368.102111260977,-14.7351494662008,-2.00905666226684));
#29593=CARTESIAN_POINT('Ctrl Pts',(368.166386539706,-14.7412480621586,-2.09106374098151));
#29594=CARTESIAN_POINT('Ctrl Pts',(368.230656636426,-14.7473461664348,-2.17306420811305));
#29595=CARTESIAN_POINT('Ctrl Pts',(368.298715654354,-14.753444270711,-2.25210530946646));
#29596=CARTESIAN_POINT('Ctrl Pts',(368.370253171042,-14.7595423749871,-2.32782952651722));
#29597=CARTESIAN_POINT('Ctrl Pts',(368.441803135644,-14.7656415403663,-2.40356691998958));
#29598=CARTESIAN_POINT('Ctrl Pts',(368.516832509931,-14.7717407057454,-2.47598597351562));
#29599=CARTESIAN_POINT('Ctrl Pts',(368.594993607598,-14.7778398711246,-2.54476560520858));
#29600=CARTESIAN_POINT('Ctrl Pts',(368.673232903487,-14.783945138566,-2.61361404920098));
#29601=CARTESIAN_POINT('Ctrl Pts',(368.75460985913,-14.7900504060074,-2.6788155202828));
#29602=CARTESIAN_POINT('Ctrl Pts',(368.838743319677,-14.7961556734488,-2.74008892986352));
#29603=CARTESIAN_POINT('Ctrl Pts',(368.922923454412,-14.8022643278708,-2.80139633170603));
#29604=CARTESIAN_POINT('Ctrl Pts',(369.009862785874,-14.8083729822929,-2.85877109705749));
#29605=CARTESIAN_POINT('Ctrl Pts',(369.099152350093,-14.8144816367149,-2.91197626007593));
#29606=CARTESIAN_POINT('Ctrl Pts',(369.188574303088,-14.8205993483798,-2.96526030987622));
#29607=CARTESIAN_POINT('Ctrl Pts',(369.280353073307,-14.8267170600448,-3.01436221111961));
#29608=CARTESIAN_POINT('Ctrl Pts',(369.374056317144,-14.8328347717098,-3.05909158227477));
#29609=CARTESIAN_POINT('Ctrl Pts',(369.423691543035,-14.8360753639027,-3.08278502500238));
#29610=CARTESIAN_POINT('Ctrl Pts',(369.473866428129,-14.8393159560956,-3.10525240129708));
#29611=CARTESIAN_POINT('Ctrl Pts',(369.524514850808,-14.8425565482884,-3.12647103894502));
#29612=CARTESIAN_POINT('Ctrl Pts',(369.620132428815,-14.8486743612509,-3.16652904338437));
#29613=CARTESIAN_POINT('Ctrl Pts',(369.71774026339,-14.8547921742134,-3.20225986171064));
#29614=CARTESIAN_POINT('Ctrl Pts',(369.816911691517,-14.8609099871759,-3.23346405030593));
#29615=CARTESIAN_POINT('Ctrl Pts',(369.915958346431,-14.86702010297,-3.26462897913713));
#29616=CARTESIAN_POINT('Ctrl Pts',(370.016564280881,-14.8731302187641,-3.29127847606453));
#29617=CARTESIAN_POINT('Ctrl Pts',(370.118282604491,-14.8792403345582,-3.31326101976171));
#29618=CARTESIAN_POINT('Ctrl Pts',(370.219901562857,-14.8853444815835,-3.33522208944361));
#29619=CARTESIAN_POINT('Ctrl Pts',(370.322630335728,-14.8914486286089,-3.35252518385291));
#29620=CARTESIAN_POINT('Ctrl Pts',(370.426007415101,-14.8975527756342,-3.36506874352068));
#29621=CARTESIAN_POINT('Ctrl Pts',(370.52931650728,-14.9036529081931,-3.37760405376389));
#29622=CARTESIAN_POINT('Ctrl Pts',(370.633272637189,-14.9097530407519,-3.38538600365403));
#29623=CARTESIAN_POINT('Ctrl Pts',(370.737405434675,-14.9158531733107,-3.38836436140374));
#29624=CARTESIAN_POINT('Ctrl Pts',(370.841503498906,-14.9219512711843,-3.39134172572908));
#29625=CARTESIAN_POINT('Ctrl Pts',(370.945777689179,-14.928049369058,-3.38951867092157));
#29626=CARTESIAN_POINT('Ctrl Pts',(371.049754640543,-14.9341474669317,-3.38289699121475));
#29627=CARTESIAN_POINT('Ctrl Pts',(371.153723398455,-14.9402450842712,-3.3762758333006));
#29628=CARTESIAN_POINT('Ctrl Pts',(371.257394539983,-14.9463427016108,-3.36485682990787));
#29629=CARTESIAN_POINT('Ctrl Pts',(371.360297713031,-14.9524403189504,-3.3486938124554));
#29630=CARTESIAN_POINT('Ctrl Pts',(371.463218990748,-14.9585390090979,-3.33252795129991));
#29631=CARTESIAN_POINT('Ctrl Pts',(371.565371611726,-14.9646376992453,-3.31161648354425));
#29632=CARTESIAN_POINT('Ctrl Pts',(371.666294203627,-14.9707363893928,-3.2860645786214));
#29633=CARTESIAN_POINT('Ctrl Pts',(371.767318111185,-14.9768412019831,-3.26048702227629));
#29634=CARTESIAN_POINT('Ctrl Pts',(371.867109111646,-14.9829460145734,-3.23025983199035));
#29635=CARTESIAN_POINT('Ctrl Pts',(371.965219891154,-14.9890508271636,-3.19553839643754));
#29636=CARTESIAN_POINT('Ctrl Pts',(372.063385279427,-14.9951590377116,-3.16079763482564));
#29637=CARTESIAN_POINT('Ctrl Pts',(372.159868190242,-15.0012672482596,-3.12155780481548));
#29638=CARTESIAN_POINT('Ctrl Pts',(372.254241977364,-15.0073754588075,-3.07802218058713));
#29639=CARTESIAN_POINT('Ctrl Pts',(372.348756026856,-15.01349274764,-3.03442185184674));
#29640=CARTESIAN_POINT('Ctrl Pts',(372.441154315709,-15.0196100364725,-2.98651317438402));
#29641=CARTESIAN_POINT('Ctrl Pts',(372.531035399137,-15.0257273253049,-2.93454504683261));
#29642=CARTESIAN_POINT('Ctrl Pts',(372.578721230837,-15.0289728136167,-2.9069736904403));
#29643=CARTESIAN_POINT('Ctrl Pts',(372.625699018816,-15.0322183019285,-2.87826042788618));
#29644=CARTESIAN_POINT('Ctrl Pts',(372.671912418313,-15.0354637902403,-2.84844716939898));
#29645=CARTESIAN_POINT('Ctrl Pts',(372.758966103217,-15.0415774222159,-2.7922869639474));
#29646=CARTESIAN_POINT('Ctrl Pts',(372.843581656635,-15.0476910541914,-2.73204285312905));
#29647=CARTESIAN_POINT('Ctrl Pts',(372.925353574086,-15.0538046861669,-2.66795327481173));
#29648=CARTESIAN_POINT('Ctrl Pts',(373.007022294952,-15.0599106027072,-2.60394457787502));
#29649=CARTESIAN_POINT('Ctrl Pts',(373.085854182912,-15.0660165192474,-2.5361003234214));
#29650=CARTESIAN_POINT('Ctrl Pts',(373.161471772641,-15.0721224357876,-2.46470276054571));
#29651=CARTESIAN_POINT('Ctrl Pts',(373.23701529353,-15.0782223714686,-2.39337513291565));
#29652=CARTESIAN_POINT('Ctrl Pts',(373.309350469883,-15.0843223071496,-2.31850140982599));
#29653=CARTESIAN_POINT('Ctrl Pts',(373.378132740677,-15.0904222428306,-2.24040417801623));
#29654=CARTESIAN_POINT('Ctrl Pts',(373.446869744383,-15.0965181640131,-2.16235834366976));
#29655=CARTESIAN_POINT('Ctrl Pts',(373.512058212156,-15.1026140851956,-2.0810935382982));
#29656=CARTESIAN_POINT('Ctrl Pts',(373.573390877461,-15.1087100063781,-1.9969687104201));
#29657=CARTESIAN_POINT('Ctrl Pts',(373.634703092097,-15.114803894946,-1.91287193299475));
#29658=CARTESIAN_POINT('Ctrl Pts',(373.692161809484,-15.120897783514,-1.82591737239204));
#29659=CARTESIAN_POINT('Ctrl Pts',(373.745500961033,-15.1269916720819,-1.73649588980455));
#29660=CARTESIAN_POINT('Ctrl Pts',(373.798835972629,-15.1330850876688,-1.64708134772249));
#29661=CARTESIAN_POINT('Ctrl Pts',(373.848051836545,-15.1391785032557,-1.55520063016936));
#29662=CARTESIAN_POINT('Ctrl Pts',(373.892927096109,-15.1452719188426,-1.4612715565008));
#29663=CARTESIAN_POINT('Ctrl Pts',(373.937810352466,-15.1513664202791,-1.36732574462576));
#29664=CARTESIAN_POINT('Ctrl Pts',(373.978351284079,-15.1574609217156,-1.27133123539307));
#29665=CARTESIAN_POINT('Ctrl Pts',(374.014375849501,-15.1635554231521,-1.17372748234632));
#29666=CARTESIAN_POINT('Ctrl Pts',(374.050436870469,-15.1696560920019,-1.07602495786037));
#29667=CARTESIAN_POINT('Ctrl Pts',(374.081972252425,-15.1757567608516,-0.976710338023476));
#29668=CARTESIAN_POINT('Ctrl Pts',(374.108857320693,-15.1818574297013,-0.87623988638124));
#29669=CARTESIAN_POINT('Ctrl Pts',(374.135757452608,-15.1879615167426,-0.775713141362782));
#29670=CARTESIAN_POINT('Ctrl Pts',(374.158001989767,-15.1940656037839,-0.674029690166241));
#29671=CARTESIAN_POINT('Ctrl Pts',(374.175517441013,-15.2001696908251,-0.571655820453991));
#29672=CARTESIAN_POINT('Ctrl Pts',(374.193059143276,-15.2062829262743,-0.469128519457345));
#29673=CARTESIAN_POINT('Ctrl Pts',(374.205857553494,-15.2123961617234,-0.365909155705961));
#29674=CARTESIAN_POINT('Ctrl Pts',(374.213891062114,-15.2185093971726,-0.262469023419861));
#29675=CARTESIAN_POINT('Ctrl Pts',(374.218210843927,-15.2217966088458,-0.206847149673646));
#29676=CARTESIAN_POINT('Ctrl Pts',(374.221153783389,-15.225083820519,-0.151161453373989));
#29677=CARTESIAN_POINT('Ctrl Pts',(374.222722742927,-15.2283710321923,-0.0954848989914071));
#29678=CARTESIAN_POINT('Ctrl Pts',(374.225646482962,-15.2344967174866,0.00826779001192193));
#29679=CARTESIAN_POINT('Ctrl Pts',(374.22380511661,-15.240622402781,0.112316487565813));
#29680=CARTESIAN_POINT('Ctrl Pts',(374.217166772466,-15.2467480880754,0.216190314493111));
#29681=CARTESIAN_POINT('Ctrl Pts',(374.210536771381,-15.2528660746201,0.319933592993223));
#29682=CARTESIAN_POINT('Ctrl Pts',(374.199121807844,-15.2589840611649,0.423502018137774));
#29683=CARTESIAN_POINT('Ctrl Pts',(374.182942004536,-15.2651020477097,0.526423171743573));
#29684=CARTESIAN_POINT('Ctrl Pts',(374.166778019509,-15.2712140529687,0.629243703872613));
#29685=CARTESIAN_POINT('Ctrl Pts',(374.14585852571,-15.2773260582276,0.731417806450445));
#29686=CARTESIAN_POINT('Ctrl Pts',(374.120255515033,-15.2834380634865,0.83247747429178));
#29687=CARTESIAN_POINT('Ctrl Pts',(374.094669534451,-15.289546003285,0.933469921300837));
#29688=CARTESIAN_POINT('Ctrl Pts',(374.064406337256,-15.2956539430835,1.03334899828593));
#29689=CARTESIAN_POINT('Ctrl Pts',(374.029588980748,-15.301761882882,1.13165696397399));
#29690=CARTESIAN_POINT('Ctrl Pts',(373.994783425207,-15.3078677524603,1.22993160923945));
#29691=CARTESIAN_POINT('Ctrl Pts',(373.95542692049,-15.3139736220386,1.32663580284301));
#29692=CARTESIAN_POINT('Ctrl Pts',(373.911692128891,-15.3200794916169,1.42132777006712));
#29693=CARTESIAN_POINT('Ctrl Pts',(373.867961104058,-15.3261848353123,1.51601158171345));
#29694=CARTESIAN_POINT('Ctrl Pts',(373.819852720375,-15.3322901790076,1.60868312717393));
#29695=CARTESIAN_POINT('Ctrl Pts',(373.767587096109,-15.3383955227029,1.69892219105149));
#29696=CARTESIAN_POINT('Ctrl Pts',(373.71531276046,-15.3445018840075,1.78917629554126));
#29697=CARTESIAN_POINT('Ctrl Pts',(373.658880019764,-15.3506082453121,1.87699674618686));
#29698=CARTESIAN_POINT('Ctrl Pts',(373.598553654873,-15.3567146066167,1.96199018738174));
#29699=CARTESIAN_POINT('Ctrl Pts',(373.53816807586,-15.3628269616989,2.04706705498447));
#29700=CARTESIAN_POINT('Ctrl Pts',(373.473881487395,-15.3689393167812,2.12931102659843));
#29701=CARTESIAN_POINT('Ctrl Pts',(373.406000461701,-15.3750516718634,2.20835993980987));
#29702=CARTESIAN_POINT('Ctrl Pts',(373.338082407272,-15.3811673612026,2.28745197377941));
#29703=CARTESIAN_POINT('Ctrl Pts',(373.266566299743,-15.3872830505417,2.3633451686863));
#29704=CARTESIAN_POINT('Ctrl Pts',(373.19179596917,-15.3933987398809,2.43571385744193));
#29705=CARTESIAN_POINT('Ctrl Pts',(373.116916696127,-15.399523339951,2.50818798940859));
#29706=CARTESIAN_POINT('Ctrl Pts',(373.038774048626,-15.4056479400212,2.57712707956269));
#29707=CARTESIAN_POINT('Ctrl Pts',(372.957745372005,-15.4117725400914,2.64224537751176));
#29708=CARTESIAN_POINT('Ctrl Pts',(372.915824972209,-15.414941118109,2.67593450089272));
#29709=CARTESIAN_POINT('Ctrl Pts',(372.873132607385,-15.4181096961266,2.70860167443043));
#29710=CARTESIAN_POINT('Ctrl Pts',(372.829723411387,-15.4212782741442,2.7402119846744));
#29711=CARTESIAN_POINT('Ctrl Pts',(372.745956983784,-15.4273926573989,2.8012101834123));
#29712=CARTESIAN_POINT('Ctrl Pts',(372.659259889217,-15.4335070406537,2.8584593510474));
#29713=CARTESIAN_POINT('Ctrl Pts',(372.570001202592,-15.4396214239084,2.91166762753366));
#29714=CARTESIAN_POINT('Ctrl Pts',(372.480861478248,-15.4457276580293,2.96480498903985));
#29715=CARTESIAN_POINT('Ctrl Pts',(372.389167315509,-15.4518338921502,3.01391195612958));
#29716=CARTESIAN_POINT('Ctrl Pts',(372.295318353059,-15.4579401262711,3.05873872731598));
#29717=CARTESIAN_POINT('Ctrl Pts',(372.203034376697,-15.463944535383,3.10281798599457));
#29718=CARTESIAN_POINT('Ctrl Pts',(372.108667275517,-15.4699489444949,3.1427585082035));
#29719=CARTESIAN_POINT('Ctrl Pts',(372.012622422842,-15.4759533536068,3.17836489467751));
#29720=CARTESIAN_POINT('',(367.444568011016,-14.2687123280742,-0.00103428840593673));
#29721=CARTESIAN_POINT('Ctrl Pts',(372.012622422822,-15.1306250182556,3.1783648946846));
#29722=CARTESIAN_POINT('Ctrl Pts',(372.161032596329,-15.1217079361894,3.12334528824775));
#29723=CARTESIAN_POINT('Ctrl Pts',(372.305414148786,-15.1131054391572,3.05799614709269));
#29724=CARTESIAN_POINT('Ctrl Pts',(372.626234746501,-15.0935376841111,2.8847866973167));
#29725=CARTESIAN_POINT('Ctrl Pts',(372.798420158046,-15.0826949788232,2.77042447763917));
#29726=CARTESIAN_POINT('Ctrl Pts',(373.014175051594,-15.0673780481445,2.59684781429391));
#29727=CARTESIAN_POINT('Ctrl Pts',(373.067817887976,-15.0634051567002,2.55085715505148));
#29728=CARTESIAN_POINT('Ctrl Pts',(373.149864917275,-15.056994278482,2.47594112509051));
#29729=CARTESIAN_POINT('Ctrl Pts',(373.1792540704,-15.0546253927127,2.44812513828116));
#29730=CARTESIAN_POINT('Ctrl Pts',(373.244456133965,-15.0491902514634,2.38416159347616));
#29731=CARTESIAN_POINT('Ctrl Pts',(373.279962741684,-15.0461059021237,2.34772517642751));
#29732=CARTESIAN_POINT('Ctrl Pts',(373.356662537957,-15.0391883457301,2.26538834555573));
#29733=CARTESIAN_POINT('Ctrl Pts',(373.39745034035,-15.0353364008036,2.21913455438393));
#29734=CARTESIAN_POINT('Ctrl Pts',(373.527516817818,-15.0225304767566,2.06326570295236));
#29735=CARTESIAN_POINT('Ctrl Pts',(373.611202371626,-15.0134356867424,1.94917852805273));
#29736=CARTESIAN_POINT('Ctrl Pts',(373.791970452569,-14.9920290988576,1.66736945561437));
#29737=CARTESIAN_POINT('Ctrl Pts',(373.882301309212,-14.9798215417997,1.49587559400311));
#29738=CARTESIAN_POINT('Ctrl Pts',(373.987577673462,-14.9633829645738,1.24633047091956));
#29739=CARTESIAN_POINT('Ctrl Pts',(374.01519497254,-14.9587633231341,1.17405676600786));
#29740=CARTESIAN_POINT('Ctrl Pts',(374.063345615591,-14.9500560196876,1.03383390403054));
#29741=CARTESIAN_POINT('Ctrl Pts',(374.084265342552,-14.9459581893863,0.966061689284126));
#29742=CARTESIAN_POINT('Ctrl Pts',(374.132246648781,-14.9356436411694,0.791346983459715));
#29743=CARTESIAN_POINT('Ctrl Pts',(374.15624401516,-14.9295212654196,0.683647579028431));
#29744=CARTESIAN_POINT('Ctrl Pts',(374.208333809067,-14.9127540858364,0.380996778704372));
#29745=CARTESIAN_POINT('Ctrl Pts',(374.224760961267,-14.9023802783531,0.184495066474512));
#29746=CARTESIAN_POINT('Ctrl Pts',(374.223581654608,-14.8849369854442,-0.139902469650937));
#29747=CARTESIAN_POINT('Ctrl Pts',(374.215915642548,-14.8779955794848,-0.267343846137505));
#29748=CARTESIAN_POINT('Ctrl Pts',(374.195477810469,-14.8680221677311,-0.441970342865693));
#29749=CARTESIAN_POINT('Ctrl Pts',(374.188845276725,-14.8652433628548,-0.489774723662178));
#29750=CARTESIAN_POINT('Ctrl Pts',(374.174560167472,-14.859954783472,-0.578737997443816));
#29751=CARTESIAN_POINT('Ctrl Pts',(374.16716147609,-14.8574570100149,-0.619926708056189));
#29752=CARTESIAN_POINT('Ctrl Pts',(374.143590976873,-14.8501412982478,-0.738487490188065));
#29753=CARTESIAN_POINT('Ctrl Pts',(374.125473354803,-14.8452384031095,-0.815442244455483));
#29754=CARTESIAN_POINT('Ctrl Pts',(374.041334333776,-14.8251222660819,-1.1240317721796));
#29755=CARTESIAN_POINT('Ctrl Pts',(373.953404546068,-14.8094634602587,-1.34896624894075));
#29756=CARTESIAN_POINT('Ctrl Pts',(373.784823303504,-14.7864706281466,-1.67347145753088));
#29757=CARTESIAN_POINT('Ctrl Pts',(373.721193318367,-14.7787644272893,-1.78099537334861));
#29758=CARTESIAN_POINT('Ctrl Pts',(373.61146277217,-14.7668915466797,-1.94502602878411));
#29759=CARTESIAN_POINT('Ctrl Pts',(373.569231248015,-14.7625977571072,-2.00397356073716));
#29760=CARTESIAN_POINT('Ctrl Pts',(373.479789195423,-14.7540237279204,-2.12071850201278));
#29761=CARTESIAN_POINT('Ctrl Pts',(373.432496037024,-14.7497497992707,-2.17840236998975));
#29762=CARTESIAN_POINT('Ctrl Pts',(373.286745472786,-14.7372699636077,-2.34466942369706));
#29763=CARTESIAN_POINT('Ctrl Pts',(373.183107685914,-14.7292694251476,-2.44848278155932));
#29764=CARTESIAN_POINT('Ctrl Pts',(372.87269969643,-14.7070186511462,-2.7215091649089));
#29765=CARTESIAN_POINT('Ctrl Pts',(372.652247452356,-14.6931519156511,-2.87344939549034));
#29766=CARTESIAN_POINT('Ctrl Pts',(372.37326153728,-14.6752685385109,-3.02066635570474));
#29767=CARTESIAN_POINT('Ctrl Pts',(372.329743820011,-14.6724681911783,-3.04244532166582));
#29768=CARTESIAN_POINT('Ctrl Pts',(372.248094252012,-14.6671673678145,-3.08113290220045));
#29769=CARTESIAN_POINT('Ctrl Pts',(372.210091483007,-14.6646799540019,-3.09828822672553));
#29770=CARTESIAN_POINT('Ctrl Pts',(372.100327774014,-14.6574539130264,-3.14542072861473));
#29771=CARTESIAN_POINT('Ctrl Pts',(372.027840722395,-14.6526335624937,-3.17363421292851));
#29772=CARTESIAN_POINT('Ctrl Pts',(371.734843158155,-14.6331231069796,-3.27621729852323));
#29773=CARTESIAN_POINT('Ctrl Pts',(371.507899067952,-14.618003500171,-3.33029138693313));
#29774=CARTESIAN_POINT('Ctrl Pts',(371.146969311252,-14.5950526482753,-3.37785555533012));
#29775=CARTESIAN_POINT('Ctrl Pts',(371.015843132775,-14.5869221363978,-3.38743469113806));
#29776=CARTESIAN_POINT('Ctrl Pts',(370.811330121631,-14.5745985275255,-3.39046142114457));
#29777=CARTESIAN_POINT('Ctrl Pts',(370.738161100129,-14.5702590859374,-3.38917573328246));
#29778=CARTESIAN_POINT('Ctrl Pts',(370.591430165902,-14.5616829878185,-3.38184113696394));
#29779=CARTESIAN_POINT('Ctrl Pts',(370.517909962575,-14.5574497732543,-3.37575637345786));
#29780=CARTESIAN_POINT('Ctrl Pts',(370.308142373715,-14.5455123115099,-3.35148120805942));
#29781=CARTESIAN_POINT('Ctrl Pts',(370.172722164459,-14.5379821371407,-3.32739884052919));
#29782=CARTESIAN_POINT('Ctrl Pts',(369.789857121636,-14.5167266111077,-3.23500559382736));
#29783=CARTESIAN_POINT('Ctrl Pts',(369.548242929142,-14.503394167927,-3.14676775322605));
#29784=CARTESIAN_POINT('Ctrl Pts',(369.266007709468,-14.4857513237065,-3.00571221788428));
#29785=CARTESIAN_POINT('Ctrl Pts',(369.213810524538,-14.4823912328421,-2.97789485603867));
#29786=CARTESIAN_POINT('Ctrl Pts',(369.127493438093,-14.4766262060756,-2.92895254361624));
#29787=CARTESIAN_POINT('Ctrl Pts',(369.092974450863,-14.4742609709537,-2.90856242904843));
#29788=CARTESIAN_POINT('Ctrl Pts',(369.008848629546,-14.468345250781,-2.85683547956148));
#29789=CARTESIAN_POINT('Ctrl Pts',(368.959682521089,-14.4647587832951,-2.82481651540905));
#29790=CARTESIAN_POINT('Ctrl Pts',(368.848659544897,-14.4564006769465,-2.74833872802926));
#29791=CARTESIAN_POINT('Ctrl Pts',(368.787420481439,-14.4515970621464,-2.70303805115297));
#29792=CARTESIAN_POINT('Ctrl Pts',(368.539424136349,-14.4314684463365,-2.5063234486351));
#29793=CARTESIAN_POINT('Ctrl Pts',(368.367490766731,-14.4159124005769,-2.33730139558551));
#29794=CARTESIAN_POINT('Ctrl Pts',(368.150095720162,-14.3946354824101,-2.07262546481399));
#29795=CARTESIAN_POINT('Ctrl Pts',(368.088898351667,-14.3884066571874,-1.990853991196));
#29796=CARTESIAN_POINT('Ctrl Pts',(367.992051158518,-14.3781229175823,-1.84846967827475));
#29797=CARTESIAN_POINT('Ctrl Pts',(367.954427826168,-14.3740002065088,-1.78928884980916));
#29798=CARTESIAN_POINT('Ctrl Pts',(367.877817820027,-14.3653019544361,-1.66009814992997));
#29799=CARTESIAN_POINT('Ctrl Pts',(367.83942255738,-14.3607483735162,-1.58978674066155));
#29800=CARTESIAN_POINT('Ctrl Pts',(367.763733007414,-14.3512895044746,-1.43868624120367));
#29801=CARTESIAN_POINT('Ctrl Pts',(367.72705547785,-14.346404665627,-1.35765656355363));
#29802=CARTESIAN_POINT('Ctrl Pts',(367.620696948552,-14.3310559962644,-1.09571952955257));
#29803=CARTESIAN_POINT('Ctrl Pts',(367.563322772153,-14.3208555793827,-0.910247476761653));
#29804=CARTESIAN_POINT('Ctrl Pts',(367.49749774033,-14.3041469388678,-0.607807753268595));
#29805=CARTESIAN_POINT('Ctrl Pts',(367.478694830229,-14.2978115900004,-0.493546797610184));
#29806=CARTESIAN_POINT('Ctrl Pts',(367.460581448105,-14.2885826425382,-0.33236769722821));
#29807=CARTESIAN_POINT('Ctrl Pts',(367.456341406009,-14.2858984701718,-0.28607736374207));
#29808=CARTESIAN_POINT('Ctrl Pts',(367.450383115971,-14.2809414647877,-0.20203436540787));
#29809=CARTESIAN_POINT('Ctrl Pts',(367.448341906129,-14.2786851309063,-0.164312631483862));
#29810=CARTESIAN_POINT('Ctrl Pts',(367.445368697389,-14.273869259302,-0.0847391577010026));
#29811=CARTESIAN_POINT('Ctrl Pts',(367.444580781391,-14.2713038080906,-0.0428875832871091));
#29812=CARTESIAN_POINT('Ctrl Pts',(367.444568011016,-14.2687123280742,-0.00103428840593673));
#29813=CARTESIAN_POINT('Ctrl Pts',(367.444568012178,-14.2687125633712,-0.00103808853340888));
#29814=CARTESIAN_POINT('Ctrl Pts',(367.444486813014,-14.2522952246477,0.264107747439789));
#29815=CARTESIAN_POINT('Ctrl Pts',(367.475513863648,-14.2349794374035,0.528358047726244));
#29816=CARTESIAN_POINT('Ctrl Pts',(367.568093262579,-14.2097942005167,0.91657956703046));
#29817=CARTESIAN_POINT('Ctrl Pts',(367.606854946636,-14.2014961560422,1.0449070873222));
#29818=CARTESIAN_POINT('Ctrl Pts',(367.678465512956,-14.188995533336,1.23951219689682));
#29819=CARTESIAN_POINT('Ctrl Pts',(367.706050543616,-14.1846387315909,1.30757000582848));
#29820=CARTESIAN_POINT('Ctrl Pts',(367.765625363201,-14.1760594106411,1.44184984123346));
#29821=CARTESIAN_POINT('Ctrl Pts',(367.797602562222,-14.1718393270823,1.50803379809492));
#29822=CARTESIAN_POINT('Ctrl Pts',(367.894187449857,-14.1600677601578,1.69238399549318));
#29823=CARTESIAN_POINT('Ctrl Pts',(367.96371929658,-14.1526812706842,1.80781610496656));
#29824=CARTESIAN_POINT('Ctrl Pts',(368.169445352685,-14.133049353021,2.10741596188419));
#29825=CARTESIAN_POINT('Ctrl Pts',(368.317703830206,-14.1210938331566,2.28240879893269));
#29826=CARTESIAN_POINT('Ctrl Pts',(368.537995053468,-14.1042569511467,2.49464561649203));
#29827=CARTESIAN_POINT('Ctrl Pts',(368.595351931787,-14.0999399590955,2.54624921906079));
#29828=CARTESIAN_POINT('Ctrl Pts',(368.686282515476,-14.0931084691456,2.62260957937955));
#29829=CARTESIAN_POINT('Ctrl Pts',(368.718639533968,-14.0906793160424,2.64878122313738));
#29830=CARTESIAN_POINT('Ctrl Pts',(368.789998573449,-14.085309354222,2.70435733068372));
#29831=CARTESIAN_POINT('Ctrl Pts',(368.82916857659,-14.0823564727328,2.73352624191801));
#29832=CARTESIAN_POINT('Ctrl Pts',(368.981141080323,-14.0709214243864,2.84167218438247));
#29833=CARTESIAN_POINT('Ctrl Pts',(369.098081785622,-14.062171411656,2.91459149570974));
#29834=CARTESIAN_POINT('Ctrl Pts',(369.371443525127,-14.0422852034675,3.0627472839411));
#29835=CARTESIAN_POINT('Ctrl Pts',(369.529879891887,-14.031153572064,3.13350769072499));
#29836=CARTESIAN_POINT('Ctrl Pts',(369.803261458631,-14.0129635656175,3.23125833311319));
#29837=CARTESIAN_POINT('Ctrl Pts',(369.915460915887,-14.0057628586697,3.2649370769629));
#29838=CARTESIAN_POINT('Ctrl Pts',(370.098790879406,-13.9944321512412,3.30976424414081));
#29839=CARTESIAN_POINT('Ctrl Pts',(370.168919351113,-13.9901965865602,3.32457293945563));
#29840=CARTESIAN_POINT('Ctrl Pts',(370.314135748325,-13.981612900004,3.35045787475958));
#29841=CARTESIAN_POINT('Ctrl Pts',(370.389232094695,-13.9772751940927,3.36125828875296));
#29842=CARTESIAN_POINT('Ctrl Pts',(370.746876534411,-13.9570133482044,3.40049703164021));
#29843=CARTESIAN_POINT('Ctrl Pts',(371.031882947741,-13.9421457106271,3.39587986295225));
#29844=CARTESIAN_POINT('Ctrl Pts',(371.44037943264,-13.9199453550903,3.3376119574648));
#29845=CARTESIAN_POINT('Ctrl Pts',(371.566623695341,-13.9129357714702,3.31220268270208));
#29846=CARTESIAN_POINT('Ctrl Pts',(371.736506950071,-13.9029526715152,3.26782218205719));
#29847=CARTESIAN_POINT('Ctrl Pts',(371.781654178895,-13.9002449115212,3.25502079464464));
#29848=CARTESIAN_POINT('Ctrl Pts',(371.867213124908,-13.8949837534719,3.22883007406804));
#29849=CARTESIAN_POINT('Ctrl Pts',(371.907665689606,-13.8924385122789,3.21560881994681));
#29850=CARTESIAN_POINT('Ctrl Pts',(371.969524478982,-13.8884673720548,3.19409413283978));
#29851=CARTESIAN_POINT('Ctrl Pts',(371.991114593161,-13.8870663757487,3.18633842028861));
#29852=CARTESIAN_POINT('Ctrl Pts',(372.012622418493,-13.8856567889318,3.1783648962896));
#29853=CARTESIAN_POINT('Origin',(370.834317853224,-11.,0.));
#29854=CARTESIAN_POINT('',(372.012622420937,-12.6303878084336,3.17836489538372));
#29855=CARTESIAN_POINT('',(372.012622422842,-12.9759351715034,3.17836489467752));
#29856=CARTESIAN_POINT('',(372.012622422842,-11.,3.17836489467752));
#29857=CARTESIAN_POINT('',(367.444568730885,-13.3589821967097,0.0024392836071674));
#29858=CARTESIAN_POINT('Ctrl Pts',(372.012622422842,-12.9759351715034,3.17836489467751));
#29859=CARTESIAN_POINT('Ctrl Pts',(371.915017028612,-12.9820340934391,3.21454981549423));
#29860=CARTESIAN_POINT('Ctrl Pts',(371.815689609152,-12.9881330153748,3.24625447667781));
#29861=CARTESIAN_POINT('Ctrl Pts',(371.715087288233,-12.9942319373105,3.27332403908544));
#29862=CARTESIAN_POINT('Ctrl Pts',(371.614508166246,-13.0003294528326,3.30038735924209));
#29863=CARTESIAN_POINT('Ctrl Pts',(371.51265513755,-13.0064269683546,3.32281759542008));
#29864=CARTESIAN_POINT('Ctrl Pts',(371.409989849561,-13.0125244838767,3.34050996333387));
#29865=CARTESIAN_POINT('Ctrl Pts',(371.307322076232,-13.0186221470086,3.35820275954781));
#29866=CARTESIAN_POINT('Ctrl Pts',(371.203842423507,-13.0247198101405,3.37115738811166));
#29867=CARTESIAN_POINT('Ctrl Pts',(371.100021206151,-13.0308174732724,3.37932046286574));
#29868=CARTESIAN_POINT('Ctrl Pts',(370.992791957507,-13.0371152980597,3.38775149839783));
#29869=CARTESIAN_POINT('Ctrl Pts',(370.885198813993,-13.0434131228471,3.39107091894942));
#29870=CARTESIAN_POINT('Ctrl Pts',(370.777762446394,-13.0497109476345,3.38927817513675));
#29871=CARTESIAN_POINT('Ctrl Pts',(370.673599818145,-13.0558168687185,3.38754005878492));
#29872=CARTESIAN_POINT('Ctrl Pts',(370.569584979175,-13.0619227898025,3.38099690442181));
#29873=CARTESIAN_POINT('Ctrl Pts',(370.466188147125,-13.0680287108865,3.36970111166964));
#29874=CARTESIAN_POINT('Ctrl Pts',(370.357916808497,-13.0744224875256,3.35787279374259));
#29875=CARTESIAN_POINT('Ctrl Pts',(370.250323700135,-13.0808162641646,3.34083282992388));
#29876=CARTESIAN_POINT('Ctrl Pts',(370.143936197829,-13.0872100408037,3.31870128700884));
#29877=CARTESIAN_POINT('Ctrl Pts',(370.037548695523,-13.0936038174428,3.29656974409381));
#29878=CARTESIAN_POINT('Ctrl Pts',(369.932367294469,-13.0999975940819,3.2693468176568));
#29879=CARTESIAN_POINT('Ctrl Pts',(369.828899033299,-13.106391370721,3.23721146344205));
#29880=CARTESIAN_POINT('Ctrl Pts',(369.729899428162,-13.112509008685,3.2064639922639));
#29881=CARTESIAN_POINT('Ctrl Pts',(369.63215510576,-13.1186266466489,3.17112243544486));
#29882=CARTESIAN_POINT('Ctrl Pts',(369.536121118617,-13.1247442846129,3.13130808141832));
#29883=CARTESIAN_POINT('Ctrl Pts',(369.4402080713,-13.1308542183662,3.09154386735977));
#29884=CARTESIAN_POINT('Ctrl Pts',(369.346001466061,-13.1369641521195,3.04731821790663));
#29885=CARTESIAN_POINT('Ctrl Pts',(369.253941066524,-13.1430740858728,2.99880213994855));
#29886=CARTESIAN_POINT('Ctrl Pts',(369.161970700197,-13.1491780442344,2.95033350973387));
#29887=CARTESIAN_POINT('Ctrl Pts',(369.072142739242,-13.155282002596,2.89758299346691));
#29888=CARTESIAN_POINT('Ctrl Pts',(368.984876048735,-13.1613859609576,2.84076927509254));
#29889=CARTESIAN_POINT('Ctrl Pts',(368.89766687766,-13.1674858960634,2.78399300391314));
#29890=CARTESIAN_POINT('Ctrl Pts',(368.813015974723,-13.1735858311693,2.723159088368));
#29891=CARTESIAN_POINT('Ctrl Pts',(368.731316017541,-13.1796857662751,2.65853123765991));
#29892=CARTESIAN_POINT('Ctrl Pts',(368.64964338308,-13.1857836613942,2.59392500028979));
#29893=CARTESIAN_POINT('Ctrl Pts',(368.570920065526,-13.1918815565134,2.52552761347874));
#29894=CARTESIAN_POINT('Ctrl Pts',(368.495507610443,-13.1979794516325,2.45364457710624));
#29895=CARTESIAN_POINT('Ctrl Pts',(368.420101159271,-13.2040768612718,2.38176726365232));
#29896=CARTESIAN_POINT('Ctrl Pts',(368.348005353698,-13.2101742709112,2.3064051460402));
#29897=CARTESIAN_POINT('Ctrl Pts',(368.279545996073,-13.2162716805506,2.22790166309281));
#29898=CARTESIAN_POINT('Ctrl Pts',(368.211074644952,-13.2223701584042,2.14938442700327));
#29899=CARTESIAN_POINT('Ctrl Pts',(368.146241286959,-13.2284686362579,2.06772505234103));
#29900=CARTESIAN_POINT('Ctrl Pts',(368.085331857782,-13.2345671141116,1.98330054690727));
#29901=CARTESIAN_POINT('Ctrl Pts',(368.024361334513,-13.2406717089322,1.89879136101349));
#29902=CARTESIAN_POINT('Ctrl Pts',(367.967322847398,-13.2467763037528,1.81151185189101));
#29903=CARTESIAN_POINT('Ctrl Pts',(367.914459292129,-13.2528808985734,1.72186847514613));
#29904=CARTESIAN_POINT('Ctrl Pts',(367.861566340936,-13.2589888879861,1.63217525026109));
#29905=CARTESIAN_POINT('Ctrl Pts',(367.81285314498,-13.2650968773988,1.54011591473524));
#29906=CARTESIAN_POINT('Ctrl Pts',(367.7685159951,-13.2712048668115,1.4461203370483));
#29907=CARTESIAN_POINT('Ctrl Pts',(367.724112968819,-13.2773219315112,1.35198510017342));
#29908=CARTESIAN_POINT('Ctrl Pts',(367.684099136276,-13.2834389962109,1.25590826811917));
#29909=CARTESIAN_POINT('Ctrl Pts',(367.648622161941,-13.2895560609105,1.15833847602657));
#29910=CARTESIAN_POINT('Ctrl Pts',(367.629787624147,-13.2928035781647,1.1065391901173));
#29911=CARTESIAN_POINT('Ctrl Pts',(367.612230948321,-13.2960510954188,1.05431936189359));
#29912=CARTESIAN_POINT('Ctrl Pts',(367.595968408265,-13.299298612673,1.00174744064329));
#29913=CARTESIAN_POINT('Ctrl Pts',(367.559542178408,-13.3065726799196,0.883992349435457));
#29914=CARTESIAN_POINT('Ctrl Pts',(367.529519206534,-13.3138467471663,0.764172611276169));
#29915=CARTESIAN_POINT('Ctrl Pts',(367.506097814895,-13.3211208144129,0.642928020050624));
#29916=CARTESIAN_POINT('Ctrl Pts',(367.482901522175,-13.3283249718652,0.52284868949087));
#29917=CARTESIAN_POINT('Ctrl Pts',(367.466180569951,-13.3355291293175,0.401371825250862));
#29918=CARTESIAN_POINT('Ctrl Pts',(367.456080611714,-13.3427332867697,0.279138321575045));
#29919=CARTESIAN_POINT('Ctrl Pts',(367.448487157846,-13.3481495900831,0.187239479087665));
#29920=CARTESIAN_POINT('Ctrl Pts',(367.444635275771,-13.3535658933964,0.0949133469536027));
#29921=CARTESIAN_POINT('Ctrl Pts',(367.444568730885,-13.3589821967097,0.00243928360717191));
#29922=CARTESIAN_POINT('Ctrl Pts',(367.444568730885,-13.3589821967504,0.00243928291276102));
#29923=CARTESIAN_POINT('Ctrl Pts',(367.444494118151,-13.3650551700416,-0.101246290872523));
#29924=CARTESIAN_POINT('Ctrl Pts',(367.449181100272,-13.3711281433329,-0.205001299518334));
#29925=CARTESIAN_POINT('Ctrl Pts',(367.458622117423,-13.3772011166241,-0.308355901186887));
#29926=CARTESIAN_POINT('Ctrl Pts',(367.468060504766,-13.3832723982799,-0.411681713281755));
#29927=CARTESIAN_POINT('Ctrl Pts',(367.482250256026,-13.3893436799356,-0.514606913146634));
#29928=CARTESIAN_POINT('Ctrl Pts',(367.501131809253,-13.3954149615913,-0.616665110718218));
#29929=CARTESIAN_POINT('Ctrl Pts',(367.520013029297,-13.4014861361136,-0.718721507377279));
#29930=CARTESIAN_POINT('Ctrl Pts',(367.543585807955,-13.4075573106359,-0.819910510422086));
#29931=CARTESIAN_POINT('Ctrl Pts',(367.571739325754,-13.4136284851582,-0.919775197855785));
#29932=CARTESIAN_POINT('Ctrl Pts',(367.599899692094,-13.4197011365364,-1.01966417807679));
#29933=CARTESIAN_POINT('Ctrl Pts',(367.632642895164,-13.4257737879145,-1.11822778979971));
#29934=CARTESIAN_POINT('Ctrl Pts',(367.66980831523,-13.4318464392927,-1.21502446331179));
#29935=CARTESIAN_POINT('Ctrl Pts',(367.707013316293,-13.4379255580158,-1.31192422482176));
#29936=CARTESIAN_POINT('Ctrl Pts',(367.748649780113,-13.4440046767389,-1.40705289148142));
#29937=CARTESIAN_POINT('Ctrl Pts',(367.794509072048,-13.4500837954619,-1.49998921208925));
#29938=CARTESIAN_POINT('Ctrl Pts',(367.840397119325,-13.456166726,-1.59298380694277));
#29939=CARTESIAN_POINT('Ctrl Pts',(367.890513059632,-13.462249656538,-1.68378294374827));
#29940=CARTESIAN_POINT('Ctrl Pts',(367.9446034245,-13.468332587076,-1.77199198161901));
#29941=CARTESIAN_POINT('Ctrl Pts',(367.998773130277,-13.4744244401874,-1.86033040640288));
#29942=CARTESIAN_POINT('Ctrl Pts',(368.056928655357,-13.4805162932987,-1.94607079582972));
#29943=CARTESIAN_POINT('Ctrl Pts',(368.118774650797,-13.48660814641,-2.0288494715611));
#29944=CARTESIAN_POINT('Ctrl Pts',(368.137717755651,-13.4884740491483,-2.05420414687838));
#29945=CARTESIAN_POINT('Ctrl Pts',(368.157006815312,-13.4903399518866,-2.07928121494589));
#29946=CARTESIAN_POINT('Ctrl Pts',(368.17663264358,-13.4922058546248,-2.10407090872422));
#29947=CARTESIAN_POINT('Ctrl Pts',(368.240978883023,-13.4983234983102,-2.18534766045084));
#29948=CARTESIAN_POINT('Ctrl Pts',(368.309158580173,-13.5044411419956,-2.26379845328729));
#29949=CARTESIAN_POINT('Ctrl Pts',(368.380894663344,-13.5105587856809,-2.33904247799338));
#29950=CARTESIAN_POINT('Ctrl Pts',(368.452540406521,-13.5166687251836,-2.41419174502113));
#29951=CARTESIAN_POINT('Ctrl Pts',(368.527733339203,-13.5227786646863,-2.48614196861558));
#29952=CARTESIAN_POINT('Ctrl Pts',(368.606155516872,-13.5288886041889,-2.55454451230814));
#29953=CARTESIAN_POINT('Ctrl Pts',(368.684500999563,-13.5349925683196,-2.62288015997952));
#29954=CARTESIAN_POINT('Ctrl Pts',(368.766069127339,-13.5410965324503,-2.68767475020128));
#29955=CARTESIAN_POINT('Ctrl Pts',(368.850505007985,-13.547200496581,-2.74861631690664));
#29956=CARTESIAN_POINT('Ctrl Pts',(368.934885235177,-13.5533004374614,-2.80951771575182));
#29957=CARTESIAN_POINT('Ctrl Pts',(369.022129112173,-13.5594003783418,-2.86657089390966));
#29958=CARTESIAN_POINT('Ctrl Pts',(369.111849178056,-13.5655003192222,-2.91950453426009));
#29959=CARTESIAN_POINT('Ctrl Pts',(369.201539239108,-13.5715982201164,-2.97242047216103));
#29960=CARTESIAN_POINT('Ctrl Pts',(369.293703477122,-13.5776961210106,-3.02121939525926));
#29961=CARTESIAN_POINT('Ctrl Pts',(369.387926661105,-13.5837940219048,-3.06567408278523));
#29962=CARTESIAN_POINT('Ctrl Pts',(369.482142343477,-13.5898914373125,-3.1101252310358));
#29963=CARTESIAN_POINT('Ctrl Pts',(369.578416261294,-13.5959888527202,-3.15023265057975));
#29964=CARTESIAN_POINT('Ctrl Pts',(369.676310667713,-13.6020862681279,-3.18581613104176));
#29965=CARTESIAN_POINT('Ctrl Pts',(369.774222224157,-13.6081847517357,-3.22140584533847));
#29966=CARTESIAN_POINT('Ctrl Pts',(369.873754433892,-13.6142832353436,-3.25246990058782));
#29967=CARTESIAN_POINT('Ctrl Pts',(369.974452596192,-13.6203817189514,-3.27887736919951));
#29968=CARTESIAN_POINT('Ctrl Pts',(370.075251760938,-13.626486319471,-3.30531132507639));
#29969=CARTESIAN_POINT('Ctrl Pts',(370.177218801532,-13.6325909199905,-3.32707926086374));
#29970=CARTESIAN_POINT('Ctrl Pts',(370.27988705099,-13.63869552051,-3.34410100745093));
#29971=CARTESIAN_POINT('Ctrl Pts',(370.382612390891,-13.6448035155974,-3.36113221927254));
#29972=CARTESIAN_POINT('Ctrl Pts',(370.486039294524,-13.6509115106849,-3.37341193435571));
#29973=CARTESIAN_POINT('Ctrl Pts',(370.589696042567,-13.6570195057723,-3.38091189359485));
#29974=CARTESIAN_POINT('Ctrl Pts',(370.693506802752,-13.6631365760567,-3.38842299619708));
#29975=CARTESIAN_POINT('Ctrl Pts',(370.797547664726,-13.6692536463411,-3.39114014979097));
#29976=CARTESIAN_POINT('Ctrl Pts',(370.901346919323,-13.6753707166254,-3.38908721734893));
#29977=CARTESIAN_POINT('Ctrl Pts',(370.956452371767,-13.6786181766092,-3.38799734660279));
#29978=CARTESIAN_POINT('Ctrl Pts',(371.011489804652,-13.681865636593,-3.38556396081711));
#29979=CARTESIAN_POINT('Ctrl Pts',(371.066389505618,-13.6851130965768,-3.38179653596353));
#29980=CARTESIAN_POINT('Ctrl Pts',(371.169810991295,-13.6912307462231,-3.37469936296128));
#29981=CARTESIAN_POINT('Ctrl Pts',(371.27307006171,-13.6973483958694,-3.36284244566665));
#29982=CARTESIAN_POINT('Ctrl Pts',(371.375695958858,-13.7034660455157,-3.34623890498568));
#29983=CARTESIAN_POINT('Ctrl Pts',(371.478192616937,-13.70957599107,-3.3296562735119));
#29984=CARTESIAN_POINT('Ctrl Pts',(371.580057270855,-13.7156859366243,-3.30833897176935));
#29985=CARTESIAN_POINT('Ctrl Pts',(371.680822578416,-13.7217958821787,-3.28235202449816));
#29986=CARTESIAN_POINT('Ctrl Pts',(371.781489341391,-13.7278998524418,-3.25639049145967));
#29987=CARTESIAN_POINT('Ctrl Pts',(371.881058486689,-13.7340038227049,-3.22576850120469));
#29988=CARTESIAN_POINT('Ctrl Pts',(371.979072017051,-13.740107792968,-3.19060228905149));
#29989=CARTESIAN_POINT('Ctrl Pts',(372.077020946197,-13.7462077400733,-3.15545925512727));
#29990=CARTESIAN_POINT('Ctrl Pts',(372.173415900603,-13.7523076871786,-3.11577809933216));
#29991=CARTESIAN_POINT('Ctrl Pts',(372.267813985683,-13.7584076342839,-3.07172490642058));
#29992=CARTESIAN_POINT('Ctrl Pts',(372.362180502342,-13.764505541457,-3.02768644569074));
#29993=CARTESIAN_POINT('Ctrl Pts',(372.454551092437,-13.77060344863,-2.97927903395538));
#29994=CARTESIAN_POINT('Ctrl Pts',(372.544503521109,-13.7767013558031,-2.92671659780389));
#29995=CARTESIAN_POINT('Ctrl Pts',(372.634448788861,-13.7827987775349,-2.87415834603511));
#29996=CARTESIAN_POINT('Ctrl Pts',(372.721975911304,-13.7888961992666,-2.81744594242623));
#29997=CARTESIAN_POINT('Ctrl Pts',(372.80668868817,-13.7949936209984,-2.75683847041411));
#29998=CARTESIAN_POINT('Ctrl Pts',(372.891416306276,-13.8010921109668,-2.69622038028676));
#29999=CARTESIAN_POINT('Ctrl Pts',(372.973328253474,-13.8071906009353,-2.63170611310799));
#30000=CARTESIAN_POINT('Ctrl Pts',(373.052059383845,-13.8132890909038,-2.56359660747514));
#30001=CARTESIAN_POINT('Ctrl Pts',(373.130869483377,-13.8193936978,-2.49541878641881));
#30002=CARTESIAN_POINT('Ctrl Pts',(373.206492074138,-13.8254983046962,-2.423638805379));
#30003=CARTESIAN_POINT('Ctrl Pts',(373.278597102448,-13.8316029115924,-2.34859617948939));
#30004=CARTESIAN_POINT('Ctrl Pts',(373.350742226157,-13.8377109130736,-2.27351182469292));
#30005=CARTESIAN_POINT('Ctrl Pts',(373.419365611014,-13.8438189145549,-2.19516153052003));
#30006=CARTESIAN_POINT('Ctrl Pts',(373.48417715561,-13.8499269160361,-2.11391833807689));
#30007=CARTESIAN_POINT('Ctrl Pts',(373.549084996078,-13.8560439926803,-2.03255443590362));
#30008=CARTESIAN_POINT('Ctrl Pts',(373.610169436892,-13.8621610693244,-1.9482893958317));
#30009=CARTESIAN_POINT('Ctrl Pts',(373.667183367057,-13.8682781459686,-1.86152572988874));
#30010=CARTESIAN_POINT('Ctrl Pts',(373.697450585566,-13.8715255434887,-1.81546514735829));
#30011=CARTESIAN_POINT('Ctrl Pts',(373.726571390993,-13.8747729410087,-1.76870081986008));
#30012=CARTESIAN_POINT('Ctrl Pts',(373.754514171867,-13.8780203385288,-1.72129559433642));
#30013=CARTESIAN_POINT('Ctrl Pts',(373.80715409437,-13.8841379384398,-1.63199140485689));
#30014=CARTESIAN_POINT('Ctrl Pts',(373.855776908335,-13.8902555383508,-1.54012915831113));
#30015=CARTESIAN_POINT('Ctrl Pts',(373.900127182339,-13.8963731382619,-1.44610449830167));
#30016=CARTESIAN_POINT('Ctrl Pts',(373.944421603874,-13.9024830339801,-1.35219824814533));
#30017=CARTESIAN_POINT('Ctrl Pts',(373.984454004348,-13.9085929296984,-1.25613538091522));
#30018=CARTESIAN_POINT('Ctrl Pts',(374.020013688675,-13.9147028254167,-1.15833807952949));
#30019=CARTESIAN_POINT('Ctrl Pts',(374.055538596553,-13.9208067458153,-1.0606364213695));
#30020=CARTESIAN_POINT('Ctrl Pts',(374.086599343483,-13.9269106662139,-0.961204100197238));
#30021=CARTESIAN_POINT('Ctrl Pts',(374.113032752499,-13.9330145866125,-0.860484556382313));
#30022=CARTESIAN_POINT('Ctrl Pts',(374.139448739715,-13.9391144840234,-0.759831395067136));
#30023=CARTESIAN_POINT('Ctrl Pts',(374.161243347015,-13.9452143814342,-0.65789310846249));
#30024=CARTESIAN_POINT('Ctrl Pts',(374.17830304957,-13.951314278845,-0.555128876135667));
#30025=CARTESIAN_POINT('Ctrl Pts',(374.195357047372,-13.9574121364541,-0.452399008101695));
#30026=CARTESIAN_POINT('Ctrl Pts',(374.2076792185,-13.9635099940632,-0.348844162284679));
#30027=CARTESIAN_POINT('Ctrl Pts',(374.215207177643,-13.9696078516723,-0.244933539011872));
#30028=CARTESIAN_POINT('Ctrl Pts',(374.222734537736,-13.9757052240352,-0.141031184583188));
#30029=CARTESIAN_POINT('Ctrl Pts',(374.225468414252,-13.9818025963981,-0.0367735329093332));
#30030=CARTESIAN_POINT('Ctrl Pts',(374.223398387063,-13.987899968761,0.0673661462176254));
#30031=CARTESIAN_POINT('Ctrl Pts',(374.221327997124,-13.9939984096205,0.171524074663072));
#30032=CARTESIAN_POINT('Ctrl Pts',(374.214452039208,-14.0000968504799,0.275563564590752));
#30033=CARTESIAN_POINT('Ctrl Pts',(374.202812174589,-14.0061952913394,0.379013283980065));
#30034=CARTESIAN_POINT('Ctrl Pts',(374.191160633504,-14.0122998498157,0.48256677837719));
#30035=CARTESIAN_POINT('Ctrl Pts',(374.174735691732,-14.0184044082921,0.585528898027552));
#30036=CARTESIAN_POINT('Ctrl Pts',(374.153630671847,-14.0245089667684,0.687435433058516));
#30037=CARTESIAN_POINT('Ctrl Pts',(374.132513914873,-14.0306169201598,0.789398641152582));
#30038=CARTESIAN_POINT('Ctrl Pts',(374.106712000254,-14.0367248735511,0.890304683607939));
#30039=CARTESIAN_POINT('Ctrl Pts',(374.076368495392,-14.0428328269425,0.9897033374286));
#30040=CARTESIAN_POINT('Ctrl Pts',(374.045979901539,-14.0489498564594,1.08924969287799));
#30041=CARTESIAN_POINT('Ctrl Pts',(374.011036383171,-14.0550668859764,1.18728378652411));
#30042=CARTESIAN_POINT('Ctrl Pts',(373.971730126654,-14.0611839154933,1.28337418122268));
#30043=CARTESIAN_POINT('Ctrl Pts',(373.950860138787,-14.0644318038224,1.33439418539578));
#30044=CARTESIAN_POINT('Ctrl Pts',(373.928761015634,-14.0676796921516,1.38486661488869));
#30045=CARTESIAN_POINT('Ctrl Pts',(373.905466724033,-14.0709275804807,1.43472982677102));
#30046=CARTESIAN_POINT('Ctrl Pts',(373.861584129846,-14.0770460651272,1.52866387419326));
#30047=CARTESIAN_POINT('Ctrl Pts',(373.813318673387,-14.0831645497737,1.62073127437622));
#30048=CARTESIAN_POINT('Ctrl Pts',(373.760852254909,-14.0892830344203,1.71049743006276));
#30049=CARTESIAN_POINT('Ctrl Pts',(373.708467293901,-14.0953920197282,1.80012421805373));
#30050=CARTESIAN_POINT('Ctrl Pts',(373.651894565734,-14.1015010050362,1.88745650870011));
#30051=CARTESIAN_POINT('Ctrl Pts',(373.591362974889,-14.1076099903442,1.97208196067124));
#30052=CARTESIAN_POINT('Ctrl Pts',(373.530885246039,-14.1137135397775,2.05663211153655));
#30053=CARTESIAN_POINT('Ctrl Pts',(373.466455902736,-14.1198170892108,2.13847986766756));
#30054=CARTESIAN_POINT('Ctrl Pts',(373.398348300586,-14.1259206386441,2.21723993458057));
#30055=CARTESIAN_POINT('Ctrl Pts',(373.330283945048,-14.1320203124772,2.29594999083454));
#30056=CARTESIAN_POINT('Ctrl Pts',(373.258546251999,-14.1381199863104,2.3715759358255));
#30057=CARTESIAN_POINT('Ctrl Pts',(373.183449650411,-14.1442196601435,2.44376448577713));
#30058=CARTESIAN_POINT('Ctrl Pts',(373.108381597546,-14.1503170151246,2.51592559252999));
#30059=CARTESIAN_POINT('Ctrl Pts',(373.029957482597,-14.1564143701058,2.58465160994283));
#30060=CARTESIAN_POINT('Ctrl Pts',(372.948528866113,-14.162511725087,2.6496257953677));
#30061=CARTESIAN_POINT('Ctrl Pts',(372.867087713778,-14.1686100187496,2.71460998350082));
#30062=CARTESIAN_POINT('Ctrl Pts',(372.782641463345,-14.1747083124122,2.77584091462108));
#30063=CARTESIAN_POINT('Ctrl Pts',(372.695574683507,-14.1808066060748,2.83304219421901));
#30064=CARTESIAN_POINT('Ctrl Pts',(372.608500865398,-14.1869053927089,2.89024809783199));
#30065=CARTESIAN_POINT('Ctrl Pts',(372.518806455965,-14.1930041793431,2.94342347496669));
#30066=CARTESIAN_POINT('Ctrl Pts',(372.426903780437,-14.1991029659772,2.9923360651741));
#30067=CARTESIAN_POINT('Ctrl Pts',(372.334933726547,-14.2052062239312,3.04128451560261));
#30068=CARTESIAN_POINT('Ctrl Pts',(372.240752553547,-14.2113094818852,3.0859637473525));
#30069=CARTESIAN_POINT('Ctrl Pts',(372.144795581832,-14.2174127398392,3.12618828372879));
#30070=CARTESIAN_POINT('Ctrl Pts',(372.101091858123,-14.2201924763667,3.14450859951888));
#30071=CARTESIAN_POINT('Ctrl Pts',(372.057020036966,-14.2229722128942,3.16190551592873));
#30072=CARTESIAN_POINT('Ctrl Pts',(372.012622422842,-14.2257519494217,3.17836489467751));
#30073=CARTESIAN_POINT('Ctrl Pts',(372.012622418493,-13.8856567889318,3.1783648962896));
#30074=CARTESIAN_POINT('Ctrl Pts',(372.070513041571,-13.8818627345421,3.15690329962443));
#30075=CARTESIAN_POINT('Ctrl Pts',(372.12780751053,-13.8780066111693,3.13386370550035));
#30076=CARTESIAN_POINT('Ctrl Pts',(372.368620390333,-13.8614490521448,3.02929673523553));
#30077=CARTESIAN_POINT('Ctrl Pts',(372.54532893171,-13.8484466958673,2.93311549986729));
#30078=CARTESIAN_POINT('Ctrl Pts',(372.834081643333,-13.8264705281444,2.74092768553833));
#30079=CARTESIAN_POINT('Ctrl Pts',(372.950327596326,-13.8173803299904,2.6522161874872));
#30080=CARTESIAN_POINT('Ctrl Pts',(373.11669844169,-13.8040520384073,2.50732881780625));
#30081=CARTESIAN_POINT('Ctrl Pts',(373.171272194672,-13.799620172036,2.45654322432826));
#30082=CARTESIAN_POINT('Ctrl Pts',(373.275553136719,-13.7910170791153,2.35287755753538));
#30083=CARTESIAN_POINT('Ctrl Pts',(373.325324664236,-13.7868442728773,2.30011927374733));
#30084=CARTESIAN_POINT('Ctrl Pts',(373.456220449226,-13.7756453699622,2.15213161379069));
#30085=CARTESIAN_POINT('Ctrl Pts',(373.533829785163,-13.7687546485385,2.05394330388658));
#30086=CARTESIAN_POINT('Ctrl Pts',(373.725399276435,-13.7507164409805,1.7819015986162));
#30087=CARTESIAN_POINT('Ctrl Pts',(373.829099798953,-13.7398195621247,1.60150000471844));
#30088=CARTESIAN_POINT('Ctrl Pts',(373.945786505632,-13.7246202110521,1.34699668922024));
#30089=CARTESIAN_POINT('Ctrl Pts',(373.973819360757,-13.7206486476821,1.28029938012707));
#30090=CARTESIAN_POINT('Ctrl Pts',(374.019977543795,-13.7134144162638,1.15982369413772));
#30091=CARTESIAN_POINT('Ctrl Pts',(374.03892686138,-13.7101852452605,1.10639007075722));
#30092=CARTESIAN_POINT('Ctrl Pts',(374.068990447567,-13.7045492733195,1.01435184059395));
#30093=CARTESIAN_POINT('Ctrl Pts',(374.080773977305,-13.7021761506524,0.97598087231898));
#30094=CARTESIAN_POINT('Ctrl Pts',(374.108841876622,-13.6960853273582,0.878443174856708));
#30095=CARTESIAN_POINT('Ctrl Pts',(374.124205002062,-13.6923253328236,0.819030871264247));
#30096=CARTESIAN_POINT('Ctrl Pts',(374.194609012155,-13.6727906785065,0.512686148507764));
#30097=CARTESIAN_POINT('Ctrl Pts',(374.223493580583,-13.656299272527,0.260568479008471));
#30098=CARTESIAN_POINT('Ctrl Pts',(374.224365259854,-13.6316788807919,-0.129190701480439));
#30099=CARTESIAN_POINT('Ctrl Pts',(374.216393176629,-13.6231952762068,-0.265866496446257));
#30100=CARTESIAN_POINT('Ctrl Pts',(374.191449947153,-13.6104994103048,-0.474867275195763));
#30101=CARTESIAN_POINT('Ctrl Pts',(374.180333843797,-13.6061240023498,-0.54773445222052));
#30102=CARTESIAN_POINT('Ctrl Pts',(374.153455770233,-13.597540289508,-0.692162265783858));
#30103=CARTESIAN_POINT('Ctrl Pts',(374.137731965901,-13.5933333741653,-0.763689358469013));
#30104=CARTESIAN_POINT('Ctrl Pts',(374.08722267471,-13.5817242720805,-0.962504994023995));
#30105=CARTESIAN_POINT('Ctrl Pts',(374.047305656414,-13.5744784172473,-1.0883563663356));
#30106=CARTESIAN_POINT('Ctrl Pts',(373.928903596409,-13.5565669101734,-1.39774104190696));
#30107=CARTESIAN_POINT('Ctrl Pts',(373.841375594435,-13.5460939647492,-1.57725731991146));
#30108=CARTESIAN_POINT('Ctrl Pts',(373.70184924996,-13.5313944454596,-1.80907255757174));
#30109=CARTESIAN_POINT('Ctrl Pts',(373.663200171553,-13.5274796950031,-1.86893115289559));
#30110=CARTESIAN_POINT('Ctrl Pts',(373.590789661747,-13.5203344156567,-1.97368099554282));
#30111=CARTESIAN_POINT('Ctrl Pts',(373.557743871837,-13.5171361034214,-2.01903528007202));
#30112=CARTESIAN_POINT('Ctrl Pts',(373.499134539538,-13.5115293513256,-2.0954166428895));
#30113=CARTESIAN_POINT('Ctrl Pts',(373.474118100249,-13.5091531645693,-2.12684580870211));
#30114=CARTESIAN_POINT('Ctrl Pts',(373.409024653371,-13.5030139021602,-2.20570737566982));
#30115=CARTESIAN_POINT('Ctrl Pts',(373.368194640828,-13.4992068230788,-2.25249363136843));
#30116=CARTESIAN_POINT('Ctrl Pts',(373.155335085181,-13.4796825656924,-2.48329044005629));
#30117=CARTESIAN_POINT('Ctrl Pts',(372.964460462119,-13.4632649864131,-2.64883923427552));
#30118=CARTESIAN_POINT('Ctrl Pts',(372.644531091319,-13.438728230231,-2.86917823654959));
#30119=CARTESIAN_POINT('Ctrl Pts',(372.527470123213,-13.4302579685121,-2.93977854851025));
#30120=CARTESIAN_POINT('Ctrl Pts',(372.341191696741,-13.4175761129384,-3.03729537254865));
#30121=CARTESIAN_POINT('Ctrl Pts',(372.274826728343,-13.4132020209173,-3.06932685687098));
#30122=CARTESIAN_POINT('Ctrl Pts',(372.140513486671,-13.404618654692,-3.12883696725013));
#30123=CARTESIAN_POINT('Ctrl Pts',(372.072613462428,-13.4004108427868,-3.15632585566594));
#30124=CARTESIAN_POINT('Ctrl Pts',(371.879889402131,-13.3887907790295,-3.22717123512479));
#30125=CARTESIAN_POINT('Ctrl Pts',(371.753342181182,-13.3815354367505,-3.2654636585629));
#30126=CARTESIAN_POINT('Ctrl Pts',(371.399454321044,-13.3618595177126,-3.35033765181226));
#30127=CARTESIAN_POINT('Ctrl Pts',(371.169099941822,-13.3497538004549,-3.38113161314876));
#30128=CARTESIAN_POINT('Ctrl Pts',(370.859832731438,-13.3327293816378,-3.39054265895115));
#30129=CARTESIAN_POINT('Ctrl Pts',(370.782191860392,-13.328386616616,-3.39023770795044));
#30130=CARTESIAN_POINT('Ctrl Pts',(370.662992540345,-13.3215250644156,-3.38567414188377));
#30131=CARTESIAN_POINT('Ctrl Pts',(370.621383690552,-13.3190929483916,-3.38331209011377));
#30132=CARTESIAN_POINT('Ctrl Pts',(370.531276565446,-13.3137290006523,-3.37652805783786));
#30133=CARTESIAN_POINT('Ctrl Pts',(370.482811430765,-13.3107854808054,-3.37182716544576));
#30134=CARTESIAN_POINT('Ctrl Pts',(370.295843737569,-13.299245024251,-3.34961763941438));
#30135=CARTESIAN_POINT('Ctrl Pts',(370.158379788995,-13.2903709614666,-3.32460442276465));
#30136=CARTESIAN_POINT('Ctrl Pts',(369.837840479298,-13.2692534386837,-3.24557413017229));
#30137=CARTESIAN_POINT('Ctrl Pts',(369.656981361309,-13.2570144628041,-3.18443207195036));
#30138=CARTESIAN_POINT('Ctrl Pts',(369.384529360016,-13.2385061653722,-3.06592003053975));
#30139=CARTESIAN_POINT('Ctrl Pts',(369.288897681958,-13.231989093711,-3.01884618102679));
#30140=CARTESIAN_POINT('Ctrl Pts',(369.133884765843,-13.2213951101897,-2.93324192970972));
#30141=CARTESIAN_POINT('Ctrl Pts',(369.073211804589,-13.2172396716112,-2.89722064228256));
#30142=CARTESIAN_POINT('Ctrl Pts',(368.947499368076,-13.208594598721,-2.8171760768655));
#30143=CARTESIAN_POINT('Ctrl Pts',(368.88277589865,-13.2041228091436,-2.77273337615041));
#30144=CARTESIAN_POINT('Ctrl Pts',(368.622384966883,-13.1859616225786,-2.58029550703354));
#30145=CARTESIAN_POINT('Ctrl Pts',(368.44152685087,-13.1729947798156,-2.41353105079744));
#30146=CARTESIAN_POINT('Ctrl Pts',(368.210693099577,-13.1541956964911,-2.14899688721272));
#30147=CARTESIAN_POINT('Ctrl Pts',(368.144916777435,-13.1485004376562,-2.0660866797941));
#30148=CARTESIAN_POINT('Ctrl Pts',(368.040914673143,-13.1386658089053,-1.92159443589303));
#30149=CARTESIAN_POINT('Ctrl Pts',(368.000590611035,-13.1346073295086,-1.86161623255362));
#30150=CARTESIAN_POINT('Ctrl Pts',(367.940417797524,-13.1280753528127,-1.76562510083742));
#30151=CARTESIAN_POINT('Ctrl Pts',(367.919254974156,-13.1256744277895,-1.73046174111507));
#30152=CARTESIAN_POINT('Ctrl Pts',(367.873477350455,-13.1202286800069,-1.65117534676109));
#30153=CARTESIAN_POINT('Ctrl Pts',(367.849203142064,-13.1171676264391,-1.60687462762368));
#30154=CARTESIAN_POINT('Ctrl Pts',(367.73574006706,-13.1020384936368,-1.38835355838938));
#30155=CARTESIAN_POINT('Ctrl Pts',(367.660768982404,-13.0894265950276,-1.20718219184014));
#30156=CARTESIAN_POINT('Ctrl Pts',(367.542651834828,-13.0643260347919,-0.833067192698608));
#30157=CARTESIAN_POINT('Ctrl Pts',(367.499873045884,-13.0518903585881,-0.640750715244693));
#30158=CARTESIAN_POINT('Ctrl Pts',(367.463644463792,-13.0351363705873,-0.367664290187277));
#30159=CARTESIAN_POINT('Ctrl Pts',(367.456007192223,-13.0304201956665,-0.289196621600946));
#30160=CARTESIAN_POINT('Ctrl Pts',(367.446737283081,-13.0216402382619,-0.140229022906423));
#30161=CARTESIAN_POINT('Ctrl Pts',(367.444554678254,-13.0175624591175,-0.0698064440528915));
#30162=CARTESIAN_POINT('Ctrl Pts',(367.444587737125,-13.0075274155424,0.106152147204749));
#30163=CARTESIAN_POINT('Ctrl Pts',(367.449534158312,-13.0016522954613,0.211614329611914));
#30164=CARTESIAN_POINT('Ctrl Pts',(367.472616562001,-12.9881242758317,0.457607467445845));
#30165=CARTESIAN_POINT('Ctrl Pts',(367.494654575996,-12.9805656122501,0.597571515404709));
#30166=CARTESIAN_POINT('Ctrl Pts',(367.565230946193,-12.9631956814482,0.914979184482697));
#30167=CARTESIAN_POINT('Ctrl Pts',(367.619575199875,-12.9534138893466,1.09065721272535));
#30168=CARTESIAN_POINT('Ctrl Pts',(367.707038470983,-12.940143029684,1.3088866854747));
#30169=CARTESIAN_POINT('Ctrl Pts',(367.727296864628,-12.9371893487096,1.35627454739195));
#30170=CARTESIAN_POINT('Ctrl Pts',(367.765508652112,-12.9317909186456,1.44030499338984));
#30171=CARTESIAN_POINT('Ctrl Pts',(367.783057472938,-12.9293669007204,1.47711809993816));
#30172=CARTESIAN_POINT('Ctrl Pts',(367.832449212682,-12.9226979167539,1.57609231510798));
#30173=CARTESIAN_POINT('Ctrl Pts',(367.86555490037,-12.918390653364,1.63759809453041));
#30174=CARTESIAN_POINT('Ctrl Pts',(367.950627351603,-12.9077682565904,1.78458238135337));
#30175=CARTESIAN_POINT('Ctrl Pts',(368.004524182653,-12.9013955768554,1.86886898487573));
#30176=CARTESIAN_POINT('Ctrl Pts',(368.212063998336,-12.8783199440914,2.16382400185837));
#30177=CARTESIAN_POINT('Ctrl Pts',(368.386176483354,-12.8616300671005,2.35902356048105));
#30178=CARTESIAN_POINT('Ctrl Pts',(368.638456329798,-12.8411462389077,2.58350927174964));
#30179=CARTESIAN_POINT('Ctrl Pts',(368.69767913548,-12.8365520910356,2.63269906327869));
#30180=CARTESIAN_POINT('Ctrl Pts',(368.814743362971,-12.8278597849995,2.72337658936432));
#30181=CARTESIAN_POINT('Ctrl Pts',(368.872316622805,-12.8237526035339,2.765142561834));
#30182=CARTESIAN_POINT('Ctrl Pts',(369.023813935776,-12.8133360112139,2.86792886438516));
#30183=CARTESIAN_POINT('Ctrl Pts',(369.119525748788,-12.8071253121815,2.92616329049916));
#30184=CARTESIAN_POINT('Ctrl Pts',(369.357145420782,-12.7923784464163,3.05506851396676));
#30185=CARTESIAN_POINT('Ctrl Pts',(369.501463512324,-12.7839682936873,3.12073440765705));
#30186=CARTESIAN_POINT('Ctrl Pts',(369.793131937548,-12.767316107652,3.22950831598888));
#30187=CARTESIAN_POINT('Ctrl Pts',(369.939860307399,-12.7590940794592,3.27318344130942));
#30188=CARTESIAN_POINT('Ctrl Pts',(370.140121829912,-12.7475200622096,3.31831898607792));
#30189=CARTESIAN_POINT('Ctrl Pts',(370.191479870665,-12.7445209553623,3.3286495304485));
#30190=CARTESIAN_POINT('Ctrl Pts',(370.282667467491,-12.7391097777666,3.34480274785764));
#30191=CARTESIAN_POINT('Ctrl Pts',(370.322397974328,-12.7367213499059,3.35111340512486));
#30192=CARTESIAN_POINT('Ctrl Pts',(370.429153553032,-12.7302289453937,3.36612749807673));
#30193=CARTESIAN_POINT('Ctrl Pts',(370.496339512593,-12.7260674455509,3.37353551269637));
#30194=CARTESIAN_POINT('Ctrl Pts',(370.658229348029,-12.7159252226104,3.38650137505278));
#30195=CARTESIAN_POINT('Ctrl Pts',(370.753033665052,-12.7098928150693,3.39010177182418));
#30196=CARTESIAN_POINT('Ctrl Pts',(371.107412093876,-12.6872371642439,3.38868606231617));
#30197=CARTESIAN_POINT('Ctrl Pts',(371.366028351237,-12.670575376013,3.35784066164272));
#30198=CARTESIAN_POINT('Ctrl Pts',(371.696309200672,-12.6498999753054,3.27929183180326));
#30199=CARTESIAN_POINT('Ctrl Pts',(371.773337089374,-12.6451144086172,3.25807127194599));
#30200=CARTESIAN_POINT('Ctrl Pts',(371.904370087706,-12.6370269314704,3.21693874071087));
#30201=CARTESIAN_POINT('Ctrl Pts',(371.958745574722,-12.6336868080168,3.19833847805212));
#30202=CARTESIAN_POINT('Ctrl Pts',(372.012622420937,-12.6303878084336,3.17836489538373));
#30203=CARTESIAN_POINT('Origin',(370.834317853224,-11.,0.));
#30204=CARTESIAN_POINT('',(372.012622422842,-11.3828409270354,3.1783648946775));
#30205=CARTESIAN_POINT('',(372.012622422842,-11.7257572018857,3.1783648946775));
#30206=CARTESIAN_POINT('',(372.012622422842,-11.,3.17836489467752));
#30207=CARTESIAN_POINT('',(373.407552280239,-11.,-2.20655152809226));
#30208=CARTESIAN_POINT('Ctrl Pts',(372.012622422842,-11.3828409270354,3.17836489467751));
#30209=CARTESIAN_POINT('Ctrl Pts',(372.109345119701,-11.376754041059,3.1425072132997));
#30210=CARTESIAN_POINT('Ctrl Pts',(372.204587584932,-11.3706671550826,3.10217174787753));
#30211=CARTESIAN_POINT('Ctrl Pts',(372.297905397225,-11.3645802691062,3.05750168659702));
#30212=CARTESIAN_POINT('Ctrl Pts',(372.391108113364,-11.3585008905623,3.01288672039581));
#30213=CARTESIAN_POINT('Ctrl Pts',(372.482390510664,-11.3524215120183,2.96394797056057));
#30214=CARTESIAN_POINT('Ctrl Pts',(372.571325986317,-11.3463421334743,2.91087749794947));
#30215=CARTESIAN_POINT('Ctrl Pts',(372.660174141899,-11.3402687238843,2.85785913185024));
#30216=CARTESIAN_POINT('Ctrl Pts',(372.746679591279,-11.3341953142943,2.800717330631));
#30217=CARTESIAN_POINT('Ctrl Pts',(372.830439152938,-11.3281219047043,2.73969064299737));
#30218=CARTESIAN_POINT('Ctrl Pts',(372.914152482963,-11.3220518473722,2.67869763944042));
#30219=CARTESIAN_POINT('Ctrl Pts',(372.995122590053,-11.3159817900401,2.61382426280361));
#30220=CARTESIAN_POINT('Ctrl Pts',(373.072974790305,-11.309911732708,2.54535266329834));
#30221=CARTESIAN_POINT('Ctrl Pts',(373.150804777861,-11.3038434072773,2.47690060002757));
#30222=CARTESIAN_POINT('Ctrl Pts',(373.225518303846,-11.2977750818467,2.40485263805723));
#30223=CARTESIAN_POINT('Ctrl Pts',(373.296774077596,-11.291706756416,2.32953094110233));
#30224=CARTESIAN_POINT('Ctrl Pts',(373.368028221444,-11.285638569792,2.2542109670526));
#30225=CARTESIAN_POINT('Ctrl Pts',(373.435824475127,-11.279570383168,2.17561771971967));
#30226=CARTESIAN_POINT('Ctrl Pts',(373.499859378019,-11.2735021965439,2.09410922401186));
#30227=CARTESIAN_POINT('Ctrl Pts',(373.563909621778,-11.2674325561622,2.01258120128319));
#30228=CARTESIAN_POINT('Ctrl Pts',(373.624196458741,-11.2613629157804,1.92813688067976));
#30229=CARTESIAN_POINT('Ctrl Pts',(373.680458166391,-11.2552932753986,1.84116549507775));
#30230=CARTESIAN_POINT('Ctrl Pts',(373.736781306444,-11.2492170075501,1.75409914504173));
#30231=CARTESIAN_POINT('Ctrl Pts',(373.78907031061,-11.2431407397016,1.66450058384919));
#30232=CARTESIAN_POINT('Ctrl Pts',(373.837108147384,-11.2370644718531,1.57278590780703));
#30233=CARTESIAN_POINT('Ctrl Pts',(373.885176022134,-11.2309844045249,1.48101388273754));
#30234=CARTESIAN_POINT('Ctrl Pts',(373.928987255592,-11.2249043371967,1.38712349765055));
#30235=CARTESIAN_POINT('Ctrl Pts',(373.968372746856,-11.2188242698685,1.29155138736463));
#30236=CARTESIAN_POINT('Ctrl Pts',(374.007818757728,-11.21273485993,1.19583242130786));
#30237=CARTESIAN_POINT('Ctrl Pts',(374.042825306534,-11.2066454499916,1.09842697564112));
#30238=CARTESIAN_POINT('Ctrl Pts',(374.073272980134,-11.2005560400532,0.999787351572205));
#30239=CARTESIAN_POINT('Ctrl Pts',(374.086021238196,-11.1980064406861,0.958487533422621));
#30240=CARTESIAN_POINT('Ctrl Pts',(374.097970920648,-11.195456841319,0.916971485992314));
#30241=CARTESIAN_POINT('Ctrl Pts',(374.109115940059,-11.1929072419519,0.875272844868533));
#30242=CARTESIAN_POINT('Ctrl Pts',(374.136432135908,-11.1866582303457,0.773070398589751));
#30243=CARTESIAN_POINT('Ctrl Pts',(374.15899710704,-11.1804092187395,0.66944827717487));
#30244=CARTESIAN_POINT('Ctrl Pts',(374.176670633579,-11.1741602071332,0.564874281725621));
#30245=CARTESIAN_POINT('Ctrl Pts',(374.194319493875,-11.1679199170256,0.460446236069472));
#30246=CARTESIAN_POINT('Ctrl Pts',(374.207090429813,-11.1616796269179,0.355069354057219));
#30247=CARTESIAN_POINT('Ctrl Pts',(374.214893580216,-11.1554393368102,0.249224430124238));
#30248=CARTESIAN_POINT('Ctrl Pts',(374.222992272363,-11.1489626977765,0.139370664667613));
#30249=CARTESIAN_POINT('Ctrl Pts',(374.225739291032,-11.1424860587427,0.0290131187424228));
#30250=CARTESIAN_POINT('Ctrl Pts',(374.223092751951,-11.1360094197089,-0.0813003582986123));
#30251=CARTESIAN_POINT('Ctrl Pts',(374.220548538229,-11.1297831924027,-0.18734869284634));
#30252=CARTESIAN_POINT('Ctrl Pts',(374.213020091719,-11.1235569650965,-0.293355855965398));
#30253=CARTESIAN_POINT('Ctrl Pts',(374.200523137763,-11.1173307377903,-0.398832101063093));
#30254=CARTESIAN_POINT('Ctrl Pts',(374.188033748519,-11.1111082793712,-0.504244498819675));
#30255=CARTESIAN_POINT('Ctrl Pts',(374.170581884868,-11.104885820952,-0.609126219935277));
#30256=CARTESIAN_POINT('Ctrl Pts',(374.148235192962,-11.0986633625329,-0.712991534229913));
#30257=CARTESIAN_POINT('Ctrl Pts',(374.125897319379,-11.0924433595844,-0.816815861793191));
#30258=CARTESIAN_POINT('Ctrl Pts',(374.098668547604,-11.086223356636,-0.919624188569452));
#30259=CARTESIAN_POINT('Ctrl Pts',(374.066667714442,-11.0800033536875,-1.02094046701289));
#30260=CARTESIAN_POINT('Ctrl Pts',(374.034672769757,-11.0737844952825,-1.12223810223613));
#30261=CARTESIAN_POINT('Ctrl Pts',(373.997907634394,-11.0675656368775,-1.22204385312564));
#30262=CARTESIAN_POINT('Ctrl Pts',(373.956540975599,-11.0613467784725,-1.31989690378075));
#30263=CARTESIAN_POINT('Ctrl Pts',(373.915161472763,-11.0551259891582,-1.41778033708062));
#30264=CARTESIAN_POINT('Ctrl Pts',(373.869177746436,-11.0489051998439,-1.51370948746967));
#30265=CARTESIAN_POINT('Ctrl Pts',(373.818806512561,-11.0426844105296,-1.60724376022663));
#30266=CARTESIAN_POINT('Ctrl Pts',(373.768426585783,-11.0364625476517,-1.70079417482431));
#30267=CARTESIAN_POINT('Ctrl Pts',(373.713657840655,-11.0302406847738,-1.79194853828177));
#30268=CARTESIAN_POINT('Ctrl Pts',(373.654762289082,-11.0240188218959,-1.88029206421186));
#30269=CARTESIAN_POINT('Ctrl Pts',(373.595824822343,-11.0177925310024,-1.96869846303269));
#30270=CARTESIAN_POINT('Ctrl Pts',(373.532754914756,-11.011566240109,-2.05428970018529));
#30271=CARTESIAN_POINT('Ctrl Pts',(373.465857042497,-11.0053399492156,-2.13668120172826));
#30272=CARTESIAN_POINT('Ctrl Pts',(373.446732160252,-11.0035599661437,-2.16023543016395));
#30273=CARTESIAN_POINT('Ctrl Pts',(373.427294673612,-11.0017799830719,-2.18352836019791));
#30274=CARTESIAN_POINT('Ctrl Pts',(373.407552280239,-11.,-2.2065515280921));
#30275=CARTESIAN_POINT('',(368.26051712127,-11.0000050991267,-2.20589094351711));
#30276=CARTESIAN_POINT('Origin',(370.834317853224,-11.,0.));
#30277=CARTESIAN_POINT('Ctrl Pts',(368.26051712127,-11.0000050991267,-2.20589094351711));
#30278=CARTESIAN_POINT('Ctrl Pts',(368.327238606422,-11.0060529733972,-2.28374057965987));
#30279=CARTESIAN_POINT('Ctrl Pts',(368.397609433174,-11.0121008476677,-2.35869323798605));
#30280=CARTESIAN_POINT('Ctrl Pts',(368.471345744128,-11.0181487219382,-2.43038430585211));
#30281=CARTESIAN_POINT('Ctrl Pts',(368.544992275328,-11.0241892324464,-2.50198808420878));
#30282=CARTESIAN_POINT('Ctrl Pts',(368.621995836498,-11.0302297429547,-2.57033786311652));
#30283=CARTESIAN_POINT('Ctrl Pts',(368.702032769653,-11.0362702534629,-2.63510253783068));
#30284=CARTESIAN_POINT('Ctrl Pts',(368.781992799466,-11.0423049599576,-2.69980498352423));
#30285=CARTESIAN_POINT('Ctrl Pts',(368.864980068054,-11.0483396664523,-2.76092890201313));
#30286=CARTESIAN_POINT('Ctrl Pts',(368.950635343321,-11.0543743729469,-2.81818119793333));
#30287=CARTESIAN_POINT('Ctrl Pts',(369.036246162658,-11.0604059473697,-2.87540377934964));
#30288=CARTESIAN_POINT('Ctrl Pts',(369.124521876229,-11.0664375217924,-2.928758488164));
#30289=CARTESIAN_POINT('Ctrl Pts',(369.21507220216,-11.0724690962151,-2.97799405372326));
#30290=CARTESIAN_POINT('Ctrl Pts',(369.305600031744,-11.0784991721518,-3.02721738718517));
#30291=CARTESIAN_POINT('Ctrl Pts',(369.398400967749,-11.0845292480886,-3.07232340306702));
#30292=CARTESIAN_POINT('Ctrl Pts',(369.493058817224,-11.0905593240253,-3.11310604715739));
#30293=CARTESIAN_POINT('Ctrl Pts',(369.587718761295,-11.096589533396,-3.15388959368942));
#30294=CARTESIAN_POINT('Ctrl Pts',(369.684235299469,-11.1026197427668,-3.19034940715939));
#30295=CARTESIAN_POINT('Ctrl Pts',(369.782171840681,-11.1086499521375,-3.22232739348286));
#30296=CARTESIAN_POINT('Ctrl Pts',(369.880194401973,-11.1146854579899,-3.25433346686037));
#30297=CARTESIAN_POINT('Ctrl Pts',(369.979639042066,-11.1207209638422,-3.28184971538478));
#30298=CARTESIAN_POINT('Ctrl Pts',(370.080053780211,-11.1267564696946,-3.30476788453618));
#30299=CARTESIAN_POINT('Ctrl Pts',(370.180513544078,-11.1327946818529,-3.32769633013833));
#30300=CARTESIAN_POINT('Ctrl Pts',(370.281943843126,-11.1388328940113,-3.34602251246441));
#30301=CARTESIAN_POINT('Ctrl Pts',(370.383884254303,-11.1448711061696,-3.35968966356459));
#30302=CARTESIAN_POINT('Ctrl Pts',(370.485979959136,-11.1509185168003,-3.37337763488563));
#30303=CARTESIAN_POINT('Ctrl Pts',(370.588586893703,-11.1569659274309,-3.38239235982936));
#30304=CARTESIAN_POINT('Ctrl Pts',(370.691241218024,-11.1630133380615,-3.38672912098973));
#30305=CARTESIAN_POINT('Ctrl Pts',(370.772186774208,-11.1677818757749,-3.39014876791141));
#30306=CARTESIAN_POINT('Ctrl Pts',(370.853161697947,-11.1725504134883,-3.39066082917184));
#30307=CARTESIAN_POINT('Ctrl Pts',(370.933940689546,-11.1773189512018,-3.38828575432815));
#30308=CARTESIAN_POINT('Ctrl Pts',(371.037700383489,-11.1834440835401,-3.38523499776391));
#30309=CARTESIAN_POINT('Ctrl Pts',(371.14147946567,-11.1895692158784,-3.37740907499611));
#30310=CARTESIAN_POINT('Ctrl Pts',(371.244805940947,-11.1956943482167,-3.36480379700469));
#30311=CARTESIAN_POINT('Ctrl Pts',(371.34800445609,-11.2018118951539,-3.3522141294661));
#30312=CARTESIAN_POINT('Ctrl Pts',(371.450751061336,-11.2079294420911,-3.33485692743649));
#30313=CARTESIAN_POINT('Ctrl Pts',(371.552575288547,-11.2140469890283,-3.31277999859691));
#30314=CARTESIAN_POINT('Ctrl Pts',(371.654301838623,-11.2201586675737,-3.29072424753808));
#30315=CARTESIAN_POINT('Ctrl Pts',(371.755107358307,-11.2262703461192,-3.26395786434406));
#30316=CARTESIAN_POINT('Ctrl Pts',(371.854528840641,-11.2323820246646,-3.23258017745184));
#30317=CARTESIAN_POINT('Ctrl Pts',(371.953886936492,-11.2384898066899,-3.20122249550376));
#30318=CARTESIAN_POINT('Ctrl Pts',(372.051862346872,-11.2445975887152,-3.16525948434695));
#30319=CARTESIAN_POINT('Ctrl Pts',(372.148005306803,-11.2507053707405,-3.12484084983702));
#30320=CARTESIAN_POINT('Ctrl Pts',(372.244117328946,-11.2568111873462,-3.08443522161612));
#30321=CARTESIAN_POINT('Ctrl Pts',(372.338397682649,-11.2629170039519,-3.03957698459175));
#30322=CARTESIAN_POINT('Ctrl Pts',(372.43041546605,-11.2690228205576,-2.99046442427135));
#30323=CARTESIAN_POINT('Ctrl Pts',(372.522426902253,-11.2751282159966,-2.94135525163432));
#30324=CARTESIAN_POINT('Ctrl Pts',(372.612175704924,-11.2812336114356,-2.88799253923605));
#30325=CARTESIAN_POINT('Ctrl Pts',(372.699255291481,-11.2873390068746,-2.83062067643958));
#30326=CARTESIAN_POINT('Ctrl Pts',(372.78635088544,-11.2934455246377,-2.77323826726252));
#30327=CARTESIAN_POINT('Ctrl Pts',(372.870775934383,-11.2995520424008,-2.71184547624207));
#30328=CARTESIAN_POINT('Ctrl Pts',(372.952153301272,-11.3056585601639,-2.64672969482942));
#30329=CARTESIAN_POINT('Ctrl Pts',(373.033612645684,-11.3117712294801,-2.58154831740837));
#30330=CARTESIAN_POINT('Ctrl Pts',(373.112017846769,-11.3178838987964,-2.51263672652615));
#30331=CARTESIAN_POINT('Ctrl Pts',(373.187025360339,-11.3239965681127,-2.44032220177244));
#30332=CARTESIAN_POINT('Ctrl Pts',(373.262074892831,-11.3301126617228,-2.36796716669925));
#30333=CARTESIAN_POINT('Ctrl Pts',(373.333722654894,-11.336228755333,-2.29220570779313));
#30334=CARTESIAN_POINT('Ctrl Pts',(373.401663732762,-11.3423448489432,-2.21340014396834));
#30335=CARTESIAN_POINT('Ctrl Pts',(373.469705307953,-11.3484699893783,-2.13447801225122));
#30336=CARTESIAN_POINT('Ctrl Pts',(373.534028988151,-11.3545951298134,-2.05250311663614));
#30337=CARTESIAN_POINT('Ctrl Pts',(373.594371677701,-11.3607202702485,-1.96786888498483));
#30338=CARTESIAN_POINT('Ctrl Pts',(373.625587993518,-11.3638889112169,-1.92408613476411));
#30339=CARTESIAN_POINT('Ctrl Pts',(373.655739655371,-11.3670575521853,-1.87959214961196));
#30340=CARTESIAN_POINT('Ctrl Pts',(373.684795056208,-11.3702261931537,-1.83444399690095));
#30341=CARTESIAN_POINT('Ctrl Pts',(373.740856860613,-11.3763400213948,-1.74733155537407));
#30342=CARTESIAN_POINT('Ctrl Pts',(373.79301145112,-11.3824538496358,-1.65750742219757));
#30343=CARTESIAN_POINT('Ctrl Pts',(373.84098795833,-11.3885676778769,-1.56535617083158));
#30344=CARTESIAN_POINT('Ctrl Pts',(373.888903605762,-11.3946737505257,-1.4733218163604));
#30345=CARTESIAN_POINT('Ctrl Pts',(373.932651513083,-11.4007798231745,-1.37896658795512));
#30346=CARTESIAN_POINT('Ctrl Pts',(373.972004434163,-11.4068858958233,-1.28270338827569));
#30347=CARTESIAN_POINT('Ctrl Pts',(374.011318551552,-11.4129859476188,-1.1865351082987));
#30348=CARTESIAN_POINT('Ctrl Pts',(374.046246141194,-11.4190859994143,-1.08846299077901));
#30349=CARTESIAN_POINT('Ctrl Pts',(374.07660657782,-11.4251860512099,-0.988923095522964));
#30350=CARTESIAN_POINT('Ctrl Pts',(374.106946735835,-11.4312820286051,-0.88944968583013));
#30351=CARTESIAN_POINT('Ctrl Pts',(374.13272568395,-11.4373780060003,-0.788510854248488));
#30352=CARTESIAN_POINT('Ctrl Pts',(374.153811776626,-11.4434739833955,-0.686560379718457));
#30353=CARTESIAN_POINT('Ctrl Pts',(374.174890710039,-11.4495678910519,-0.584644519958852));
#30354=CARTESIAN_POINT('Ctrl Pts',(374.191279869243,-11.4556617987083,-0.481718116460937));
#30355=CARTESIAN_POINT('Ctrl Pts',(374.202898305428,-11.4617557063647,-0.378247008616722));
#30356=CARTESIAN_POINT('Ctrl Pts',(374.214515769122,-11.4678491039458,-0.274784561562532));
#30357=CARTESIAN_POINT('Ctrl Pts',(374.221363256811,-11.4739425015269,-0.170777923839477));
#30358=CARTESIAN_POINT('Ctrl Pts',(374.223411581066,-11.480035899108,-0.0666990734491657));
#30359=CARTESIAN_POINT('Ctrl Pts',(374.225460257866,-11.4861303454451,0.0373976903179456));
#30360=CARTESIAN_POINT('Ctrl Pts',(374.222708121683,-11.4922247917823,0.141566265914222));
#30361=CARTESIAN_POINT('Ctrl Pts',(374.215178102404,-11.4983192381195,0.245334543055125));
#30362=CARTESIAN_POINT('Ctrl Pts',(374.20764053214,-11.5044197958714,0.34920687738912));
#30363=CARTESIAN_POINT('Ctrl Pts',(374.195315543526,-11.5105203536233,0.452677686648481));
#30364=CARTESIAN_POINT('Ctrl Pts',(374.178277969535,-11.5166209113752,0.555279932126297));
#30365=CARTESIAN_POINT('Ctrl Pts',(374.16123093833,-11.5227248554238,0.657939130042905));
#30366=CARTESIAN_POINT('Ctrl Pts',(374.139466199945,-11.5288287994724,0.75972838772451));
#30367=CARTESIAN_POINT('Ctrl Pts',(374.113109344737,-11.534932743521,0.860192663117589));
#30368=CARTESIAN_POINT('Ctrl Pts',(374.086713195783,-11.5410457875485,0.960806714259869));
#30369=CARTESIAN_POINT('Ctrl Pts',(374.055711385291,-11.5471588315761,1.06009143237605));
#30370=CARTESIAN_POINT('Ctrl Pts',(374.02027882491,-11.5532718756036,1.15760863394903));
#30371=CARTESIAN_POINT('Ctrl Pts',(374.001225562142,-11.5565590621043,1.21004686720024));
#30372=CARTESIAN_POINT('Ctrl Pts',(373.980891938843,-11.5598462486049,1.2619743706633));
#30373=CARTESIAN_POINT('Ctrl Pts',(373.959310691612,-11.5631334351056,1.31332586303767));
#30374=CARTESIAN_POINT('Ctrl Pts',(373.919141241698,-11.5692519171414,1.4089070488158));
#30375=CARTESIAN_POINT('Ctrl Pts',(373.87451915558,-11.5753703991772,1.50279467947119));
#30376=CARTESIAN_POINT('Ctrl Pts',(373.825609166001,-11.5814888812131,1.59454737922916));
#30377=CARTESIAN_POINT('Ctrl Pts',(373.776774474275,-11.5875979437302,1.68615882397154));
#30378=CARTESIAN_POINT('Ctrl Pts',(373.723665216347,-11.5937070062472,1.77564150736957));
#30379=CARTESIAN_POINT('Ctrl Pts',(373.666493968443,-11.5998160687643,1.86257443203849));
#30380=CARTESIAN_POINT('Ctrl Pts',(373.609373083787,-11.6059197496911,1.94943077582751));
#30381=CARTESIAN_POINT('Ctrl Pts',(373.54819755381,-11.6120234306179,2.03374147229159));
#30382=CARTESIAN_POINT('Ctrl Pts',(373.483225436315,-11.6181271115447,2.11511079585554));
#30383=CARTESIAN_POINT('Ctrl Pts',(373.418294000153,-11.6242269707418,2.19642917121784));
#30384=CARTESIAN_POINT('Ctrl Pts',(373.349570967265,-11.6303268299388,2.27480950428586));
#30385=CARTESIAN_POINT('Ctrl Pts',(373.277356699608,-11.6364266891358,2.34988643503427));
#30386=CARTESIAN_POINT('Ctrl Pts',(373.205169250553,-11.6425242829952,2.42493548405761));
#30387=CARTESIAN_POINT('Ctrl Pts',(373.12949344011,-11.6486218768546,2.49668326527966));
#30388=CARTESIAN_POINT('Ctrl Pts',(373.05066817607,-11.654719470714,2.56479946758382));
#30389=CARTESIAN_POINT('Ctrl Pts',(372.971823960306,-11.6608185305997,2.63293204686428));
#30390=CARTESIAN_POINT('Ctrl Pts',(372.88982909368,-11.6669175904855,2.69743101766755));
#30391=CARTESIAN_POINT('Ctrl Pts',(372.805057149596,-11.6730166503713,2.75800501961741));
#30392=CARTESIAN_POINT('Ctrl Pts',(372.72027809087,-11.6791162221319,2.81858410535232));
#30393=CARTESIAN_POINT('Ctrl Pts',(372.632721841388,-11.6852157938926,2.8752373257988));
#30394=CARTESIAN_POINT('Ctrl Pts',(372.542791456492,-11.6913153656532,2.92771634716142));
#30395=CARTESIAN_POINT('Ctrl Pts',(372.452776154428,-11.6974206969618,2.98024492207464));
#30396=CARTESIAN_POINT('Ctrl Pts',(372.360382609697,-11.7035260282703,3.02859121535317));
#30397=CARTESIAN_POINT('Ctrl Pts',(372.266038973352,-11.7096313595789,3.07255263529865));
#30398=CARTESIAN_POINT('Ctrl Pts',(372.18297656306,-11.7150066403478,3.11125732850278));
#30399=CARTESIAN_POINT('Ctrl Pts',(372.098403070811,-11.7203819211167,3.14656372242825));
#30400=CARTESIAN_POINT('Ctrl Pts',(372.012622422842,-11.7257572018857,3.17836489467751));
#30401=CARTESIAN_POINT('Origin',(370.834317853224,-11.,0.));
#30402=CARTESIAN_POINT('',(367.444568709247,-12.1089821967158,-0.00240902652174493));
#30403=CARTESIAN_POINT('Ctrl Pts',(372.012622422842,-11.7257572018857,3.17836489467751));
#30404=CARTESIAN_POINT('Ctrl Pts',(371.915005782587,-11.7318741625465,3.21455398469513));
#30405=CARTESIAN_POINT('Ctrl Pts',(371.81582598781,-11.7379911232073,3.24620278346893));
#30406=CARTESIAN_POINT('Ctrl Pts',(371.715542697541,-11.7441080838681,3.27320146588291));
#30407=CARTESIAN_POINT('Ctrl Pts',(371.650333858663,-11.7480856149312,3.2907572593431));
#30408=CARTESIAN_POINT('Ctrl Pts',(371.584658684559,-11.7520631459944,3.30634793040135));
#30409=CARTESIAN_POINT('Ctrl Pts',(371.518645161599,-11.7560406770575,3.31995499932034));
#30410=CARTESIAN_POINT('Ctrl Pts',(371.417102457427,-11.7621589577062,3.3408855376696));
#30411=CARTESIAN_POINT('Ctrl Pts',(371.314438573247,-11.7682772383548,3.35718623096852));
#30412=CARTESIAN_POINT('Ctrl Pts',(371.211110629511,-11.7743955190035,3.36874342540923));
#30413=CARTESIAN_POINT('Ctrl Pts',(371.107912570322,-11.7805061088952,3.38028609230866));
#30414=CARTESIAN_POINT('Ctrl Pts',(371.004052530467,-11.7866166987868,3.38709706969832));
#30415=CARTESIAN_POINT('Ctrl Pts',(370.899998259857,-11.7927272886784,3.38911362256926));
#30416=CARTESIAN_POINT('Ctrl Pts',(370.796045530335,-11.7988319155668,3.39112820759235));
#30417=CARTESIAN_POINT('Ctrl Pts',(370.691899369855,-11.8049365424553,3.38835766518394));
#30418=CARTESIAN_POINT('Ctrl Pts',(370.58803226137,-11.8110411693437,3.38079110116927));
#30419=CARTESIAN_POINT('Ctrl Pts',(370.484233341735,-11.8171417885391,3.37322950461059));
#30420=CARTESIAN_POINT('Ctrl Pts',(370.380713532429,-11.8232424077346,3.36087817934067));
#30421=CARTESIAN_POINT('Ctrl Pts',(370.277944140033,-11.8293430269301,3.34377830511685));
#30422=CARTESIAN_POINT('Ctrl Pts',(370.175208956113,-11.8354416154345,3.32668412286631));
#30423=CARTESIAN_POINT('Ctrl Pts',(370.073224111271,-11.8415402039389,3.30484460356575));
#30424=CARTESIAN_POINT('Ctrl Pts',(369.972453844031,-11.8476387924433,3.27835255763599));
#30425=CARTESIAN_POINT('Ctrl Pts',(369.871691460177,-11.8537369038474,3.2518625842125));
#30426=CARTESIAN_POINT('Ctrl Pts',(369.772143875763,-11.8598350152515,3.22072091642667));
#30427=CARTESIAN_POINT('Ctrl Pts',(369.674262364553,-11.8659331266557,3.18507085097094));
#30428=CARTESIAN_POINT('Ctrl Pts',(369.576363587411,-11.8720323137438,3.14941449697693));
#30429=CARTESIAN_POINT('Ctrl Pts',(369.480131866643,-11.878131500832,3.10924831049607));
#30430=CARTESIAN_POINT('Ctrl Pts',(369.38599979111,-11.8842306879202,3.06476424108832));
#30431=CARTESIAN_POINT('Ctrl Pts',(369.291773199658,-11.8903359990662,3.02023550621803));
#30432=CARTESIAN_POINT('Ctrl Pts',(369.199650847426,-11.8964413102121,2.97138041394359));
#30433=CARTESIAN_POINT('Ctrl Pts',(369.110041870335,-11.9025466213581,2.91843749244896));
#30434=CARTESIAN_POINT('Ctrl Pts',(369.02038299778,-11.9086553320221,2.86546509163551));
#30435=CARTESIAN_POINT('Ctrl Pts',(368.933240643547,-11.914764042686,2.80840056001482));
#30436=CARTESIAN_POINT('Ctrl Pts',(368.848994454445,-11.92087275335,2.74752544387843));
#30437=CARTESIAN_POINT('Ctrl Pts',(368.764623093409,-11.9269905402598,2.68655988025695));
#30438=CARTESIAN_POINT('Ctrl Pts',(368.683156823088,-11.9331083271695,2.62177268999682));
#30439=CARTESIAN_POINT('Ctrl Pts',(368.60494178693,-11.9392261140793,2.55348534703728));
#30440=CARTESIAN_POINT('Ctrl Pts',(368.563511155485,-11.9424667157227,2.51731343077369));
#30441=CARTESIAN_POINT('Ctrl Pts',(368.522992146512,-11.9457073173661,2.48016005265332));
#30442=CARTESIAN_POINT('Ctrl Pts',(368.483431780173,-11.9489479190095,2.44207693040921));
#30443=CARTESIAN_POINT('Ctrl Pts',(368.409809033748,-11.9549787527741,2.3712033690256));
#30444=CARTESIAN_POINT('Ctrl Pts',(368.339260858662,-11.9610095865388,2.29686894666904));
#30445=CARTESIAN_POINT('Ctrl Pts',(368.272134796697,-11.9670404203034,2.21937447208579));
#30446=CARTESIAN_POINT('Ctrl Pts',(368.205109404078,-11.9730622095916,2.14199621641739));
#30447=CARTESIAN_POINT('Ctrl Pts',(368.141496201636,-11.9790839988797,2.06146766348274));
#30448=CARTESIAN_POINT('Ctrl Pts',(368.081607009118,-11.9851057881678,1.97812741532029));
#30449=CARTESIAN_POINT('Ctrl Pts',(368.021768662514,-11.9911224649579,1.89485792301379));
#30450=CARTESIAN_POINT('Ctrl Pts',(367.965648301211,-11.997139141748,1.80878183074363));
#30451=CARTESIAN_POINT('Ctrl Pts',(367.913518094768,-12.0031558185381,1.72027144180929));
#30452=CARTESIAN_POINT('Ctrl Pts',(367.861417856758,-12.0091690364819,1.63181193542088));
#30453=CARTESIAN_POINT('Ctrl Pts',(367.813303438478,-12.0151822544257,1.54092128970282));
#30454=CARTESIAN_POINT('Ctrl Pts',(367.769403602583,-12.0211954723694,1.44800058657285));
#30455=CARTESIAN_POINT('Ctrl Pts',(367.725516971768,-12.0272068815359,1.35510783401123));
#30456=CARTESIAN_POINT('Ctrl Pts',(367.685842590214,-12.0332182907024,1.26018663443941));
#30457=CARTESIAN_POINT('Ctrl Pts',(367.65056268499,-12.0392296998688,1.16366150200399));
#30458=CARTESIAN_POINT('Ctrl Pts',(367.615268449658,-12.0452435507693,1.06709716267199));
#30459=CARTESIAN_POINT('Ctrl Pts',(367.584372414241,-12.0512574016698,0.968927999078147));
#30460=CARTESIAN_POINT('Ctrl Pts',(367.55800797976,-12.0572712525702,0.869596846557717));
#30461=CARTESIAN_POINT('Ctrl Pts',(367.531638896956,-12.063286163775,0.770248180925193));
#30462=CARTESIAN_POINT('Ctrl Pts',(367.509803106472,-12.0693010749797,0.669737546039836));
#30463=CARTESIAN_POINT('Ctrl Pts',(367.492583177307,-12.0753159861844,0.568519496830185));
#30464=CARTESIAN_POINT('Ctrl Pts',(367.475343572843,-12.0813377699597,0.467185797005666));
#30465=CARTESIAN_POINT('Ctrl Pts',(367.462730425957,-12.0873595537349,0.365143503568449));
#30466=CARTESIAN_POINT('Ctrl Pts',(367.454774543377,-12.0933813375101,0.262853722376045));
#30467=CARTESIAN_POINT('Ctrl Pts',(367.447904009737,-12.098581623912,0.174518408781142));
#30468=CARTESIAN_POINT('Ctrl Pts',(367.444505879605,-12.1037819103139,0.0859987702498958));
#30469=CARTESIAN_POINT('Ctrl Pts',(367.444568709247,-12.1089821967158,-0.00240902652174046));
#30470=CARTESIAN_POINT('Ctrl Pts',(367.444568709248,-12.1089821967504,-0.00240902711028121));
#30471=CARTESIAN_POINT('Ctrl Pts',(367.444679279279,-12.1181338593118,-0.157992443353066));
#30472=CARTESIAN_POINT('Ctrl Pts',(367.455504799377,-12.1272855218732,-0.313184958602908));
#30473=CARTESIAN_POINT('Ctrl Pts',(367.476864661899,-12.1364371844346,-0.466811664981343));
#30474=CARTESIAN_POINT('Ctrl Pts',(367.481079824371,-12.1382431766102,-0.497128411017277));
#30475=CARTESIAN_POINT('Ctrl Pts',(367.485705090691,-12.1400491687858,-0.527384267298463));
#30476=CARTESIAN_POINT('Ctrl Pts',(367.490738871252,-12.1418551609614,-0.557570312889645));
#30477=CARTESIAN_POINT('Ctrl Pts',(367.507790544157,-12.1479728666244,-0.659823990703624));
#30478=CARTESIAN_POINT('Ctrl Pts',(367.529564114787,-12.1540905722874,-0.761456326808137));
#30479=CARTESIAN_POINT('Ctrl Pts',(367.556001056195,-12.1602082779504,-0.862000023675843));
#30480=CARTESIAN_POINT('Ctrl Pts',(367.582404705976,-12.1663182796823,-0.962417107436716));
#30481=CARTESIAN_POINT('Ctrl Pts',(367.613459942336,-12.1724282814141,-1.06174786995216));
#30482=CARTESIAN_POINT('Ctrl Pts',(367.649056907049,-12.1785382831459,-1.15953342654357));
#30483=CARTESIAN_POINT('Ctrl Pts',(367.684619060071,-12.1846423096636,-1.2572233547437));
#30484=CARTESIAN_POINT('Ctrl Pts',(367.72471396307,-12.1907463361814,-1.3533706849762));
#30485=CARTESIAN_POINT('Ctrl Pts',(367.769181689171,-12.1968503626991,-1.4475307797468));
#30486=CARTESIAN_POINT('Ctrl Pts',(367.813620105697,-12.2029503659299,-1.54162881170132));
#30487=CARTESIAN_POINT('Ctrl Pts',(367.862425431984,-12.2090503691608,-1.63374182994585));
#30488=CARTESIAN_POINT('Ctrl Pts',(367.915389583341,-12.2151503723916,-1.72344504344643));
#30489=CARTESIAN_POINT('Ctrl Pts',(367.968336021748,-12.221248335581,-1.81311825724637));
#30490=CARTESIAN_POINT('Ctrl Pts',(368.02543830442,-12.2273462987704,-1.9003829028048));
#30491=CARTESIAN_POINT('Ctrl Pts',(368.086442723697,-12.2334442619598,-1.98483937260049));
#30492=CARTESIAN_POINT('Ctrl Pts',(368.14744228475,-12.2395417395243,-2.06928911651609));
#30493=CARTESIAN_POINT('Ctrl Pts',(368.212343115232,-12.2456392170888,-2.15093078515682));
#30494=CARTESIAN_POINT('Ctrl Pts',(368.280849075954,-12.2517366946532,-2.22939504485151));
#30495=CARTESIAN_POINT('Ctrl Pts',(368.349367035554,-12.2578352401961,-2.30787304762822));
#30496=CARTESIAN_POINT('Ctrl Pts',(368.421491100579,-12.2639337857389,-2.38317221552238));
#30497=CARTESIAN_POINT('Ctrl Pts',(368.49688647126,-12.2700323312818,-2.45495816606099));
#30498=CARTESIAN_POINT('Ctrl Pts',(368.572357455551,-12.276136993023,-2.52681611034187));
#30499=CARTESIAN_POINT('Ctrl Pts',(368.651105987684,-12.2822416547643,-2.59515350894791));
#30500=CARTESIAN_POINT('Ctrl Pts',(368.732762260525,-12.2883463165056,-2.65967463297596));
#30501=CARTESIAN_POINT('Ctrl Pts',(368.814463934897,-12.2944543724868,-2.72423163125671));
#30502=CARTESIAN_POINT('Ctrl Pts',(368.899076225481,-12.300562428468,-2.78496788031011));
#30503=CARTESIAN_POINT('Ctrl Pts',(368.986199813889,-12.3066704844492,-2.84163065425215));
#30504=CARTESIAN_POINT('Ctrl Pts',(369.073452832902,-12.3127876145445,-2.89837760628197));
#30505=CARTESIAN_POINT('Ctrl Pts',(369.163224233733,-12.3189047446398,-2.95103878339532));
#30506=CARTESIAN_POINT('Ctrl Pts',(369.255089516233,-12.325021874735,-2.99940709510121));
#30507=CARTESIAN_POINT('Ctrl Pts',(369.303849656955,-12.3282687174611,-3.02507996760658));
#30508=CARTESIAN_POINT('Ctrl Pts',(369.353199339037,-12.3315155601872,-3.04954423421724));
#30509=CARTESIAN_POINT('Ctrl Pts',(369.403072991065,-12.3347624029133,-3.07277451288639));
#30510=CARTESIAN_POINT('Ctrl Pts',(369.497044704206,-12.3408800895246,-3.1165449005463));
#30511=CARTESIAN_POINT('Ctrl Pts',(369.593174606421,-12.3469977761359,-3.15606977135722));
#30512=CARTESIAN_POINT('Ctrl Pts',(369.691044219909,-12.3531154627471,-3.19113309999219));
#30513=CARTESIAN_POINT('Ctrl Pts',(369.788790599952,-12.3592254462158,-3.22615227830726));
#30514=CARTESIAN_POINT('Ctrl Pts',(369.888271938434,-12.3653354296845,-3.25672094264121));
#30515=CARTESIAN_POINT('Ctrl Pts',(369.989047663817,-12.3714454131532,-3.2826701584837));
#30516=CARTESIAN_POINT('Ctrl Pts',(370.08972484969,-12.3775494222191,-3.30859400092413));
#30517=CARTESIAN_POINT('Ctrl Pts',(370.191693495577,-12.383653431285,-3.32990727304869));
#30518=CARTESIAN_POINT('Ctrl Pts',(370.294496461912,-12.389757440351,-3.3464903896444));
#30519=CARTESIAN_POINT('Ctrl Pts',(370.397231690275,-12.3958574274201,-3.36306257944745));
#30520=CARTESIAN_POINT('Ctrl Pts',(370.500799727228,-12.4019574144892,-3.37491074498608));
#30521=CARTESIAN_POINT('Ctrl Pts',(370.604732563532,-12.4080574015584,-3.38196624129472));
#30522=CARTESIAN_POINT('Ctrl Pts',(370.708630654981,-12.4141553493955,-3.38901937894357));
#30523=CARTESIAN_POINT('Ctrl Pts',(370.812892879723,-12.4202532972326,-3.39128300367998));
#30524=CARTESIAN_POINT('Ctrl Pts',(370.917046194091,-12.4263512450696,-3.38874033884531));
#30525=CARTESIAN_POINT('Ctrl Pts',(371.021191228166,-12.4324487081138,-3.38619787615503));
#30526=CARTESIAN_POINT('Ctrl Pts',(371.125226944248,-12.4385461711579,-3.37884989457313));
#30527=CARTESIAN_POINT('Ctrl Pts',(371.228681267264,-12.4446436342021,-3.36673173272935));
#30528=CARTESIAN_POINT('Ctrl Pts',(371.332153724948,-12.45074216608,-3.35461144667422));
#30529=CARTESIAN_POINT('Ctrl Pts',(371.435044164988,-12.4568406979578,-3.33771936831974));
#30530=CARTESIAN_POINT('Ctrl Pts',(371.536887471093,-12.4629392298357,-3.31614248706946));
#30531=CARTESIAN_POINT('Ctrl Pts',(371.638832938744,-12.4690438793022,-3.29454396151456));
#30532=CARTESIAN_POINT('Ctrl Pts',(371.739728758831,-12.4751485287686,-3.26825133832305));
#30533=CARTESIAN_POINT('Ctrl Pts',(371.839121893272,-12.481253178235,-3.2374023388518));
#30534=CARTESIAN_POINT('Ctrl Pts',(371.938570303792,-12.4873612227155,-3.2065361831479));
#30535=CARTESIAN_POINT('Ctrl Pts',(372.036513964408,-12.493469267196,-3.17110874785328));
#30536=CARTESIAN_POINT('Ctrl Pts',(372.132518610855,-12.4995773116765,-3.13130641352555));
#30537=CARTESIAN_POINT('Ctrl Pts',(372.228665902626,-12.5056944315925,-3.09144494021768));
#30538=CARTESIAN_POINT('Ctrl Pts',(372.322868042418,-12.5118115515086,-3.047195767398));
#30539=CARTESIAN_POINT('Ctrl Pts',(372.41471415927,-12.5179286714247,-2.9987918531196));
#30540=CARTESIAN_POINT('Ctrl Pts',(372.463466436875,-12.5211756625715,-2.97309886633938));
#30541=CARTESIAN_POINT('Ctrl Pts',(372.511555359975,-12.5244226537184,-2.94623602231471));
#30542=CARTESIAN_POINT('Ctrl Pts',(372.558922902766,-12.5276696448653,-2.91824304772476));
#30543=CARTESIAN_POINT('Ctrl Pts',(372.648167311643,-12.5337872475201,-2.8655019443706));
#30544=CARTESIAN_POINT('Ctrl Pts',(372.735131232971,-12.5399048501749,-2.80857991414978));
#30545=CARTESIAN_POINT('Ctrl Pts',(372.819399833067,-12.5460224528297,-2.74769987367639));
#30546=CARTESIAN_POINT('Ctrl Pts',(372.903562301904,-12.5521323507301,-2.68689650797124));
#30547=CARTESIAN_POINT('Ctrl Pts',(372.985035857425,-12.5582422486304,-2.62214529098456));
#30548=CARTESIAN_POINT('Ctrl Pts',(373.063432003934,-12.5643521465307,-2.55371399448042));
#30549=CARTESIAN_POINT('Ctrl Pts',(373.141751473892,-12.5704560685519,-2.48534962825292));
#30550=CARTESIAN_POINT('Ctrl Pts',(373.216999202493,-12.576559990573,-2.41331261936389));
#30551=CARTESIAN_POINT('Ctrl Pts',(373.288818020092,-12.5826639125942,-2.33791231515347));
#30552=CARTESIAN_POINT('Ctrl Pts',(373.360589493313,-12.5887638107899,-2.26256171630684));
#30553=CARTESIAN_POINT('Ctrl Pts',(373.428936258777,-12.5948637089857,-2.18385253869375));
#30554=CARTESIAN_POINT('Ctrl Pts',(373.493537008161,-12.6009636071814,-2.1021319055941));
#30555=CARTESIAN_POINT('Ctrl Pts',(373.558116149598,-12.607061465056,-2.02043860677535));
#30556=CARTESIAN_POINT('Ctrl Pts',(373.618951502498,-12.6131593229306,-1.93573618799773));
#30557=CARTESIAN_POINT('Ctrl Pts',(373.675761685678,-12.6192571808052,-1.84840526116668));
#30558=CARTESIAN_POINT('Ctrl Pts',(373.732567343268,-12.6253545529148,-1.76108129125671));
#30559=CARTESIAN_POINT('Ctrl Pts',(373.785348237423,-12.6314519250243,-1.67112958618058));
#30560=CARTESIAN_POINT('Ctrl Pts',(373.833866513226,-12.6375492971338,-1.5789594354455));
#30561=CARTESIAN_POINT('Ctrl Pts',(373.882393287187,-12.643647737221,-1.48677314076177));
#30562=CARTESIAN_POINT('Ctrl Pts',(373.926655761318,-12.6497461773082,-1.39236800438883));
#30563=CARTESIAN_POINT('Ctrl Pts',(373.966462612032,-12.6558446173954,-1.29617679055429));
#30564=CARTESIAN_POINT('Ctrl Pts',(374.00630938966,-12.6619491743166,-1.19988909537721));
#30565=CARTESIAN_POINT('Ctrl Pts',(374.04169145814,-12.6680537312378,-1.10181213916787));
#30566=CARTESIAN_POINT('Ctrl Pts',(374.072466163087,-12.674158288159,-1.00239741910693));
#30567=CARTESIAN_POINT('Ctrl Pts',(374.10325798046,-12.680266239549,-0.902927419002685));
#30568=CARTESIAN_POINT('Ctrl Pts',(374.129437223958,-12.6863741909391,-0.802118584415533));
#30569=CARTESIAN_POINT('Ctrl Pts',(374.150911986072,-12.6924821423291,-0.700434451222036));
#30570=CARTESIAN_POINT('Ctrl Pts',(374.172418656284,-12.6985991691683,-0.598599231499183));
#30571=CARTESIAN_POINT('Ctrl Pts',(374.189206817382,-12.7047161960074,-0.495886535152319));
#30572=CARTESIAN_POINT('Ctrl Pts',(374.201236204739,-12.7108332228466,-0.392766949641725));
#30573=CARTESIAN_POINT('Ctrl Pts',(374.207623311376,-12.7140811108368,-0.338014719164696));
#30574=CARTESIAN_POINT('Ctrl Pts',(374.212669720767,-12.717328998827,-0.283147824870211));
#30575=CARTESIAN_POINT('Ctrl Pts',(374.216375377086,-12.7205768868171,-0.228236648652391));
#30576=CARTESIAN_POINT('Ctrl Pts',(374.223355268854,-12.7266945363493,-0.124807179250421));
#30577=CARTESIAN_POINT('Ctrl Pts',(374.225597296935,-12.7328121858815,-0.0208937739322935));
#30578=CARTESIAN_POINT('Ctrl Pts',(374.223050682688,-12.7389298354137,0.0830353720467266));
#30579=CARTESIAN_POINT('Ctrl Pts',(374.220507275439,-12.7450397808774,0.186833638140619));
#30580=CARTESIAN_POINT('Ctrl Pts',(374.213187227127,-12.751149726341,0.290647183804213));
#30581=CARTESIAN_POINT('Ctrl Pts',(374.201091647165,-12.7572596718046,0.394004166137646));
#30582=CARTESIAN_POINT('Ctrl Pts',(374.189007896168,-12.7633636420002,0.497260069718577));
#30583=CARTESIAN_POINT('Ctrl Pts',(374.172157951284,-12.7694676121959,0.600059877867714));
#30584=CARTESIAN_POINT('Ctrl Pts',(374.150594926402,-12.7755715823916,0.701934068423815));
#30585=CARTESIAN_POINT('Ctrl Pts',(374.129046113696,-12.7816715294642,0.80374111376403));
#30586=CARTESIAN_POINT('Ctrl Pts',(374.102790486939,-12.7877714765369,0.904623340137016));
#30587=CARTESIAN_POINT('Ctrl Pts',(374.071932595962,-12.7938714236096,1.00411943517842));
#30588=CARTESIAN_POINT('Ctrl Pts',(374.041085024312,-12.7999693307716,1.10358225728431));
#30589=CARTESIAN_POINT('Ctrl Pts',(374.005638373792,-12.8060672379336,1.20165946400976));
#30590=CARTESIAN_POINT('Ctrl Pts',(373.965747393962,-12.8121651450956,1.2979037305952));
#30591=CARTESIAN_POINT('Ctrl Pts',(373.925859589626,-12.8182625668379,1.39414033572181));
#30592=CARTESIAN_POINT('Ctrl Pts',(373.881528322661,-12.8243599885802,1.48854389844459));
#30593=CARTESIAN_POINT('Ctrl Pts',(373.832956610308,-12.8304574103225,1.5806867706829));
#30594=CARTESIAN_POINT('Ctrl Pts',(373.784376388271,-12.8365559003231,1.67284578620112));
#30595=CARTESIAN_POINT('Ctrl Pts',(373.731554442832,-12.8426543903237,1.76274294830886));
#30596=CARTESIAN_POINT('Ctrl Pts',(373.674739467748,-12.8487528803243,1.84997570639374));
#30597=CARTESIAN_POINT('Ctrl Pts',(373.617867505614,-12.8548574872851,1.9372959614356));
#30598=CARTESIAN_POINT('Ctrl Pts',(373.556994749451,-12.860962094246,2.02194611991554));
#30599=CARTESIAN_POINT('Ctrl Pts',(373.49241286819,-12.8670667012068,2.10355317354001));
#30600=CARTESIAN_POINT('Ctrl Pts',(373.427795074727,-12.8731747027713,2.18520560659621));
#30601=CARTESIAN_POINT('Ctrl Pts',(373.359464326172,-12.8792827043357,2.26381124322872));
#30602=CARTESIAN_POINT('Ctrl Pts',(373.287750921077,-12.8853907059001,2.33903211693762));
#30603=CARTESIAN_POINT('Ctrl Pts',(373.215930965116,-12.8915077826556,2.41436475286438));
#30604=CARTESIAN_POINT('Ctrl Pts',(373.14071862285,-12.8976248594111,2.48630228933271));
#30605=CARTESIAN_POINT('Ctrl Pts',(373.062479216396,-12.9037419361666,2.5545453611489));
#30606=CARTESIAN_POINT('Ctrl Pts',(373.020943942972,-12.9069893337008,2.59077383955402));
#30607=CARTESIAN_POINT('Ctrl Pts',(372.978556096282,-12.9102367312349,2.62596181878191));
#30608=CARTESIAN_POINT('Ctrl Pts',(372.935373661073,-12.9134841287691,2.66006946428179));
#30609=CARTESIAN_POINT('Ctrl Pts',(372.854036840211,-12.9196008053813,2.72431335045043));
#30610=CARTESIAN_POINT('Ctrl Pts',(372.769622249332,-12.9257174819936,2.78492482186272));
#30611=CARTESIAN_POINT('Ctrl Pts',(372.682487112647,-12.9318341586059,2.84159734146523));
#30612=CARTESIAN_POINT('Ctrl Pts',(372.595448309454,-12.9379440728391,2.89820720595616));
#30613=CARTESIAN_POINT('Ctrl Pts',(372.505695289837,-12.9440539870724,2.9508865411481));
#30614=CARTESIAN_POINT('Ctrl Pts',(372.413617795613,-12.9501639013057,2.9993693928008));
#30615=CARTESIAN_POINT('Ctrl Pts',(372.321635227428,-12.9562675166061,3.04780226171774));
#30616=CARTESIAN_POINT('Ctrl Pts',(372.227333326346,-12.9623711319065,3.09204705697198));
#30617=CARTESIAN_POINT('Ctrl Pts',(372.131129266487,-12.9684747472069,3.131882057315));
#30618=CARTESIAN_POINT('Ctrl Pts',(372.091932655392,-12.9709615553057,3.14811211058583));
#30619=CARTESIAN_POINT('Ctrl Pts',(372.05242058511,-12.9734483634045,3.1636106553068));
#30620=CARTESIAN_POINT('Ctrl Pts',(372.012622422842,-12.9759351715034,3.17836489467751));
#30621=CARTESIAN_POINT('',(367.444567879036,-11.766017803207,-0.000418324226323652));
#30622=CARTESIAN_POINT('Ctrl Pts',(372.012622420937,-12.6303878084336,3.17836489538373));
#30623=CARTESIAN_POINT('Ctrl Pts',(372.024541985714,-12.6296579468698,3.1739459950733));
#30624=CARTESIAN_POINT('Ctrl Pts',(372.036437143336,-12.6289300869064,3.16945987625657));
#30625=CARTESIAN_POINT('Ctrl Pts',(372.144170050708,-12.6223418396811,3.12813587321469));
#30626=CARTESIAN_POINT('Ctrl Pts',(372.238317516829,-12.6166147135911,3.08702677986565));
#30627=CARTESIAN_POINT('Ctrl Pts',(372.587203778726,-12.5952877562432,2.91541792870016));
#30628=CARTESIAN_POINT('Ctrl Pts',(372.826901990794,-12.5805117446766,2.75714699729164));
#30629=CARTESIAN_POINT('Ctrl Pts',(373.100889355238,-12.5605982380091,2.52164899902446));
#30630=CARTESIAN_POINT('Ctrl Pts',(373.156267313735,-12.5563838383691,2.47075073252989));
#30631=CARTESIAN_POINT('Ctrl Pts',(373.239129564653,-12.5496953357588,2.38934391166878));
#30632=CARTESIAN_POINT('Ctrl Pts',(373.267832046144,-12.5473020891819,2.3601042932173));
#30633=CARTESIAN_POINT('Ctrl Pts',(373.329787010923,-12.5419494394304,2.29465781631356));
#30634=CARTESIAN_POINT('Ctrl Pts',(373.362794112095,-12.5389760885359,2.25823560716289));
#30635=CARTESIAN_POINT('Ctrl Pts',(373.506301568501,-12.5255427559874,2.09278850339456));
#30636=CARTESIAN_POINT('Ctrl Pts',(373.607796347794,-12.5146641112427,1.95628976816168));
#30637=CARTESIAN_POINT('Ctrl Pts',(373.815885838914,-12.4897407625858,1.62749352155561));
#30638=CARTESIAN_POINT('Ctrl Pts',(373.91490585672,-12.4757778559277,1.43125230674521));
#30639=CARTESIAN_POINT('Ctrl Pts',(374.023531232821,-12.4574762311982,1.15145790770657));
#30640=CARTESIAN_POINT('Ctrl Pts',(374.050079629289,-12.4526279127671,1.07508840826241));
#30641=CARTESIAN_POINT('Ctrl Pts',(374.094457835642,-12.4437416491078,0.931011198078606));
#30642=CARTESIAN_POINT('Ctrl Pts',(374.112969826725,-12.4396846224251,0.863560536736765));
#30643=CARTESIAN_POINT('Ctrl Pts',(374.152908152123,-12.4299585174775,0.698147772515782));
#30644=CARTESIAN_POINT('Ctrl Pts',(374.172101285132,-12.4243586756921,0.599713328662823));
#30645=CARTESIAN_POINT('Ctrl Pts',(374.226845438165,-12.403991383365,0.233059627178938));
#30646=CARTESIAN_POINT('Ctrl Pts',(374.234624679967,-12.3899568418653,-0.038246620854701));
#30647=CARTESIAN_POINT('Ctrl Pts',(374.202045271429,-12.3703371535882,-0.395810311365903));
#30648=CARTESIAN_POINT('Ctrl Pts',(374.190551283893,-12.3654156264134,-0.483682314978925));
#30649=CARTESIAN_POINT('Ctrl Pts',(374.168380716414,-12.3578739319596,-0.613418354381483));
#30650=CARTESIAN_POINT('Ctrl Pts',(374.160324201544,-12.3553719966445,-0.655697196522826));
#30651=CARTESIAN_POINT('Ctrl Pts',(374.141961403044,-12.3500942474341,-0.742987573549507));
#30652=CARTESIAN_POINT('Ctrl Pts',(374.131536247922,-12.3473137480415,-0.787963681452503));
#30653=CARTESIAN_POINT('Ctrl Pts',(374.091156387942,-12.337277161592,-0.94730280752861));
#30654=CARTESIAN_POINT('Ctrl Pts',(374.056143761887,-12.3298184305544,-1.06028923587759));
#30655=CARTESIAN_POINT('Ctrl Pts',(373.93484686775,-12.3074405468112,-1.38973066729631));
#30656=CARTESIAN_POINT('Ctrl Pts',(373.832074768309,-12.2924075616409,-1.59940737685245));
#30657=CARTESIAN_POINT('Ctrl Pts',(373.65589259147,-12.2717981328518,-1.88122611755117));
#30658=CARTESIAN_POINT('Ctrl Pts',(373.599484548662,-12.2657394971227,-1.96319935736157));
#30659=CARTESIAN_POINT('Ctrl Pts',(373.497427743177,-12.255636549475,-2.09836531919811));
#30660=CARTESIAN_POINT('Ctrl Pts',(373.453589272517,-12.2515306801244,-2.15283756022057));
#30661=CARTESIAN_POINT('Ctrl Pts',(373.35519552766,-12.2427840420527,-2.26763945555668));
#30662=CARTESIAN_POINT('Ctrl Pts',(373.300090257508,-12.2381681513635,-2.32744083769161));
#30663=CARTESIAN_POINT('Ctrl Pts',(373.178788291599,-12.2285333713003,-2.4499308197327));
#30664=CARTESIAN_POINT('Ctrl Pts',(373.112106473679,-12.2235372207244,-2.51204759948053));
#30665=CARTESIAN_POINT('Ctrl Pts',(372.890001381342,-12.2076652007979,-2.70282246159297));
#30666=CARTESIAN_POINT('Ctrl Pts',(372.725584470146,-12.1970684666635,-2.82031763257719));
#30667=CARTESIAN_POINT('Ctrl Pts',(372.462451106292,-12.1805269397434,-2.9749460007408));
#30668=CARTESIAN_POINT('Ctrl Pts',(372.370850887397,-12.1748315781369,-3.02327380487728));
#30669=CARTESIAN_POINT('Ctrl Pts',(372.235650033008,-12.1663205469626,-3.08687231732244));
#30670=CARTESIAN_POINT('Ctrl Pts',(372.193718462074,-12.1636667960863,-3.10556630893179));
#30671=CARTESIAN_POINT('Ctrl Pts',(372.1114904902,-12.1584119518731,-3.14024095276223));
#30672=CARTESIAN_POINT('Ctrl Pts',(372.071242236142,-12.1558158016115,-3.1563112459577));
#30673=CARTESIAN_POINT('Ctrl Pts',(371.945821072504,-12.1476750061479,-3.20362220617634));
#30674=CARTESIAN_POINT('Ctrl Pts',(371.859697016181,-12.142014576942,-3.23221746721734));
#30675=CARTESIAN_POINT('Ctrl Pts',(371.618405912662,-12.1261402783332,-3.30171747762077));
#30676=CARTESIAN_POINT('Ctrl Pts',(371.461319782611,-12.1157976081619,-3.33511629259839));
#30677=CARTESIAN_POINT('Ctrl Pts',(371.134604612752,-12.0947822326438,-3.38067393947525));
#30678=CARTESIAN_POINT('Ctrl Pts',(370.965214086299,-12.0841565256868,-3.39146084121734));
#30679=CARTESIAN_POINT('Ctrl Pts',(370.719315785102,-12.0692551819074,-3.38865997171175));
#30680=CARTESIAN_POINT('Ctrl Pts',(370.642968974927,-12.0646988967876,-3.38520735498392));
#30681=CARTESIAN_POINT('Ctrl Pts',(370.495560815927,-12.0560259011502,-3.373537531118));
#30682=CARTESIAN_POINT('Ctrl Pts',(370.424515094832,-12.051901961379,-3.3656462324077));
#30683=CARTESIAN_POINT('Ctrl Pts',(370.240078235639,-12.0413107443668,-3.33923266716984));
#30684=CARTESIAN_POINT('Ctrl Pts',(370.127283562862,-12.0349497918939,-3.3171827490274));
#30685=CARTESIAN_POINT('Ctrl Pts',(369.854246246075,-12.0196243835144,-3.2492439831244));
#30686=CARTESIAN_POINT('Ctrl Pts',(369.695856069102,-12.0108029022286,-3.19719143226251));
#30687=CARTESIAN_POINT('Ctrl Pts',(369.413500394245,-11.9944411268758,-3.08074379185336));
#30688=CARTESIAN_POINT('Ctrl Pts',(369.288458472916,-11.9869418276964,-3.01993661350908));
#30689=CARTESIAN_POINT('Ctrl Pts',(369.121997341835,-11.9761701922901,-2.92593498675344));
#30690=CARTESIAN_POINT('Ctrl Pts',(369.077087351888,-11.9731797615429,-2.89918564597729));
#30691=CARTESIAN_POINT('Ctrl Pts',(368.998652822822,-11.9677739784008,-2.84997640764891));
#30692=CARTESIAN_POINT('Ctrl Pts',(368.964879139731,-11.9653816962809,-2.82793741047045));
#30693=CARTESIAN_POINT('Ctrl Pts',(368.876955795875,-11.9589873337304,-2.76829981613006));
#30694=CARTESIAN_POINT('Ctrl Pts',(368.82349850278,-11.9549319488835,-2.72971692192652));
#30695=CARTESIAN_POINT('Ctrl Pts',(368.698826341713,-11.9451275722923,-2.6340846304576));
#30696=CARTESIAN_POINT('Ctrl Pts',(368.628722693403,-11.9393306095287,-2.57566968285829));
#30697=CARTESIAN_POINT('Ctrl Pts',(368.353015442919,-11.9155744517769,-2.32641447151465));
#30698=CARTESIAN_POINT('Ctrl Pts',(368.169076352201,-11.8975425384769,-2.11319710994955));
#30699=CARTESIAN_POINT('Ctrl Pts',(367.971453027551,-11.8759526132159,-1.81663412427158));
#30700=CARTESIAN_POINT('Ctrl Pts',(367.931532080886,-11.8714315729378,-1.75213887541297));
#30701=CARTESIAN_POINT('Ctrl Pts',(367.858410241795,-11.8628122266085,-1.62463566630747));
#30702=CARTESIAN_POINT('Ctrl Pts',(367.824965147646,-11.8587071669493,-1.5618144904171));
#30703=CARTESIAN_POINT('Ctrl Pts',(367.742903175331,-11.8481534707186,-1.3952346788963));
#30704=CARTESIAN_POINT('Ctrl Pts',(367.697523779782,-11.841811192184,-1.28998092952482));
#30705=CARTESIAN_POINT('Ctrl Pts',(367.588423274243,-11.824783161097,-0.996915563777684));
#30706=CARTESIAN_POINT('Ctrl Pts',(367.535707360988,-11.8143561533316,-0.805506497705102));
#30707=CARTESIAN_POINT('Ctrl Pts',(367.477924655452,-11.7970798734975,-0.489966768151784));
#30708=CARTESIAN_POINT('Ctrl Pts',(367.462399460329,-11.7903875998426,-0.368244433617266));
#30709=CARTESIAN_POINT('Ctrl Pts',(367.450168323851,-11.780803097834,-0.200122982120811));
#30710=CARTESIAN_POINT('Ctrl Pts',(367.447766301528,-11.7781515277329,-0.15422505874192));
#30711=CARTESIAN_POINT('Ctrl Pts',(367.445147143127,-11.7733336456054,-0.0722844906329021));
#30712=CARTESIAN_POINT('Ctrl Pts',(367.444570387077,-11.7711856518553,-0.036260890360518));
#30713=CARTESIAN_POINT('Ctrl Pts',(367.444567861555,-11.7690118023792,-0.000237649104901999));
#30714=CARTESIAN_POINT('Ctrl Pts',(367.444567879036,-11.766017803207,-0.000418324226323596));
#30715=CARTESIAN_POINT('Ctrl Pts',(367.444555127666,-11.7599203887752,0.102908127781684));
#30716=CARTESIAN_POINT('Ctrl Pts',(367.449271066985,-11.7538229743435,0.20640283311262));
#30717=CARTESIAN_POINT('Ctrl Pts',(367.458735803286,-11.7477255599117,0.309597943527872));
#30718=CARTESIAN_POINT('Ctrl Pts',(367.46818869345,-11.741635777051,0.412663894144712));
#30719=CARTESIAN_POINT('Ctrl Pts',(367.482378525081,-11.7355459941903,0.515430572031453));
#30720=CARTESIAN_POINT('Ctrl Pts',(367.501273385533,-11.7294562113296,0.617429865570024));
#30721=CARTESIAN_POINT('Ctrl Pts',(367.52076030823,-11.7231756077682,0.72262526266596));
#30722=CARTESIAN_POINT('Ctrl Pts',(367.545252007484,-11.7168950042068,0.827003927291572));
#30723=CARTESIAN_POINT('Ctrl Pts',(367.574655535011,-11.7106144006454,0.930057328190894));
#30724=CARTESIAN_POINT('Ctrl Pts',(367.603119667462,-11.7045344521942,1.02981833986042));
#30725=CARTESIAN_POINT('Ctrl Pts',(367.636186423178,-11.6984545037431,1.1283370346564));
#30726=CARTESIAN_POINT('Ctrl Pts',(367.673719753446,-11.692374555292,1.22516313778319));
#30727=CARTESIAN_POINT('Ctrl Pts',(367.711241689998,-11.6862964524862,1.32195984812046));
#30728=CARTESIAN_POINT('Ctrl Pts',(367.75322735116,-11.6802183496804,1.41706458906934));
#30729=CARTESIAN_POINT('Ctrl Pts',(367.79949161502,-11.6741402468746,1.51004462397916));
#30730=CARTESIAN_POINT('Ctrl Pts',(367.845753861071,-11.6680624091643,1.60302060357878));
#30731=CARTESIAN_POINT('Ctrl Pts',(367.896294147212,-11.661984571454,1.69387167827921));
#30732=CARTESIAN_POINT('Ctrl Pts',(367.950880634756,-11.6559067337438,1.78218822509042));
#30733=CARTESIAN_POINT('Ctrl Pts',(368.005478930917,-11.6498275812234,1.87052387729691));
#30734=CARTESIAN_POINT('Ctrl Pts',(368.064124942212,-11.643748428703,1.9563235480984));
#30735=CARTESIAN_POINT('Ctrl Pts',(368.126543117109,-11.6376692761826,2.03920598296474));
#30736=CARTESIAN_POINT('Ctrl Pts',(368.189023917612,-11.6315840243072,2.12217157570357));
#30737=CARTESIAN_POINT('Ctrl Pts',(368.25528417705,-11.6254987724318,2.20221374864857));
#30738=CARTESIAN_POINT('Ctrl Pts',(368.325007729987,-11.6194135205565,2.27898393322951));
#30739=CARTESIAN_POINT('Ctrl Pts',(368.394773337554,-11.6133245982855,2.35580042270546));
#30740=CARTESIAN_POINT('Ctrl Pts',(368.468006096334,-11.6072356760145,2.42934069098724));
#30741=CARTESIAN_POINT('Ctrl Pts',(368.544353964849,-11.6011467537435,2.49929399079757));
#30742=CARTESIAN_POINT('Ctrl Pts',(368.620807472042,-11.5950494065392,2.56934408144579));
#30743=CARTESIAN_POINT('Ctrl Pts',(368.700384362463,-11.5889520593348,2.63579702564753));
#30744=CARTESIAN_POINT('Ctrl Pts',(368.782700804078,-11.5828547121305,2.6983833208337));
#30745=CARTESIAN_POINT('Ctrl Pts',(368.801299751674,-11.5814770500389,2.71252435027497));
#30746=CARTESIAN_POINT('Ctrl Pts',(368.820038446072,-11.5800993879474,2.72646816341016));
#30747=CARTESIAN_POINT('Ctrl Pts',(368.838912275429,-11.5787217258558,2.74021197037831));
#30748=CARTESIAN_POINT('Ctrl Pts',(368.92268496215,-11.5726068854265,2.80121472788649));
#30749=CARTESIAN_POINT('Ctrl Pts',(369.009388754275,-11.5664920449973,2.85846789347928));
#30750=CARTESIAN_POINT('Ctrl Pts',(369.098654492841,-11.560377204568,2.911679543137));
#30751=CARTESIAN_POINT('Ctrl Pts',(369.187809743689,-11.5542699327174,2.96482533064221));
#30752=CARTESIAN_POINT('Ctrl Pts',(369.279520273,-11.5481626608668,3.01393933253664));
#30753=CARTESIAN_POINT('Ctrl Pts',(369.373386233634,-11.5420553890161,3.05877162687604));
#30754=CARTESIAN_POINT('Ctrl Pts',(369.467162497687,-11.5359539531618,3.10356108030176));
#30755=CARTESIAN_POINT('Ctrl Pts',(369.563089714454,-11.5298525173075,3.14407678110448));
#30756=CARTESIAN_POINT('Ctrl Pts',(369.660742346388,-11.5237510814532,3.18011408478605));
#30757=CARTESIAN_POINT('Ctrl Pts',(369.758334125979,-11.5176534477153,3.21612893178302));
#30758=CARTESIAN_POINT('Ctrl Pts',(369.857648784432,-11.5115558139773,3.24767078430108));
#30759=CARTESIAN_POINT('Ctrl Pts',(369.958240372104,-11.5054581802393,3.2745829214686));
#30760=CARTESIAN_POINT('Ctrl Pts',(370.058800594723,-11.4993624477796,3.3014866672727));
#30761=CARTESIAN_POINT('Ctrl Pts',(370.160636544409,-11.4932667153199,3.32376345748213));
#30762=CARTESIAN_POINT('Ctrl Pts',(370.26328743465,-11.4871709828601,3.34130652942278));
#30763=CARTESIAN_POINT('Ctrl Pts',(370.365932548757,-11.4810755934054,3.35884861422019));
#30764=CARTESIAN_POINT('Ctrl Pts',(370.469392092768,-11.4749802039507,3.37165743917901));
#30765=CARTESIAN_POINT('Ctrl Pts',(370.57319629566,-11.4688848144959,3.37967758738546));
#30766=CARTESIAN_POINT('Ctrl Pts',(370.677021182592,-11.462788210473,3.38769933368773));
#30767=CARTESIAN_POINT('Ctrl Pts',(370.781190440714,-11.4566916064502,3.39093047427338));
#30768=CARTESIAN_POINT('Ctrl Pts',(370.885231289961,-11.4505950024273,3.38936762309131));
#30769=CARTESIAN_POINT('Ctrl Pts',(370.989380563611,-11.4444920449322,3.38780314321044));
#30770=CARTESIAN_POINT('Ctrl Pts',(371.093400735166,-11.4383890874371,3.38143470324141));
#30771=CARTESIAN_POINT('Ctrl Pts',(371.196821203217,-11.4322861299419,3.37031102181144));
#30772=CARTESIAN_POINT('Ctrl Pts',(371.300301437738,-11.4261796455606,3.35918091202953));
#30773=CARTESIAN_POINT('Ctrl Pts',(371.403180858199,-11.4200731611793,3.34329015203459));
#30774=CARTESIAN_POINT('Ctrl Pts',(371.504998040673,-11.413966676798,3.32273880235326));
#30775=CARTESIAN_POINT('Ctrl Pts',(371.606970257111,-11.4078508942563,3.30215615974923));
#30776=CARTESIAN_POINT('Ctrl Pts',(371.707876593251,-11.4017351117147,3.276898859421));
#30777=CARTESIAN_POINT('Ctrl Pts',(371.807269721178,-11.3956193291731,3.24711714065645));
#30778=CARTESIAN_POINT('Ctrl Pts',(371.860385531707,-11.3923510474167,3.23120175330404));
#30779=CARTESIAN_POINT('Ctrl Pts',(371.913069505805,-11.3890827656602,3.21399509497087));
#30780=CARTESIAN_POINT('Ctrl Pts',(371.965255865135,-11.3858144839038,3.19552566500655));
#30781=CARTESIAN_POINT('Ctrl Pts',(371.981082642912,-11.384823298281,3.18992436291385));
#30782=CARTESIAN_POINT('Ctrl Pts',(371.996872144802,-11.3838321126582,3.18420394249049));
#30783=CARTESIAN_POINT('Ctrl Pts',(372.012622422842,-11.3828409270354,3.17836489467751));
#30784=CARTESIAN_POINT('Origin',(370.834317853224,-8.23961502859548,0.));
#30785=CARTESIAN_POINT('',(366.749317961181,-12.6146150285594,0.000939151365601897));
#30786=CARTESIAN_POINT('Ctrl Pts',(373.320592904309,-11.8073874696441,-3.2412437998941));
#30787=CARTESIAN_POINT('Ctrl Pts',(373.416781140934,-11.813285821701,-3.16746026872723));
#30788=CARTESIAN_POINT('Ctrl Pts',(373.509749908528,-11.8191841737578,-3.08933937017736));
#30789=CARTESIAN_POINT('Ctrl Pts',(373.599093399365,-11.8250825258147,-3.00719822749649));
#30790=CARTESIAN_POINT('Ctrl Pts',(373.687265105201,-11.8309035180056,-2.92613440738434));
#30791=CARTESIAN_POINT('Ctrl Pts',(373.77190575925,-11.8367245101966,-2.84115545631612));
#30792=CARTESIAN_POINT('Ctrl Pts',(373.852659007258,-11.8425455023875,-2.75260634269847));
#30793=CARTESIAN_POINT('Ctrl Pts',(373.933401209199,-11.8483656983371,-2.66406934152782));
#30794=CARTESIAN_POINT('Ctrl Pts',(374.010256789676,-11.8541858942867,-2.5719634488751));
#30795=CARTESIAN_POINT('Ctrl Pts',(374.082907474943,-11.8600060902364,-2.4766692289559));
#30796=CARTESIAN_POINT('Ctrl Pts',(374.155565073807,-11.8658268400484,-2.38136594063285));
#30797=CARTESIAN_POINT('Ctrl Pts',(374.224016735994,-11.8716475898605,-2.2828740443364));
#30798=CARTESIAN_POINT('Ctrl Pts',(374.287985947505,-11.8774683396725,-2.18160530219018));
#30799=CARTESIAN_POINT('Ctrl Pts',(374.35344848064,-11.8834249712839,-2.07797250397809));
#30800=CARTESIAN_POINT('Ctrl Pts',(374.414216440752,-11.8893816028953,-1.9714319762906));
#30801=CARTESIAN_POINT('Ctrl Pts',(374.470042452942,-11.8953382345067,-1.86245312290073));
#30802=CARTESIAN_POINT('Ctrl Pts',(374.524671339382,-11.901167132884,-1.75581119788089));
#30803=CARTESIAN_POINT('Ctrl Pts',(374.574567975965,-11.9069960312612,-1.64683486665082));
#30804=CARTESIAN_POINT('Ctrl Pts',(374.619549142882,-11.9128249296384,-1.53598472772121));
#30805=CARTESIAN_POINT('Ctrl Pts',(374.666008871328,-11.9188454278669,-1.42149086938519));
#30806=CARTESIAN_POINT('Ctrl Pts',(374.707224259818,-11.9248659260954,-1.30499834529334));
#30807=CARTESIAN_POINT('Ctrl Pts',(374.743049388451,-11.9308864243239,-1.18703108026663));
#30808=CARTESIAN_POINT('Ctrl Pts',(374.778874517084,-11.9369069225524,-1.0690638152399));
#30809=CARTESIAN_POINT('Ctrl Pts',(374.809309328429,-11.9429274207809,-0.949622280235242));
#30810=CARTESIAN_POINT('Ctrl Pts',(374.834266080049,-11.9489479190094,-0.829240123678208));
#30811=CARTESIAN_POINT('Ctrl Pts',(374.858468388882,-11.9547864175316,-0.712497120611384));
#30812=CARTESIAN_POINT('Ctrl Pts',(374.877592108987,-11.9606249160538,-0.594517395874913));
#30813=CARTESIAN_POINT('Ctrl Pts',(374.891516289371,-11.9664634145759,-0.475779202702064));
#30814=CARTESIAN_POINT('Ctrl Pts',(374.905423635505,-11.9722948543886,-0.357184563289714));
#30815=CARTESIAN_POINT('Ctrl Pts',(374.914143900232,-11.9781262942012,-0.237833679427054));
#30816=CARTESIAN_POINT('Ctrl Pts',(374.917606972006,-11.9839577340138,-0.118215787594323));
#30817=CARTESIAN_POINT('Ctrl Pts',(374.921066744893,-11.9897836188555,0.00128815743634286));
#30818=CARTESIAN_POINT('Ctrl Pts',(374.919279277512,-11.9956095036971,0.121058200836194));
#30819=CARTESIAN_POINT('Ctrl Pts',(374.912226234157,-12.0014353885387,0.240599743798495));
#30820=CARTESIAN_POINT('Ctrl Pts',(374.905142998665,-12.0072862123897,0.360653011199787));
#30821=CARTESIAN_POINT('Ctrl Pts',(374.892748956364,-12.0131370362406,0.480475405878789));
#30822=CARTESIAN_POINT('Ctrl Pts',(374.875078489537,-12.0189878600916,0.599565242504155));
#30823=CARTESIAN_POINT('Ctrl Pts',(374.857501492598,-12.0248077353632,0.71802514027771));
#30824=CARTESIAN_POINT('Ctrl Pts',(374.834703826155,-12.0306276106347,0.835759807168469));
#30825=CARTESIAN_POINT('Ctrl Pts',(374.806771267674,-12.0364474859063,0.952280877696166));
#30826=CARTESIAN_POINT('Ctrl Pts',(374.778842205623,-12.0422666326808,1.06878736281487));
#30827=CARTESIAN_POINT('Ctrl Pts',(374.745779624748,-12.0480857794553,1.18408015929471));
#30828=CARTESIAN_POINT('Ctrl Pts',(374.707720126321,-12.0539049262298,1.29768248457338));
#30829=CARTESIAN_POINT('Ctrl Pts',(374.669656554385,-12.0597246958277,1.41129696871103));
#30830=CARTESIAN_POINT('Ctrl Pts',(374.626595130418,-12.0655444654256,1.52322023718578));
#30831=CARTESIAN_POINT('Ctrl Pts',(374.578721698208,-12.0713642350235,1.63299260429113));
#30832=CARTESIAN_POINT('Ctrl Pts',(374.53040016091,-12.0772384788517,1.74379246313863));
#30833=CARTESIAN_POINT('Ctrl Pts',(374.477176225592,-12.0831127226798,1.85240055634729));
#30834=CARTESIAN_POINT('Ctrl Pts',(374.41928935173,-12.088986966508,1.95836777825303));
#30835=CARTESIAN_POINT('Ctrl Pts',(374.361858438797,-12.0948149403358,2.06350032193764));
#30836=CARTESIAN_POINT('Ctrl Pts',(374.299838045423,-12.1006429141637,2.16603312997207));
#30837=CARTESIAN_POINT('Ctrl Pts',(374.233506141718,-12.1064708879916,2.26555599784294));
#30838=CARTESIAN_POINT('Ctrl Pts',(374.166384295241,-12.1123682668199,2.36626407774338));
#30839=CARTESIAN_POINT('Ctrl Pts',(374.094847833739,-12.1182656456482,2.46388971553068));
#30840=CARTESIAN_POINT('Ctrl Pts',(374.019226672328,-12.1241630244765,2.55804237924118));
#30841=CARTESIAN_POINT('Ctrl Pts',(373.943605510917,-12.1300604033048,2.65219504295168));
#30842=CARTESIAN_POINT('Ctrl Pts',(373.863899971763,-12.1359577821331,2.74287445019914));
#30843=CARTESIAN_POINT('Ctrl Pts',(373.780477569685,-12.1418551609614,2.82972930244228));
#30844=CARTESIAN_POINT('Ctrl Pts',(373.697882115775,-12.1476940803532,2.91572318138476));
#30845=CARTESIAN_POINT('Ctrl Pts',(373.6113939645,-12.1535329997451,2.99822749085314));
#30846=CARTESIAN_POINT('Ctrl Pts',(373.521339213008,-12.159371919137,3.07687198499739));
#30847=CARTESIAN_POINT('Ctrl Pts',(373.431393249344,-12.1652037850048,3.15542147511918));
#30848=CARTESIAN_POINT('Ctrl Pts',(373.337889559631,-12.1710356508726,3.23012016079347));
#30849=CARTESIAN_POINT('Ctrl Pts',(373.241192047349,-12.1768675167404,3.30063351701688));
#30850=CARTESIAN_POINT('Ctrl Pts',(373.144586565468,-12.1826938322177,3.37107976321517));
#30851=CARTESIAN_POINT('Ctrl Pts',(373.044793635231,-12.188520147695,3.43734836784025));
#30852=CARTESIAN_POINT('Ctrl Pts',(372.942210860599,-12.1943464631723,3.49914447679125));
#30853=CARTESIAN_POINT('Ctrl Pts',(372.83919938364,-12.2001971273282,3.56119883705051));
#30854=CARTESIAN_POINT('Ctrl Pts',(372.733375005362,-12.2060477914841,3.61874296561396));
#30855=CARTESIAN_POINT('Ctrl Pts',(372.625170852556,-12.2118984556399,3.67152155581092));
#30856=CARTESIAN_POINT('Ctrl Pts',(372.517528002055,-12.2177187698398,3.72402636035735));
#30857=CARTESIAN_POINT('Ctrl Pts',(372.407530380524,-12.2235390840396,3.77181477977987));
#30858=CARTESIAN_POINT('Ctrl Pts',(372.295629324332,-12.2293593982395,3.81468134768921));
#30859=CARTESIAN_POINT('Ctrl Pts',(372.183742230063,-12.2351789862372,3.85754256712574));
#30860=CARTESIAN_POINT('Ctrl Pts',(372.069952552326,-12.2409985742349,3.89548301161378));
#30861=CARTESIAN_POINT('Ctrl Pts',(371.954730816777,-12.2468181622326,3.92834568121259));
#30862=CARTESIAN_POINT('Ctrl Pts',(371.839496714967,-12.2526383748221,3.96121187782273));
#30863=CARTESIAN_POINT('Ctrl Pts',(371.722830639862,-12.2584585874116,3.98899910471113));
#30864=CARTESIAN_POINT('Ctrl Pts',(371.605216865551,-12.2642788000011,4.01160064223666));
#30865=CARTESIAN_POINT('Ctrl Pts',(371.486523569872,-12.2701524335771,4.03440962861617));
#30866=CARTESIAN_POINT('Ctrl Pts',(371.366865501073,-12.2760260671531,4.05193715902417));
#30867=CARTESIAN_POINT('Ctrl Pts',(371.246748258264,-12.2818997007292,4.0641267402725));
#30868=CARTESIAN_POINT('Ctrl Pts',(371.127555703666,-12.2877281178184,4.07622248351881));
#30869=CARTESIAN_POINT('Ctrl Pts',(371.007911431417,-12.2935565349076,4.08306221230075));
#30870=CARTESIAN_POINT('Ctrl Pts',(370.888311011204,-12.2993849519968,4.08464315930915));
#30871=CARTESIAN_POINT('Ctrl Pts',(370.767318812382,-12.3052811938163,4.08624250364613));
#30872=CARTESIAN_POINT('Ctrl Pts',(370.646371920567,-12.3111774356357,4.08245991020879));
#30873=CARTESIAN_POINT('Ctrl Pts',(370.525978655253,-12.3170736774551,4.07334652822396));
#30874=CARTESIAN_POINT('Ctrl Pts',(370.405585389938,-12.3229699192745,4.06423314623914));
#30875=CARTESIAN_POINT('Ctrl Pts',(370.285746165596,-12.3288661610939,4.04978908149056));
#30876=CARTESIAN_POINT('Ctrl Pts',(370.166958227814,-12.3347624029133,4.03011862485116));
#30877=CARTESIAN_POINT('Ctrl Pts',(370.049325495705,-12.3406013041295,4.01063946223983));
#30878=CARTESIAN_POINT('Ctrl Pts',(369.932368949583,-12.3464402053458,3.98597640810493));
#30879=CARTESIAN_POINT('Ctrl Pts',(369.816578360685,-12.352279106562,3.95618899009212));
#30880=CARTESIAN_POINT('Ctrl Pts',(369.700927635187,-12.3581109549722,3.92643755228791));
#30881=CARTESIAN_POINT('Ctrl Pts',(369.586440455055,-12.3639428033823,3.89157416417475));
#30882=CARTESIAN_POINT('Ctrl Pts',(369.473598515069,-12.3697746517924,3.85170973500986));
#30883=CARTESIAN_POINT('Ctrl Pts',(369.360863956748,-12.3756009505497,3.81188324128655));
#30884=CARTESIAN_POINT('Ctrl Pts',(369.249771903986,-12.3814272493069,3.7670653101199));
#30885=CARTESIAN_POINT('Ctrl Pts',(369.140790395302,-12.3872535480642,3.7174170803481));
#30886=CARTESIAN_POINT('Ctrl Pts',(369.031353006958,-12.3931042187642,3.66756116747138));
#30887=CARTESIAN_POINT('Ctrl Pts',(368.924044259686,-12.3989548894643,3.61283455966244));
#30888=CARTESIAN_POINT('Ctrl Pts',(368.819319673422,-12.4048055601643,3.55345006091209));
#30889=CARTESIAN_POINT('Ctrl Pts',(368.715138720673,-12.4106258595754,3.49437383173733));
#30890=CARTESIAN_POINT('Ctrl Pts',(368.613515515265,-12.4164461589864,3.43068816584515));
#30891=CARTESIAN_POINT('Ctrl Pts',(368.514874767661,-12.4222664583974,3.36264907072311));
#30892=CARTESIAN_POINT('Ctrl Pts',(368.416246314658,-12.4280860323653,3.2946184560065));
#30893=CARTESIAN_POINT('Ctrl Pts',(368.32059991382,-12.4339056063331,3.22223572178511));
#30894=CARTESIAN_POINT('Ctrl Pts',(368.228331158398,-12.439725180301,3.14580011227508));
#30895=CARTESIAN_POINT('Ctrl Pts',(368.136052487785,-12.4455453796397,3.06935628900222));
#30896=CARTESIAN_POINT('Ctrl Pts',(368.047152496659,-12.4513655789783,2.98885898329061));
#30897=CARTESIAN_POINT('Ctrl Pts',(367.961993087948,-12.457185778317,2.90464721485749));
#30898=CARTESIAN_POINT('Ctrl Pts',(367.87605152407,-12.4630594338627,2.81966199495578));
#30899=CARTESIAN_POINT('Ctrl Pts',(367.793919909523,-12.4689330894084,2.73089402274613));
#30900=CARTESIAN_POINT('Ctrl Pts',(367.715930792127,-12.4748067449541,2.63872831818381));
#30901=CARTESIAN_POINT('Ctrl Pts',(367.638542489789,-12.4806351508442,2.54727264272517));
#30902=CARTESIAN_POINT('Ctrl Pts',(367.565233284147,-12.4864635567344,2.45247176293892));
#30903=CARTESIAN_POINT('Ctrl Pts',(367.49628573707,-12.4922919626245,2.35473280682202));
#30904=CARTESIAN_POINT('Ctrl Pts',(367.426535263906,-12.498188242998,2.25585563533917));
#30905=CARTESIAN_POINT('Ctrl Pts',(367.361248913144,-12.5040845233714,2.153971882455));
#30906=CARTESIAN_POINT('Ctrl Pts',(367.300671998537,-12.5099808037449,2.04952969572403));
#30907=CARTESIAN_POINT('Ctrl Pts',(367.24009508393,-12.5158770841183,1.94508750899306));
#30908=CARTESIAN_POINT('Ctrl Pts',(367.184227752654,-12.5217733644918,1.83808729008043));
#30909=CARTESIAN_POINT('Ctrl Pts',(367.133265227715,-12.5276696448652,1.72899810966225));
#30910=CARTESIAN_POINT('Ctrl Pts',(367.079121526908,-12.533933982058,1.61309937911611));
#30911=CARTESIAN_POINT('Ctrl Pts',(367.030369879211,-12.5401983192508,1.49453584255141));
#30912=CARTESIAN_POINT('Ctrl Pts',(366.987258854716,-12.5464626564436,1.37381296470686));
#30913=CARTESIAN_POINT('Ctrl Pts',(366.944274342146,-12.5527086105576,1.25344435549594));
#30914=CARTESIAN_POINT('Ctrl Pts',(366.906897545925,-12.5589545646716,1.13092933426704));
#30915=CARTESIAN_POINT('Ctrl Pts',(366.875328960634,-12.5652005187856,1.00679290241326));
#30916=CARTESIAN_POINT('Ctrl Pts',(366.843818211393,-12.5714350298365,0.882883897947502));
#30917=CARTESIAN_POINT('Ctrl Pts',(366.818094544775,-12.5776695408873,0.757359701769412));
#30918=CARTESIAN_POINT('Ctrl Pts',(366.798309421592,-12.5839040519381,0.630762189572842));
#30919=CARTESIAN_POINT('Ctrl Pts',(366.778578298236,-12.5901215470465,0.504510201823112));
#30920=CARTESIAN_POINT('Ctrl Pts',(366.764753447751,-12.5963390421549,0.377191045207156));
#30921=CARTESIAN_POINT('Ctrl Pts',(366.75693562444,-12.6025565372633,0.249357495166076));
#30922=CARTESIAN_POINT('Ctrl Pts',(366.751881544369,-12.606576034362,0.166715438429602));
#30923=CARTESIAN_POINT('Ctrl Pts',(366.749337024585,-12.6105955314607,0.0838586970475943));
#30924=CARTESIAN_POINT('Ctrl Pts',(366.749317961181,-12.6146150285594,0.000939151365612782));
#30925=CARTESIAN_POINT('Ctrl Pts',(366.74931796118,-12.6146150285955,0.00093915062137102));
#30926=CARTESIAN_POINT('Ctrl Pts',(366.749289612733,-12.6205922712843,-0.122367381518829));
#30927=CARTESIAN_POINT('Ctrl Pts',(366.754848656197,-12.6265695139731,-0.245621759676924));
#30928=CARTESIAN_POINT('Ctrl Pts',(366.76595478391,-12.6325467566619,-0.368302777942603));
#30929=CARTESIAN_POINT('Ctrl Pts',(366.777068607145,-12.6385281410287,-0.491068802841755));
#30930=CARTESIAN_POINT('Ctrl Pts',(366.79373714086,-12.6445095253955,-0.613260304939521));
#30931=CARTESIAN_POINT('Ctrl Pts',(366.815868431614,-12.6504909097623,-0.734363156729659));
#30932=CARTESIAN_POINT('Ctrl Pts',(366.83803627101,-12.6564821720652,-0.855666003395637));
#30933=CARTESIAN_POINT('Ctrl Pts',(366.865684827507,-12.662473434368,-0.97587623954742));
#30934=CARTESIAN_POINT('Ctrl Pts',(366.898671177634,-12.6684646966709,-1.09449086104898));
#30935=CARTESIAN_POINT('Ctrl Pts',(366.931685318874,-12.6744610066327,-1.21320541577318));
#30936=CARTESIAN_POINT('Ctrl Pts',(366.970046106514,-12.6804573165944,-1.33032132056031));
#30937=CARTESIAN_POINT('Ctrl Pts',(367.013561534935,-12.6864536265562,-1.44535329807331));
#30938=CARTESIAN_POINT('Ctrl Pts',(367.057161999254,-12.6924616542379,-1.56061006591746));
#30939=CARTESIAN_POINT('Ctrl Pts',(367.105937094125,-12.6984696819197,-1.67377442208256));
#30940=CARTESIAN_POINT('Ctrl Pts',(367.159647196542,-12.7044777096014,-1.78438240434055));
#30941=CARTESIAN_POINT('Ctrl Pts',(367.20762125741,-12.7098441020066,-1.88317786058538));
#30942=CARTESIAN_POINT('Ctrl Pts',(367.259531793322,-12.7152104944119,-1.9799339922456));
#30943=CARTESIAN_POINT('Ctrl Pts',(367.315178694938,-12.7205768868172,-2.07433955383816));
#30944=CARTESIAN_POINT('Ctrl Pts',(367.375724918107,-12.7264157526434,-2.17705686665494));
#30945=CARTESIAN_POINT('Ctrl Pts',(367.440863361581,-12.7322546184696,-2.27727604182428));
#30946=CARTESIAN_POINT('Ctrl Pts',(367.510362071704,-12.7380934842958,-2.37456163586078));
#30947=CARTESIAN_POINT('Ctrl Pts',(367.579776823804,-12.7439252964713,-2.47172970388697));
#30948=CARTESIAN_POINT('Ctrl Pts',(367.653541130018,-12.7497571086467,-2.5659709132208));
#30949=CARTESIAN_POINT('Ctrl Pts',(367.73137801369,-12.7555889208222,-2.65687586315837));
#30950=CARTESIAN_POINT('Ctrl Pts',(367.809140815875,-12.7614151825529,-2.7476942940379));
#30951=CARTESIAN_POINT('Ctrl Pts',(367.89096822068,-12.7672414442837,-2.83518247686381));
#30952=CARTESIAN_POINT('Ctrl Pts',(367.976541313123,-12.7730677060145,-2.918961844021));
#30953=CARTESIAN_POINT('Ctrl Pts',(368.062473111248,-12.7789183902959,-3.00309239791412));
#30954=CARTESIAN_POINT('Ctrl Pts',(368.152181827448,-12.7847690745773,-3.08348263761303));
#30955=CARTESIAN_POINT('Ctrl Pts',(368.245304849742,-12.7906197588588,-3.15978427551634));
#30956=CARTESIAN_POINT('Ctrl Pts',(368.337943631764,-12.796440019547,-3.23568914444657));
#30957=CARTESIAN_POINT('Ctrl Pts',(368.433960972766,-12.8022602802352,-3.30754757947248));
#30958=CARTESIAN_POINT('Ctrl Pts',(368.532965065346,-12.8080805409234,-3.37505560631587));
#30959=CARTESIAN_POINT('Ctrl Pts',(368.631956808287,-12.8139000756001,-3.4425552122984));
#30960=CARTESIAN_POINT('Ctrl Pts',(368.733934226552,-12.8197196102768,-3.50570526114235));
#30961=CARTESIAN_POINT('Ctrl Pts',(368.838475667358,-12.8255391449535,-3.56424451589903));
#30962=CARTESIAN_POINT('Ctrl Pts',(368.943028332845,-12.8313593044774,-3.62279005605317));
#30963=CARTESIAN_POINT('Ctrl Pts',(369.050145214291,-12.8371794640013,-3.6767236195874));
#30964=CARTESIAN_POINT('Ctrl Pts',(369.159379689806,-12.8429996235251,-3.72582972621208));
#30965=CARTESIAN_POINT('Ctrl Pts',(369.269619193418,-12.8488733322955,-3.77538764090064));
#30966=CARTESIAN_POINT('Ctrl Pts',(369.382015076121,-12.8547470410658,-3.82002863338509));
#30967=CARTESIAN_POINT('Ctrl Pts',(369.496088355519,-12.8606207498361,-3.85958117047339));
#30968=CARTESIAN_POINT('Ctrl Pts',(369.609281016511,-12.866449114981,-3.89882837144481));
#30969=CARTESIAN_POINT('Ctrl Pts',(369.72412485796,-12.8722774801259,-3.93306534577048));
#30970=CARTESIAN_POINT('Ctrl Pts',(369.840138302784,-12.8781058452708,-3.96217516289817));
#30971=CARTESIAN_POINT('Ctrl Pts',(369.957505592998,-12.8840022258538,-3.99162468368515));
#30972=CARTESIAN_POINT('Ctrl Pts',(370.076069538853,-12.8898986064369,-4.01582653432596));
#30973=CARTESIAN_POINT('Ctrl Pts',(370.195323679133,-12.8957949870199,-4.03471330400041));
#30974=CARTESIAN_POINT('Ctrl Pts',(370.314577819413,-12.901691367603,-4.05360007367485));
#30975=CARTESIAN_POINT('Ctrl Pts',(370.434521726344,-12.907587748186,-4.06717176978063));
#30976=CARTESIAN_POINT('Ctrl Pts',(370.554647464531,-12.9134841287691,-4.0754152516876));
#30977=CARTESIAN_POINT('Ctrl Pts',(370.676637201473,-12.9194720038664,-4.08378664823011));
#30978=CARTESIAN_POINT('Ctrl Pts',(370.79919182361,-12.9254598789638,-4.08668894203072));
#30979=CARTESIAN_POINT('Ctrl Pts',(370.921782419112,-12.9314477540612,-4.08406353399574));
#30980=CARTESIAN_POINT('Ctrl Pts',(371.041157801345,-12.9372785837067,-4.08150698317379));
#30981=CARTESIAN_POINT('Ctrl Pts',(371.160566852821,-12.9431094133522,-4.07370905134738));
#30982=CARTESIAN_POINT('Ctrl Pts',(371.279515472225,-12.9489402429977,-4.06066793520912));
#30983=CARTESIAN_POINT('Ctrl Pts',(371.398360288104,-12.9547659842221,-4.04763819973106));
#30984=CARTESIAN_POINT('Ctrl Pts',(371.516745070039,-12.9605917254464,-4.02937442427085));
#30985=CARTESIAN_POINT('Ctrl Pts',(371.634177461656,-12.9664174666708,-4.00592680996524));
#30986=CARTESIAN_POINT('Ctrl Pts',(371.751534635918,-12.9722394764132,-3.98249421423779));
#30987=CARTESIAN_POINT('Ctrl Pts',(371.867940236911,-12.9780614861556,-3.95388446452583));
#30988=CARTESIAN_POINT('Ctrl Pts',(371.982909365183,-12.983883495898,-3.92019929833372));
#30989=CARTESIAN_POINT('Ctrl Pts',(372.103548474738,-12.9899926321653,-3.88485286650701));
#30990=CARTESIAN_POINT('Ctrl Pts',(372.222605346488,-12.9961017684327,-3.84391770095398));
#30991=CARTESIAN_POINT('Ctrl Pts',(372.339534650271,-13.0022109047,-3.79757124934956));
#30992=CARTESIAN_POINT('Ctrl Pts',(372.45092388261,-13.0080305921269,-3.75342067717669));
#30993=CARTESIAN_POINT('Ctrl Pts',(372.56038212615,-13.0138502795537,-3.70436000839369));
#30994=CARTESIAN_POINT('Ctrl Pts',(372.667456912096,-13.0196699669806,-3.65059258077859));
#30995=CARTESIAN_POINT('Ctrl Pts',(372.774535253417,-13.0254898476478,-3.59682336783856));
#30996=CARTESIAN_POINT('Ctrl Pts',(372.879229620213,-13.031309728315,-3.53834727302077));
#30997=CARTESIAN_POINT('Ctrl Pts',(372.981111631913,-13.0371296089822,-3.47541385618776));
#30998=CARTESIAN_POINT('Ctrl Pts',(373.083044319446,-13.042952384442,-3.41244913644588));
#30999=CARTESIAN_POINT('Ctrl Pts',(373.182161519185,-13.0487751599019,-3.34502288954575));
#31000=CARTESIAN_POINT('Ctrl Pts',(373.278063575703,-13.0545979353618,-3.27342814857261));
#31001=CARTESIAN_POINT('Ctrl Pts',(373.292311340686,-13.0554630006097,-3.26279161917505));
#31002=CARTESIAN_POINT('Ctrl Pts',(373.306488199698,-13.0563280658577,-3.2520631573204));
#31003=CARTESIAN_POINT('Ctrl Pts',(373.320592904309,-13.0571931311057,-3.2412437998941));
#31004=CARTESIAN_POINT('',(366.749318884821,-12.5103849713753,-0.00290312669601772));
#31005=CARTESIAN_POINT('Ctrl Pts',(366.749318884821,-12.5103849714045,-0.00290312729419502));
#31006=CARTESIAN_POINT('Ctrl Pts',(366.749446060986,-12.5191195890899,-0.181853083703761));
#31007=CARTESIAN_POINT('Ctrl Pts',(366.7613354519,-12.5278542067754,-0.360374148224009));
#31008=CARTESIAN_POINT('Ctrl Pts',(366.784798877521,-12.5365888244608,-0.537234646521026));
#31009=CARTESIAN_POINT('Ctrl Pts',(366.790770525782,-12.5388118615124,-0.582247199425974));
#31010=CARTESIAN_POINT('Ctrl Pts',(366.797491656539,-12.5410348985639,-0.627152337215535));
#31011=CARTESIAN_POINT('Ctrl Pts',(366.804958714245,-12.5432579356155,-0.671930003142868));
#31012=CARTESIAN_POINT('Ctrl Pts',(366.824571319474,-12.5490968550161,-0.789540810446197));
#31013=CARTESIAN_POINT('Ctrl Pts',(366.849367068929,-12.5549357744167,-0.906469559074163));
#31014=CARTESIAN_POINT('Ctrl Pts',(366.879285881915,-12.5607746938174,-1.02222654334833));
#31015=CARTESIAN_POINT('Ctrl Pts',(366.909168552415,-12.5666065596941,-1.13784369101978));
#31016=CARTESIAN_POINT('Ctrl Pts',(366.944161874345,-12.5724384255709,-1.25229150054339));
#31017=CARTESIAN_POINT('Ctrl Pts',(366.984154394552,-12.5782702914476,-1.36508840061911));
#31018=CARTESIAN_POINT('Ctrl Pts',(367.02410885248,-12.584096606934,-1.47777794794653));
#31019=CARTESIAN_POINT('Ctrl Pts',(367.069052906905,-12.5899229224203,-1.58881933170769));
#31020=CARTESIAN_POINT('Ctrl Pts',(367.118824890523,-12.5957492379067,-1.69774469344546));
#31021=CARTESIAN_POINT('Ctrl Pts',(367.168804875479,-12.6015999020592,-1.80712526350073));
#31022=CARTESIAN_POINT('Ctrl Pts',(367.223653126755,-12.6074505662118,-1.91437168577231));
#31023=CARTESIAN_POINT('Ctrl Pts',(367.283156328575,-12.6133012303643,-2.01902868376213));
#31024=CARTESIAN_POINT('Ctrl Pts',(367.34235086137,-12.6191215445735,-2.12314278031752));
#31025=CARTESIAN_POINT('Ctrl Pts',(367.406151954314,-12.6249418587826,-2.22469390223052));
#31026=CARTESIAN_POINT('Ctrl Pts',(367.474303120528,-12.6307621729918,-2.32325762584969));
#31027=CARTESIAN_POINT('Ctrl Pts',(367.542445783505,-12.636581760999,-2.42180905164888));
#31028=CARTESIAN_POINT('Ctrl Pts',(367.614937209356,-12.6424013490061,-2.51737348705528));
#31029=CARTESIAN_POINT('Ctrl Pts',(367.691477707239,-12.6482209370132,-2.60955567420667));
#31030=CARTESIAN_POINT('Ctrl Pts',(367.768026419891,-12.6540411496122,-2.70174775488331));
#31031=CARTESIAN_POINT('Ctrl Pts',(367.84862480948,-12.6598613622112,-2.79055655344866));
#31032=CARTESIAN_POINT('Ctrl Pts',(367.932933447541,-12.6656815748101,-2.87562054702316));
#31033=CARTESIAN_POINT('Ctrl Pts',(368.018015914505,-12.6715552083733,-2.96146530254966));
#31034=CARTESIAN_POINT('Ctrl Pts',(368.10687679585,-12.6774288419364,-3.04349585450657));
#31035=CARTESIAN_POINT('Ctrl Pts',(368.199130702685,-12.6833024754995,-3.12138009246459));
#31036=CARTESIAN_POINT('Ctrl Pts',(368.290674419577,-12.6891308925982,-3.19866476120734));
#31037=CARTESIAN_POINT('Ctrl Pts',(368.38555874387,-12.694959309697,-3.27186652911053));
#31038=CARTESIAN_POINT('Ctrl Pts',(368.483376228154,-12.7007877267958,-3.34070329055355));
#31039=CARTESIAN_POINT('Ctrl Pts',(368.582332004546,-12.7066839685911,-3.41034109838219));
#31040=CARTESIAN_POINT('Ctrl Pts',(368.684289279658,-12.7125802103864,-3.47551143355884));
#31041=CARTESIAN_POINT('Ctrl Pts',(368.788799639473,-12.7184764521816,-3.53596949042426));
#31042=CARTESIAN_POINT('Ctrl Pts',(368.893309999287,-12.7243726939769,-3.59642754728969));
#31043=CARTESIAN_POINT('Ctrl Pts',(369.000373041996,-12.7302689357721,-3.65217317911992));
#31044=CARTESIAN_POINT('Ctrl Pts',(369.109519486997,-12.7361651775674,-3.70301169264453));
#31045=CARTESIAN_POINT('Ctrl Pts',(369.217604489732,-12.7420040787845,-3.75335580484406));
#31046=CARTESIAN_POINT('Ctrl Pts',(369.328058479929,-12.7478429800017,-3.79903967485439));
#31047=CARTESIAN_POINT('Ctrl Pts',(369.440443621202,-12.7536818812188,-3.83983588520469));
#31048=CARTESIAN_POINT('Ctrl Pts',(369.552693012516,-12.7595137296299,-3.88058281783165));
#31049=CARTESIAN_POINT('Ctrl Pts',(369.666868536215,-12.765345578041,-3.91645369797176));
#31050=CARTESIAN_POINT('Ctrl Pts',(369.782510009237,-12.7711774264521,-3.94726807543239));
#31051=CARTESIAN_POINT('Ctrl Pts',(369.898041436527,-12.7770037252104,-3.97805312958341));
#31052=CARTESIAN_POINT('Ctrl Pts',(370.015035647441,-12.7828300239686,-4.00379115130258));
#31053=CARTESIAN_POINT('Ctrl Pts',(370.13301536792,-12.7886563227269,-4.02435085748074));
#31054=CARTESIAN_POINT('Ctrl Pts',(370.251488608377,-12.7945069934266,-4.04499656679313));
#31055=CARTESIAN_POINT('Ctrl Pts',(370.370955231997,-12.8003576641263,-4.06042040174536));
#31056=CARTESIAN_POINT('Ctrl Pts',(370.490919124178,-12.806208334826,-4.07054078875142));
#31057=CARTESIAN_POINT('Ctrl Pts',(370.610260274447,-12.8120286342382,-4.08060864004006));
#31058=CARTESIAN_POINT('Ctrl Pts',(370.730093133838,-12.8178489336505,-4.08542794862778));
#31059=CARTESIAN_POINT('Ctrl Pts',(370.849922621117,-12.8236692330628,-4.08497019465488));
#31060=CARTESIAN_POINT('Ctrl Pts',(370.969737172828,-12.8294888070319,-4.08451249773653));
#31061=CARTESIAN_POINT('Ctrl Pts',(371.089547947681,-12.835308381001,-4.07877904825922));
#31062=CARTESIAN_POINT('Ctrl Pts',(371.20885948237,-12.8411279549701,-4.06779345198799));
#31063=CARTESIAN_POINT('Ctrl Pts',(371.328183838266,-12.8469481543101,-4.05680667520559));
#31064=CARTESIAN_POINT('Ctrl Pts',(371.447008443368,-12.8527683536501,-4.04056666664336));
#31065=CARTESIAN_POINT('Ctrl Pts',(371.564843181007,-12.8585885529901,-4.01914888321729));
#31066=CARTESIAN_POINT('Ctrl Pts',(371.683760183603,-12.8644622085342,-3.99753438601298));
#31067=CARTESIAN_POINT('Ctrl Pts',(371.801668627411,-12.8703358640783,-3.97064658452506));
#31068=CARTESIAN_POINT('Ctrl Pts',(371.918076649626,-12.8762095196224,-3.93861547643594));
#31069=CARTESIAN_POINT('Ctrl Pts',(372.033587884055,-12.882037925514,-3.90683113060565));
#31070=CARTESIAN_POINT('Ctrl Pts',(372.147621363606,-12.8878663314056,-3.86998263011797));
#31071=CARTESIAN_POINT('Ctrl Pts',(372.259713997293,-12.8936947372973,-3.82824644353939));
#31072=CARTESIAN_POINT('Ctrl Pts',(372.373112001475,-12.8995910176676,-3.78602421979034));
#31073=CARTESIAN_POINT('Ctrl Pts',(372.484523274168,-12.9054872980379,-3.73879991462816));
#31074=CARTESIAN_POINT('Ctrl Pts',(372.593492304934,-12.9113835784083,-3.68680488342551));
#31075=CARTESIAN_POINT('Ctrl Pts',(372.7024613357,-12.9172798587786,-3.63480985222286));
#31076=CARTESIAN_POINT('Ctrl Pts',(372.808987776272,-12.923176139149,-3.57804434338448));
#31077=CARTESIAN_POINT('Ctrl Pts',(372.912645643586,-12.9290724195193,-3.51678526438691));
#31078=CARTESIAN_POINT('Ctrl Pts',(373.015293460927,-12.934911246095,-3.45612309841373));
#31079=CARTESIAN_POINT('Ctrl Pts',(373.115438001154,-12.9407500726706,-3.39087160201834));
#31080=CARTESIAN_POINT('Ctrl Pts',(373.212644085742,-12.9465888992462,-3.32126321325414));
#31081=CARTESIAN_POINT('Ctrl Pts',(373.249046223612,-12.9487754472479,-3.29519597502075));
#31082=CARTESIAN_POINT('Ctrl Pts',(373.285036497378,-12.9509619952495,-3.26851820839758));
#31083=CARTESIAN_POINT('Ctrl Pts',(373.320592904309,-12.9531485432512,-3.2412437998941));
#31084=CARTESIAN_POINT('Ctrl Pts',(373.320592904309,-11.7029891890582,-3.2412437998941));
#31085=CARTESIAN_POINT('Ctrl Pts',(373.415815346343,-11.7088227556447,-3.16820110500659));
#31086=CARTESIAN_POINT('Ctrl Pts',(373.507775120479,-11.7146563222311,-3.09099036517938));
#31087=CARTESIAN_POINT('Ctrl Pts',(373.596103007177,-11.7204898888176,-3.00994481069077));
#31088=CARTESIAN_POINT('Ctrl Pts',(373.684473431876,-11.7263262648029,-2.92886022531356));
#31089=CARTESIAN_POINT('Ctrl Pts',(373.769208197034,-11.7321626407882,-2.84393743064286));
#31090=CARTESIAN_POINT('Ctrl Pts',(373.849975623245,-11.7379990167735,-2.75554590128941));
#31091=CARTESIAN_POINT('Ctrl Pts',(373.930867304975,-11.74384437165,-2.66701838722159));
#31092=CARTESIAN_POINT('Ctrl Pts',(374.007779190319,-11.7496897265265,-2.57501178458781));
#31093=CARTESIAN_POINT('Ctrl Pts',(374.080420124952,-11.7555350814029,-2.47992843475072));
#31094=CARTESIAN_POINT('Ctrl Pts',(374.147087018295,-11.7608997102045,-2.39266480613139));
#31095=CARTESIAN_POINT('Ctrl Pts',(374.210156927106,-11.7662643390061,-2.30281024446178));
#31096=CARTESIAN_POINT('Ctrl Pts',(374.26943825272,-11.7716289678077,-2.21069510357402));
#31097=CARTESIAN_POINT('Ctrl Pts',(374.333919787428,-11.7774641864821,-2.11049954295302));
#31098=CARTESIAN_POINT('Ctrl Pts',(374.394112426899,-11.7832994051564,-2.00732742361212));
#31099=CARTESIAN_POINT('Ctrl Pts',(374.449731386498,-11.7891346238308,-1.90158091687371));
#31100=CARTESIAN_POINT('Ctrl Pts',(374.505282665015,-11.7949627417986,-1.7959630899606));
#31101=CARTESIAN_POINT('Ctrl Pts',(374.556271147337,-11.8007908597663,-1.68777746407828));
#31102=CARTESIAN_POINT('Ctrl Pts',(374.602455514835,-11.8066189777341,-1.5774547737256));
#31103=CARTESIAN_POINT('Ctrl Pts',(374.648595566398,-11.8124415033659,-1.46723794285413));
#31104=CARTESIAN_POINT('Ctrl Pts',(374.689940518865,-11.8182640289977,-1.35488850035528));
#31105=CARTESIAN_POINT('Ctrl Pts',(374.726295422058,-11.8240865546295,-1.24086083171895));
#31106=CARTESIAN_POINT('Ctrl Pts',(374.762834789011,-11.8299386235933,-1.12625458988658));
#31107=CARTESIAN_POINT('Ctrl Pts',(374.794333134061,-11.835790692557,-1.00995341201883));
#31108=CARTESIAN_POINT('Ctrl Pts',(374.820641806603,-11.8416427615208,-0.892438422924913));
#31109=CARTESIAN_POINT('Ctrl Pts',(374.846790335786,-11.8474592083914,-0.775638758602226));
#31110=CARTESIAN_POINT('Ctrl Pts',(374.867812118546,-11.8532756552619,-0.657640422919713));
#31111=CARTESIAN_POINT('Ctrl Pts',(374.883611621838,-11.8590921021325,-0.538929471695475));
#31112=CARTESIAN_POINT('Ctrl Pts',(374.899409092739,-11.8649078007963,-0.420233791019374));
#31113=CARTESIAN_POINT('Ctrl Pts',(374.909985566918,-11.8707234994602,-0.300826079803791));
#31114=CARTESIAN_POINT('Ctrl Pts',(374.915297099379,-11.876539198124,-0.181199868791646));
#31115=CARTESIAN_POINT('Ctrl Pts',(374.920609186343,-11.882355503923,-0.0615611692937222));
#31116=CARTESIAN_POINT('Ctrl Pts',(374.920655220787,-11.8881718097219,0.0582956694610412));
#31117=CARTESIAN_POINT('Ctrl Pts',(374.915443354271,-11.8939881155208,0.177875362829974));
#31118=CARTESIAN_POINT('Ctrl Pts',(374.910175301793,-11.8998671233741,0.298744172123527));
#31119=CARTESIAN_POINT('Ctrl Pts',(374.899535319673,-11.9057461312273,0.419329400749526));
#31120=CARTESIAN_POINT('Ctrl Pts',(374.883585693937,-11.9116251390805,0.539124247431361));
#31121=CARTESIAN_POINT('Ctrl Pts',(374.867783938921,-11.9174496420105,0.657808463019252));
#31122=CARTESIAN_POINT('Ctrl Pts',(374.846770710325,-11.9232741449405,0.775716497946804));
#31123=CARTESIAN_POINT('Ctrl Pts',(374.820657986065,-11.9290986478705,0.892366149796055));
#31124=CARTESIAN_POINT('Ctrl Pts',(374.794178722707,-11.9350049081854,1.01065318952119));
#31125=CARTESIAN_POINT('Ctrl Pts',(374.76245582688,-11.9409111685002,1.12764583113746));
#31126=CARTESIAN_POINT('Ctrl Pts',(374.725657927696,-11.9468174288151,1.24285856991482));
#31127=CARTESIAN_POINT('Ctrl Pts',(374.688860028511,-11.95272368913,1.35807130869217));
#31128=CARTESIAN_POINT('Ctrl Pts',(374.646987327792,-11.9586299494448,1.47150376096735));
#31129=CARTESIAN_POINT('Ctrl Pts',(374.600258039024,-11.9645362097597,1.58269375337675));
#31130=CARTESIAN_POINT('Ctrl Pts',(374.554060363458,-11.9703752778266,1.69261879891026));
#31131=CARTESIAN_POINT('Ctrl Pts',(374.502976104925,-11.9762143458936,1.80068521392595));
#31132=CARTESIAN_POINT('Ctrl Pts',(374.447176621336,-11.9820534139606,1.90643030863286));
#31133=CARTESIAN_POINT('Ctrl Pts',(374.391444570303,-11.9878854256311,2.01204761251769));
#31134=CARTESIAN_POINT('Ctrl Pts',(374.331008817673,-11.9937174373017,2.11534882070777));
#31135=CARTESIAN_POINT('Ctrl Pts',(374.266088835123,-11.9995494489722,2.21589100088402));
#31136=CARTESIAN_POINT('Ctrl Pts',(374.201230672302,-12.0053759071387,2.31633744027019));
#31137=CARTESIAN_POINT('Ctrl Pts',(374.131896994762,-12.0112023653052,2.41402974012144));
#31138=CARTESIAN_POINT('Ctrl Pts',(374.058352975092,-12.0170288234716,2.50854988648058));
#31139=CARTESIAN_POINT('Ctrl Pts',(373.984504106948,-12.0228794329816,2.60346182978713));
#31140=CARTESIAN_POINT('Ctrl Pts',(373.906410109799,-12.0287300424916,2.69517489856014));
#31141=CARTESIAN_POINT('Ctrl Pts',(373.824383482065,-12.0345806520016,2.78329526554843));
#31142=CARTESIAN_POINT('Ctrl Pts',(373.742779725081,-12.0404010999446,2.87096134681634));
#31143=CARTESIAN_POINT('Ctrl Pts',(373.657284075261,-12.0462215478876,2.95507138812689));
#31144=CARTESIAN_POINT('Ctrl Pts',(373.568243958236,-12.0520419958305,3.03527149565442));
#31145=CARTESIAN_POINT('Ctrl Pts',(373.479215007267,-12.0578617138616,3.11546154570612));
#31146=CARTESIAN_POINT('Ctrl Pts',(373.386642774676,-12.0636814318926,3.19174236597793));
#31147=CARTESIAN_POINT('Ctrl Pts',(373.290910004576,-12.0695011499237,3.2637984009301));
#31148=CARTESIAN_POINT('Ctrl Pts',(373.195167024865,-12.0753214886101,3.33586212044165));
#31149=CARTESIAN_POINT('Ctrl Pts',(373.096263161563,-12.0811418272966,3.40369991485691));
#31150=CARTESIAN_POINT('Ctrl Pts',(372.994612051475,-12.0869621659831,3.46703821395211));
#31151=CARTESIAN_POINT('Ctrl Pts',(372.89203352869,-12.0928356064604,3.53095437926721));
#31152=CARTESIAN_POINT('Ctrl Pts',(372.786657728871,-12.0987090469378,3.59028830160311));
#31153=CARTESIAN_POINT('Ctrl Pts',(372.678936160524,-12.1045824874152,3.6448056601651));
#31154=CARTESIAN_POINT('Ctrl Pts',(372.572038233735,-12.1104110194333,3.69890617776557));
#31155=CARTESIAN_POINT('Ctrl Pts',(372.462830682531,-12.1162395514514,3.74826341729464));
#31156=CARTESIAN_POINT('Ctrl Pts',(372.351775027263,-12.1220680834695,3.79269676153494));
#31157=CARTESIAN_POINT('Ctrl Pts',(372.239435857118,-12.1279639781765,3.83764363980664));
#31158=CARTESIAN_POINT('Ctrl Pts',(372.125205998687,-12.1338598728836,3.87755194849058));
#31159=CARTESIAN_POINT('Ctrl Pts',(372.00957812619,-12.1397557675906,3.91228683646628));
#31160=CARTESIAN_POINT('Ctrl Pts',(371.893950253693,-12.1456516622976,3.94702172444198));
#31161=CARTESIAN_POINT('Ctrl Pts',(371.776924791736,-12.1515475570046,3.97658314152301));
#31162=CARTESIAN_POINT('Ctrl Pts',(371.65900317064,-12.1574434517116,4.00088979193848));
#31163=CARTESIAN_POINT('Ctrl Pts',(371.542210115674,-12.1632829198956,4.02496381612208));
#31164=CARTESIAN_POINT('Ctrl Pts',(371.424186382237,-12.1691223880796,4.04395573241407));
#31165=CARTESIAN_POINT('Ctrl Pts',(371.305410560004,-12.1749618562636,4.05774526820234));
#31166=CARTESIAN_POINT('Ctrl Pts',(371.18677796321,-12.1807942829439,4.07151817592381));
#31167=CARTESIAN_POINT('Ctrl Pts',(371.067395481479,-12.1866267096242,4.08010113631497));
#31168=CARTESIAN_POINT('Ctrl Pts',(370.947752608512,-12.1924591363045,4.08342473376119));
#31169=CARTESIAN_POINT('Ctrl Pts',(370.828223363506,-12.1982860237768,4.08674517470008));
#31170=CARTESIAN_POINT('Ctrl Pts',(370.708434622704,-12.2041129112491,4.08481618009358));
#31171=CARTESIAN_POINT('Ctrl Pts',(370.588881163619,-12.2099397987214,4.07762011857352));
#31172=CARTESIAN_POINT('Ctrl Pts',(370.468844178012,-12.2157902526773,4.07039495303064));
#31173=CARTESIAN_POINT('Ctrl Pts',(370.349044792529,-12.2216407066332,4.05785997917041));
#31174=CARTESIAN_POINT('Ctrl Pts',(370.229984438167,-12.2274911605891,4.04005026249004));
#31175=CARTESIAN_POINT('Ctrl Pts',(370.111525327859,-12.2333120702801,4.02233048327302));
#31176=CARTESIAN_POINT('Ctrl Pts',(369.993798205446,-12.2391329799711,3.99938918136034));
#31177=CARTESIAN_POINT('Ctrl Pts',(369.877291467069,-12.2449538896621,3.97131281772197));
#31178=CARTESIAN_POINT('Ctrl Pts',(369.760799109049,-12.2507740808816,3.94323991953254));
#31179=CARTESIAN_POINT('Ctrl Pts',(369.645527229608,-12.2565942721012,3.91003331549513));
#31180=CARTESIAN_POINT('Ctrl Pts',(369.531952572461,-12.2624144633207,3.87183027461999));
#31181=CARTESIAN_POINT('Ctrl Pts',(369.418365590151,-12.2682352861495,3.83362308793687));
#31182=CARTESIAN_POINT('Ctrl Pts',(369.306476580753,-12.2740561089783,3.79041851562361));
#31183=CARTESIAN_POINT('Ctrl Pts',(369.196745125933,-12.2798769318072,3.74240304655078));
#31184=CARTESIAN_POINT('Ctrl Pts',(369.086033567296,-12.2857497452952,3.6939587109822));
#31185=CARTESIAN_POINT('Ctrl Pts',(368.977518684715,-12.2916225587832,3.64061727279132));
#31186=CARTESIAN_POINT('Ctrl Pts',(368.871648847597,-12.2974953722713,3.58261850806819));
#31187=CARTESIAN_POINT('Ctrl Pts',(368.766568138098,-12.303324411258,3.52505205181276));
#31188=CARTESIAN_POINT('Ctrl Pts',(368.664093494809,-12.3091534502448,3.46289772609776));
#31189=CARTESIAN_POINT('Ctrl Pts',(368.564634915113,-12.3149824892315,3.39643406537638));
#31190=CARTESIAN_POINT('Ctrl Pts',(368.464055974995,-12.3208771899702,3.32922171856612));
#31191=CARTESIAN_POINT('Ctrl Pts',(368.366561810464,-12.3267718907088,3.25760260622925));
#31192=CARTESIAN_POINT('Ctrl Pts',(368.272541956757,-12.3326665914475,3.18190654424048));
#31193=CARTESIAN_POINT('Ctrl Pts',(368.17852210305,-12.3385612921862,3.10621048225171));
#31194=CARTESIAN_POINT('Ctrl Pts',(368.087976841197,-12.3444559929248,3.02643779192481));
#31195=CARTESIAN_POINT('Ctrl Pts',(368.001256533536,-12.3503506936635,2.94295575211157));
#31196=CARTESIAN_POINT('Ctrl Pts',(367.9165766391,-12.3561066999525,2.86143793339836));
#31197=CARTESIAN_POINT('Ctrl Pts',(367.835271661091,-12.3618627062415,2.77612121230425));
#31198=CARTESIAN_POINT('Ctrl Pts',(367.757706503519,-12.3676187125305,2.68731978053693));
#31199=CARTESIAN_POINT('Ctrl Pts',(367.677546125477,-12.373567306649,2.59554717845714));
#31200=CARTESIAN_POINT('Ctrl Pts',(367.601380589502,-12.3795159007675,2.50005283176456));
#31201=CARTESIAN_POINT('Ctrl Pts',(367.529574331816,-12.3854644948861,2.40122786459643));
#31202=CARTESIAN_POINT('Ctrl Pts',(367.460253043918,-12.3912072284413,2.30582289264145));
#31203=CARTESIAN_POINT('Ctrl Pts',(367.394994607325,-12.3969499619965,2.20731436332425));
#31204=CARTESIAN_POINT('Ctrl Pts',(367.334087684944,-12.4026926955517,2.10608968685201));
#31205=CARTESIAN_POINT('Ctrl Pts',(367.27321546527,-12.4084321570915,2.00492268477958));
#31206=CARTESIAN_POINT('Ctrl Pts',(367.21669004701,-12.4141716186312,1.90104296940387));
#31207=CARTESIAN_POINT('Ctrl Pts',(367.164757049688,-12.4199110801709,1.79486726783742));
#31208=CARTESIAN_POINT('Ctrl Pts',(367.112840676174,-12.4256487045029,1.68872555322491));
#31209=CARTESIAN_POINT('Ctrl Pts',(367.065513984074,-12.431386328835,1.58028968977207));
#31210=CARTESIAN_POINT('Ctrl Pts',(367.022976482881,-12.437123953167,1.47000066622797));
#31211=CARTESIAN_POINT('Ctrl Pts',(366.980441978597,-12.4428611732642,1.35971941291494));
#31212=CARTESIAN_POINT('Ctrl Pts',(366.942696142886,-12.4485983933614,1.24758565055968));
#31213=CARTESIAN_POINT('Ctrl Pts',(366.909889918337,-12.4543356134585,1.1340592506042));
#31214=CARTESIAN_POINT('Ctrl Pts',(366.877065297994,-12.4600760506502,1.02046919174208));
#31215=CARTESIAN_POINT('Ctrl Pts',(366.84918593581,-12.4658164878419,0.905485338707638));
#31216=CARTESIAN_POINT('Ctrl Pts',(366.826352499821,-12.4715569250336,0.789581361179868));
#31217=CARTESIAN_POINT('Ctrl Pts',(366.803511276543,-12.4772993199879,0.673637854874063));
#31218=CARTESIAN_POINT('Ctrl Pts',(366.785719471897,-12.4830417149421,0.556774012647749));
#31219=CARTESIAN_POINT('Ctrl Pts',(366.773026140141,-12.4887841098964,0.439470842312813));
#31220=CARTESIAN_POINT('Ctrl Pts',(366.76032005478,-12.4945322745129,0.322049811802265));
#31221=CARTESIAN_POINT('Ctrl Pts',(366.752722693894,-12.5002804391295,0.204188989423663));
#31222=CARTESIAN_POINT('Ctrl Pts',(366.750231054696,-12.506028603746,0.0863714194148228));
#31223=CARTESIAN_POINT('Ctrl Pts',(366.749601607614,-12.5074807262891,0.0566079104001104));
#31224=CARTESIAN_POINT('Ctrl Pts',(366.749297741899,-12.5089328488322,0.0268471468875288));
#31225=CARTESIAN_POINT('Ctrl Pts',(366.749318884821,-12.5103849713753,-0.00290312669603759));
#31226=CARTESIAN_POINT('Ctrl Pts',(373.401623314432,-11.0032428439321,-2.20447834017448));
#31227=CARTESIAN_POINT('Ctrl Pts',(374.114700529909,-11.0675900496771,-1.37412681370391));
#31228=CARTESIAN_POINT('Ctrl Pts',(374.66124545863,-11.196239669406,1.01921189732481));
#31229=CARTESIAN_POINT('Ctrl Pts',(372.15745436975,-11.389191703119,3.73759104365418));
#31230=CARTESIAN_POINT('Ctrl Pts',(368.501159821847,-11.5820989450709,3.2032473452642));
#31231=CARTESIAN_POINT('Ctrl Pts',(366.872921458626,-11.7750061870228,-0.11142543318611));
#31232=CARTESIAN_POINT('Ctrl Pts',(368.685853908291,-11.9679134289748,-3.33036403785688));
#31233=CARTESIAN_POINT('Ctrl Pts',(372.365673949634,-12.1608206709267,-3.65521049942478));
#31234=CARTESIAN_POINT('Ctrl Pts',(374.714873489798,-12.3537279128786,-0.804512557128141));
#31235=CARTESIAN_POINT('Ctrl Pts',(373.692556454241,-12.5466351548306,2.74528784991064));
#31236=CARTESIAN_POINT('Ctrl Pts',(370.186873789973,-12.7395423967825,3.90983325738364));
#31237=CARTESIAN_POINT('Ctrl Pts',(367.243724661677,-12.9324496387344,1.67739797356575));
#31238=CARTESIAN_POINT('Ctrl Pts',(367.420207209062,-13.1253568806864,-2.01243168312488));
#31239=CARTESIAN_POINT('Ctrl Pts',(370.562994506799,-13.3182641226383,-3.95378328020931));
#31240=CARTESIAN_POINT('Ctrl Pts',(373.94151615113,-13.5111713645902,-2.45994757806193));
#31241=CARTESIAN_POINT('Ctrl Pts',(374.620392573799,-13.7040786065421,1.17118017245572));
#31242=CARTESIAN_POINT('Ctrl Pts',(372.009790107051,-13.8969858484941,3.78474415645268));
#31243=CARTESIAN_POINT('Ctrl Pts',(368.377896041367,-14.089893090446,3.10998560565922));
#31244=CARTESIAN_POINT('Ctrl Pts',(366.880227630963,-14.2828003323979,-0.266839434936402));
#31245=CARTESIAN_POINT('Ctrl Pts',(368.818020032292,-14.4757075743499,-3.41182744672225));
#31246=CARTESIAN_POINT('Ctrl Pts',(372.507634480805,-14.6686148163018,-3.59249097137997));
#31247=CARTESIAN_POINT('Ctrl Pts',(374.743433236741,-14.8615220582537,-0.651882042676315));
#31248=CARTESIAN_POINT('Ctrl Pts',(373.582802876223,-15.0544293002057,2.85513267318201));
#31249=CARTESIAN_POINT('Ctrl Pts',(370.034294735369,-15.2473365421576,3.88144023527511));
#31250=CARTESIAN_POINT('Ctrl Pts',(367.180641638276,-15.4402437841095,1.53553640908976));
#31251=CARTESIAN_POINT('Ctrl Pts',(367.501931150595,-15.6331510260615,-2.1448253743439));
#31252=CARTESIAN_POINT('Ctrl Pts',(370.717388069785,-15.8260582680134,-3.96115480385039));
#31253=CARTESIAN_POINT('Ctrl Pts',(374.036763485299,-16.0189655099653,-2.33765246017688));
#31254=CARTESIAN_POINT('Ctrl Pts',(374.568178063822,-16.2118727519173,1.31882301565855));
#31255=CARTESIAN_POINT('Ctrl Pts',(372.767084587514,-16.3404775798852,2.98520783922849));
#31256=CARTESIAN_POINT('Ctrl Pts',(371.710656479833,-16.4047799938692,3.26845729696387));
#31257=CARTESIAN_POINT('Ctrl Pts',(373.579892666462,-10.8675815057962,-2.35755359016106));
#31258=CARTESIAN_POINT('Ctrl Pts',(374.342484758555,-10.9319287115412,-1.46954385713212));
#31259=CARTESIAN_POINT('Ctrl Pts',(374.926980843371,-11.0605783312701,1.08998424882815));
#31260=CARTESIAN_POINT('Ctrl Pts',(372.249330733125,-11.2535303649831,3.99712304854097));
#31261=CARTESIAN_POINT('Ctrl Pts',(368.339149271594,-11.446437606935,3.42567542686938));
#31262=CARTESIAN_POINT('Ctrl Pts',(366.597848788441,-11.6393448488869,-0.119162626938022));
#31263=CARTESIAN_POINT('Ctrl Pts',(368.536668203236,-11.8322520908389,-3.5616188877462));
#31264=CARTESIAN_POINT('Ctrl Pts',(372.472008728708,-12.0251593327908,-3.90902213855786));
#31265=CARTESIAN_POINT('Ctrl Pts',(374.984332714381,-12.2180665747427,-0.860376549327761));
#31266=CARTESIAN_POINT('Ctrl Pts',(373.891027711771,-12.4109738166947,2.93591599819036));
#31267=CARTESIAN_POINT('Ctrl Pts',(370.141916368515,-12.6038810586466,4.18132547047225));
#31268=CARTESIAN_POINT('Ctrl Pts',(366.994399939188,-12.7967883005985,1.79387365375332));
#31269=CARTESIAN_POINT('Ctrl Pts',(367.183137136378,-12.9896955425505,-2.15217153783848));
#31270=CARTESIAN_POINT('Ctrl Pts',(370.544154272207,-13.1826027845024,-4.22832730859968));
#31271=CARTESIAN_POINT('Ctrl Pts',(374.157274749227,-13.3755100264543,-2.6307621801396));
#31272=CARTESIAN_POINT('Ctrl Pts',(374.883291203265,-13.5684172684062,1.25250494413109));
#31273=CARTESIAN_POINT('Ctrl Pts',(372.091412913603,-13.7613245103582,4.04755039379517));
#31274=CARTESIAN_POINT('Ctrl Pts',(368.207326262535,-13.9542317523101,3.32593774969494));
#31275=CARTESIAN_POINT('Ctrl Pts',(366.605662289035,-14.147138994262,-0.285368314292926));
#31276=CARTESIAN_POINT('Ctrl Pts',(368.678011719503,-14.340046236214,-3.64873897803573));
#31277=CARTESIAN_POINT('Ctrl Pts',(372.623826759225,-14.5329534781659,-3.84194747249261));
#31278=CARTESIAN_POINT('Ctrl Pts',(375.014875601881,-14.7258607201178,-0.697147629924748));
#31279=CARTESIAN_POINT('Ctrl Pts',(373.773653030798,-14.9187679620698,3.05338826033268));
#31280=CARTESIAN_POINT('Ctrl Pts',(369.978742482244,-15.1116752040217,4.1509608848977));
#31281=CARTESIAN_POINT('Ctrl Pts',(366.926936537262,-15.3045824459736,1.64216146201104));
#31282=CARTESIAN_POINT('Ctrl Pts',(367.270535850282,-15.4974896879256,-2.29375842320719));
#31283=CARTESIAN_POINT('Ctrl Pts',(370.709268663256,-15.6903969298775,-4.23621069838323));
#31284=CARTESIAN_POINT('Ctrl Pts',(374.259135897296,-15.8833041718294,-2.4999750959688));
#31285=CARTESIAN_POINT('Ctrl Pts',(374.827451005967,-16.0762114137814,1.41039985682362));
#31286=CARTESIAN_POINT('Ctrl Pts',(372.901292642829,-16.2048162417493,3.19249562605957));
#31287=CARTESIAN_POINT('Ctrl Pts',(371.771507952899,-16.2691186557333,3.49541344739883));
#31288=CARTESIAN_POINT('Ctrl Pts',(373.758162018492,-10.7319201676602,-2.51062884014765));
#31289=CARTESIAN_POINT('Ctrl Pts',(374.570268987202,-10.7962673734052,-1.56496090056034));
#31290=CARTESIAN_POINT('Ctrl Pts',(375.192716228111,-10.9249169931341,1.16075660033148));
#31291=CARTESIAN_POINT('Ctrl Pts',(372.3412070965,-11.1178690268471,4.25665505342777));
#31292=CARTESIAN_POINT('Ctrl Pts',(368.177138721342,-11.310776268799,3.64810350847456));
#31293=CARTESIAN_POINT('Ctrl Pts',(366.322776118255,-11.5036835107509,-0.126899820689938));
#31294=CARTESIAN_POINT('Ctrl Pts',(368.38748249818,-11.6965907527029,-3.7928737376355));
#31295=CARTESIAN_POINT('Ctrl Pts',(372.578343507783,-11.8894979946548,-4.16283377769094));
#31296=CARTESIAN_POINT('Ctrl Pts',(375.253791938965,-12.0824052366067,-0.916240541527381));
#31297=CARTESIAN_POINT('Ctrl Pts',(374.089498969301,-12.2753124785587,3.12654414647007));
#31298=CARTESIAN_POINT('Ctrl Pts',(370.096958947057,-12.4682197205106,4.45281768356085));
#31299=CARTESIAN_POINT('Ctrl Pts',(366.7450752167,-12.6611269624625,1.91034933394088));
#31300=CARTESIAN_POINT('Ctrl Pts',(366.946067063693,-12.8540342044145,-2.29191139255208));
#31301=CARTESIAN_POINT('Ctrl Pts',(370.525314037616,-13.0469414463664,-4.50287133699005));
#31302=CARTESIAN_POINT('Ctrl Pts',(374.373033347323,-13.2398486883183,-2.80157678221726));
#31303=CARTESIAN_POINT('Ctrl Pts',(375.146189832731,-13.4327559302702,1.33382971580646));
#31304=CARTESIAN_POINT('Ctrl Pts',(372.173035720154,-13.6256631722222,4.31035663113766));
#31305=CARTESIAN_POINT('Ctrl Pts',(368.036756483703,-13.8185704141741,3.54188989373065));
#31306=CARTESIAN_POINT('Ctrl Pts',(366.331096947107,-14.011477656126,-0.303897193649457));
#31307=CARTESIAN_POINT('Ctrl Pts',(368.538003406714,-14.204384898078,-3.88565050934918));
#31308=CARTESIAN_POINT('Ctrl Pts',(372.740019037646,-14.3972921400299,-4.09140397360527));
#31309=CARTESIAN_POINT('Ctrl Pts',(375.286317967022,-14.5901993819818,-0.742413217173175));
#31310=CARTESIAN_POINT('Ctrl Pts',(373.964503185373,-14.7831066239338,3.25164384748334));
#31311=CARTESIAN_POINT('Ctrl Pts',(369.92319022912,-14.9760138658857,4.42048153452028));
#31312=CARTESIAN_POINT('Ctrl Pts',(366.67323143625,-15.1689211078376,1.74878651493233));
#31313=CARTESIAN_POINT('Ctrl Pts',(367.03914054997,-15.3618283497896,-2.44269147207048));
#31314=CARTESIAN_POINT('Ctrl Pts',(370.701149256725,-15.5547355917415,-4.51126659291607));
#31315=CARTESIAN_POINT('Ctrl Pts',(374.481508309292,-15.7476428336934,-2.66229773176073));
#31316=CARTESIAN_POINT('Ctrl Pts',(375.086723948113,-15.9405500756454,1.50197669798869));
#31317=CARTESIAN_POINT('Ctrl Pts',(373.035500698143,-16.0691549036133,3.39978341289065));
#31318=CARTESIAN_POINT('Ctrl Pts',(371.832359425964,-16.1334573175973,3.72236959783378));
#31319=CARTESIAN_POINT('Ctrl Pts',(373.936431370522,-10.5962588295242,-2.66370409013424));
#31320=CARTESIAN_POINT('Ctrl Pts',(374.798053215848,-10.6606060352692,-1.66037794398857));
#31321=CARTESIAN_POINT('Ctrl Pts',(375.458451612851,-10.7892556549982,1.2315289518348));
#31322=CARTESIAN_POINT('Ctrl Pts',(372.433083459874,-10.9822076887111,4.51618705831456));
#31323=CARTESIAN_POINT('Ctrl Pts',(368.01512817109,-11.175114930663,3.87053159007975));
#31324=CARTESIAN_POINT('Ctrl Pts',(366.047703448069,-11.3680221726149,-0.134637014441852));
#31325=CARTESIAN_POINT('Ctrl Pts',(368.238296793125,-11.5609294145669,-4.02412858752481));
#31326=CARTESIAN_POINT('Ctrl Pts',(372.684678286857,-11.7538366565188,-4.41664541682402));
#31327=CARTESIAN_POINT('Ctrl Pts',(375.52325116355,-11.9467438984707,-0.972104533727002));
#31328=CARTESIAN_POINT('Ctrl Pts',(374.287970226831,-12.1396511404227,3.31717229474979));
#31329=CARTESIAN_POINT('Ctrl Pts',(370.052001525598,-12.3325583823746,4.72430989664947));
#31330=CARTESIAN_POINT('Ctrl Pts',(366.495750494211,-12.5254656243265,2.02682501412844));
#31331=CARTESIAN_POINT('Ctrl Pts',(366.708996991008,-12.7183728662785,-2.43165124726568));
#31332=CARTESIAN_POINT('Ctrl Pts',(370.506473803024,-12.9112801082304,-4.77741536538043));
#31333=CARTESIAN_POINT('Ctrl Pts',(374.588791945419,-13.1041873501823,-2.97239138429492));
#31334=CARTESIAN_POINT('Ctrl Pts',(375.409088462197,-13.2970945921343,1.41515448748183));
#31335=CARTESIAN_POINT('Ctrl Pts',(372.254658526706,-13.4900018340862,4.57316286848015));
#31336=CARTESIAN_POINT('Ctrl Pts',(367.866186704872,-13.6829090760381,3.75784203776637));
#31337=CARTESIAN_POINT('Ctrl Pts',(366.056531605179,-13.8758163179901,-0.322426073005982));
#31338=CARTESIAN_POINT('Ctrl Pts',(368.397995093925,-14.068723559942,-4.12256204066265));
#31339=CARTESIAN_POINT('Ctrl Pts',(372.856211316067,-14.2616308018939,-4.34086047471791));
#31340=CARTESIAN_POINT('Ctrl Pts',(375.557760332163,-14.4545380438458,-0.787678804421608));
#31341=CARTESIAN_POINT('Ctrl Pts',(374.155353339948,-14.6474452857978,3.449899434634));
#31342=CARTESIAN_POINT('Ctrl Pts',(369.867637975995,-14.8403525277497,4.69000218414286));
#31343=CARTESIAN_POINT('Ctrl Pts',(366.419526335239,-15.0332597697016,1.8554115678536));
#31344=CARTESIAN_POINT('Ctrl Pts',(366.807745249658,-15.2261670116536,-2.59162452093377));
#31345=CARTESIAN_POINT('Ctrl Pts',(370.693029850195,-15.4190742536055,-4.78632248744892));
#31346=CARTESIAN_POINT('Ctrl Pts',(374.703880721289,-15.6119814955574,-2.82462036755265));
#31347=CARTESIAN_POINT('Ctrl Pts',(375.345996890258,-15.8048887375094,1.59355353915376));
#31348=CARTESIAN_POINT('Ctrl Pts',(373.169708753457,-15.9334935654773,3.60707119972172));
#31349=CARTESIAN_POINT('Ctrl Pts',(371.89321089903,-15.9977959794613,3.94932574826872));
#31350=CARTESIAN_POINT('',(373.410035938374,-16.0015042489531,-2.20760138325762));
#31351=CARTESIAN_POINT('Ctrl Pts',(371.892222276197,-16.,3.94563850749836));
#31352=CARTESIAN_POINT('Ctrl Pts',(372.00766095465,-15.9999999999999,3.90400799429217));
#31353=CARTESIAN_POINT('Ctrl Pts',(372.120751036376,-16.,3.85687012175642));
#31354=CARTESIAN_POINT('Ctrl Pts',(372.231265838281,-16.,3.80457808135728));
#31355=CARTESIAN_POINT('Ctrl Pts',(372.344397845895,-16.,3.75104766361569));
#31356=CARTESIAN_POINT('Ctrl Pts',(372.454831795132,-15.9999999999999,3.69211553098066));
#31357=CARTESIAN_POINT('Ctrl Pts',(372.562297061756,-16.,3.62811345741236));
#31358=CARTESIAN_POINT('Ctrl Pts',(372.670203120231,-16.,3.5638488656059));
#31359=CARTESIAN_POINT('Ctrl Pts',(372.775116671354,-16.,3.49447195769568));
#31360=CARTESIAN_POINT('Ctrl Pts',(372.876727258344,-16.,3.42028126215052));
#31361=CARTESIAN_POINT('Ctrl Pts',(372.96904895601,-16.,3.35287282404679));
#31362=CARTESIAN_POINT('Ctrl Pts',(373.058643839984,-15.9999999999999,3.28148965541649));
#31363=CARTESIAN_POINT('Ctrl Pts',(373.145247083194,-16.0000000000001,3.20633639014722));
#31364=CARTESIAN_POINT('Ctrl Pts',(373.164880954339,-16.0000000000001,3.18929835009579));
#31365=CARTESIAN_POINT('Ctrl Pts',(373.184360925769,-16.,3.17206647738346));
#31366=CARTESIAN_POINT('Ctrl Pts',(373.203683664656,-15.9999999999999,3.15464306282877));
#31367=CARTESIAN_POINT('Ctrl Pts',(373.216927786189,-15.9999999999999,3.14270076928359));
#31368=CARTESIAN_POINT('Ctrl Pts',(373.23009863355,-16.0000000000001,3.13066785595378));
#31369=CARTESIAN_POINT('Ctrl Pts',(373.243183050314,-16.0000000000001,3.11855646221841));
#31370=CARTESIAN_POINT('Ctrl Pts',(373.33364353757,-16.0000000000001,3.03482307169897));
#31371=CARTESIAN_POINT('Ctrl Pts',(373.42011548176,-16.,2.94721697828212));
#31372=CARTESIAN_POINT('Ctrl Pts',(373.502339350481,-16.,2.85605153031309));
#31373=CARTESIAN_POINT('Ctrl Pts',(373.584244725785,-15.9999999999999,2.76523921088744));
#31374=CARTESIAN_POINT('Ctrl Pts',(373.661935350705,-16.0000000000002,2.67089432715435));
#31375=CARTESIAN_POINT('Ctrl Pts',(373.735112222466,-16.0000000000001,2.57329767500623));
#31376=CARTESIAN_POINT('Ctrl Pts',(373.806575122233,-16.0000000000001,2.47798696272338));
#31377=CARTESIAN_POINT('Ctrl Pts',(373.87373351298,-15.9999999999999,2.37957432698915));
#31378=CARTESIAN_POINT('Ctrl Pts',(373.936263021939,-16.,2.27830427081384));
#31379=CARTESIAN_POINT('Ctrl Pts',(373.987439735759,-16.,2.19542070480252));
#31380=CARTESIAN_POINT('Ctrl Pts',(374.035515083554,-16.,2.11062265575148));
#31381=CARTESIAN_POINT('Ctrl Pts',(374.080285480975,-16.0000000000002,2.02404008054505));
#31382=CARTESIAN_POINT('Ctrl Pts',(374.091160603096,-16.0000000000002,2.00300841379185));
#31383=CARTESIAN_POINT('Ctrl Pts',(374.101840603285,-16.0000000000002,1.98187144431043));
#31384=CARTESIAN_POINT('Ctrl Pts',(374.1123223389,-16.0000000000001,1.96063102654543));
#31385=CARTESIAN_POINT('Ctrl Pts',(374.119864193759,-16.,1.9453480472948));
#31386=CARTESIAN_POINT('Ctrl Pts',(374.127303555414,-16.0000000000001,1.93001104216781));
#31387=CARTESIAN_POINT('Ctrl Pts',(374.134632738564,-16.0000000000001,1.91463475312349));
#31388=CARTESIAN_POINT('Ctrl Pts',(374.18577050072,-16.,1.80735008088746));
#31389=CARTESIAN_POINT('Ctrl Pts',(374.231630364951,-15.9999999999999,1.69799098092543));
#31390=CARTESIAN_POINT('Ctrl Pts',(374.271931697881,-15.9999999999999,1.58681986635038));
#31391=CARTESIAN_POINT('Ctrl Pts',(374.31223303081,-16.,1.47564875177531));
#31392=CARTESIAN_POINT('Ctrl Pts',(374.346976278227,-16.,1.36266495248243));
#31393=CARTESIAN_POINT('Ctrl Pts',(374.375826174163,-16.0000000000001,1.24811885600915));
#31394=CARTESIAN_POINT('Ctrl Pts',(374.404754628375,-16.0000000000001,1.13326085047907));
#31395=CARTESIAN_POINT('Ctrl Pts',(374.427757026081,-15.9999999999998,1.01683097387319));
#31396=CARTESIAN_POINT('Ctrl Pts',(374.444913268172,-15.9999999999999,0.899262695184769));
#31397=CARTESIAN_POINT('Ctrl Pts',(374.454304156307,-15.9999999999999,0.834908826340758));
#31398=CARTESIAN_POINT('Ctrl Pts',(374.461942509795,-16.,0.770213970303242));
#31399=CARTESIAN_POINT('Ctrl Pts',(374.467835068193,-16.,0.705250877016903));
#31400=CARTESIAN_POINT('Ctrl Pts',(374.471057772603,-15.9999999999999,0.669721853270472));
#31401=CARTESIAN_POINT('Ctrl Pts',(374.473758213052,-16.,0.634112624184912));
#31402=CARTESIAN_POINT('Ctrl Pts',(374.475936951666,-16.,0.598435335677741));
#31403=CARTESIAN_POINT('Ctrl Pts',(374.477004684917,-16.,0.580950986248066));
#31404=CARTESIAN_POINT('Ctrl Pts',(374.477947198307,-15.9999999999998,0.563448511156703));
#31405=CARTESIAN_POINT('Ctrl Pts',(374.478764267789,-15.9999999999999,0.545934959024219));
#31406=CARTESIAN_POINT('Ctrl Pts',(374.484180436908,-16.0000000000001,0.429841576206889));
#31407=CARTESIAN_POINT('Ctrl Pts',(374.484072705153,-16.,0.3136354074497));
#31408=CARTESIAN_POINT('Ctrl Pts',(374.47857613537,-15.9999999999999,0.197720257635413));
#31409=CARTESIAN_POINT('Ctrl Pts',(374.47306143737,-15.9999999999998,0.0814228084803152));
#31410=CARTESIAN_POINT('Ctrl Pts',(374.462122003252,-16.0000000000001,-0.0345826156124334));
#31411=CARTESIAN_POINT('Ctrl Pts',(374.44584221609,-16.0000000000001,-0.149879655715812));
#31412=CARTESIAN_POINT('Ctrl Pts',(374.42973649359,-16.,-0.263943931526349));
#31413=CARTESIAN_POINT('Ctrl Pts',(374.408403628591,-16.0000000000001,-0.37731571180236));
#31414=CARTESIAN_POINT('Ctrl Pts',(374.381879673776,-16.,-0.489570606992328));
#31415=CARTESIAN_POINT('Ctrl Pts',(374.365217561952,-15.9999999999999,-0.56008813084572));
#31416=CARTESIAN_POINT('Ctrl Pts',(374.346506033578,-16.0000000000001,-0.630164438406834));
#31417=CARTESIAN_POINT('Ctrl Pts',(374.32574563494,-16.,-0.699687792345608));
#31418=CARTESIAN_POINT('Ctrl Pts',(374.314654561951,-15.9999999999999,-0.736830074941256));
#31419=CARTESIAN_POINT('Ctrl Pts',(374.302978605753,-16.,-0.773814439918066));
#31420=CARTESIAN_POINT('Ctrl Pts',(374.290717142131,-16.,-0.810623111675999));
#31421=CARTESIAN_POINT('Ctrl Pts',(374.284608867747,-15.9999999999999,-0.828960030801155));
#31422=CARTESIAN_POINT('Ctrl Pts',(374.278354559896,-15.9999999999998,-0.847255206523337));
#31423=CARTESIAN_POINT('Ctrl Pts',(374.271960105546,-15.9999999999998,-0.865489809766218));
#31424=CARTESIAN_POINT('Ctrl Pts',(374.234721434297,-16.0000000000001,-0.971680636746369));
#31425=CARTESIAN_POINT('Ctrl Pts',(374.192694947791,-16.0000000000001,-1.075938071221));
#31426=CARTESIAN_POINT('Ctrl Pts',(374.145929614334,-16.0000000000001,-1.17786253481042));
#31427=CARTESIAN_POINT('Ctrl Pts',(374.110855614242,-16.0000000000001,-1.25430588250247));
#31428=CARTESIAN_POINT('Ctrl Pts',(374.073115090259,-15.9999999999998,-1.32943652806763));
#31429=CARTESIAN_POINT('Ctrl Pts',(374.032714072705,-16.,-1.40307333334082));
#31430=CARTESIAN_POINT('Ctrl Pts',(374.012405921882,-16.0000000000001,-1.44008792946224));
#31431=CARTESIAN_POINT('Ctrl Pts',(373.991425351126,-15.9999999999998,-1.47672488375371));
#31432=CARTESIAN_POINT('Ctrl Pts',(373.969772022922,-16.,-1.51295991340807));
#31433=CARTESIAN_POINT('Ctrl Pts',(373.957520800147,-16.0000000000001,-1.53346130776109));
#31434=CARTESIAN_POINT('Ctrl Pts',(373.945054202837,-16.,-1.55383402251675));
#31435=CARTESIAN_POINT('Ctrl Pts',(373.932372070541,-16.,-1.57407352405639));
#31436=CARTESIAN_POINT('Ctrl Pts',(373.922781198224,-16.0000000000001,-1.58937966268586));
#31437=CARTESIAN_POINT('Ctrl Pts',(373.913068078195,-16.0000000000001,-1.60460789185709));
#31438=CARTESIAN_POINT('Ctrl Pts',(373.90323766738,-16.0000000000001,-1.61974887144166));
#31439=CARTESIAN_POINT('Ctrl Pts',(373.844544342933,-15.9999999999998,-1.71014940952207));
#31440=CARTESIAN_POINT('Ctrl Pts',(373.781624617244,-15.9999999999999,-1.79751979106278));
#31441=CARTESIAN_POINT('Ctrl Pts',(373.714499732742,-16.,-1.88147730110623));
#31442=CARTESIAN_POINT('Ctrl Pts',(373.677193093894,-16.0000000000001,-1.92813916919038));
#31443=CARTESIAN_POINT('Ctrl Pts',(373.638586897237,-15.9999999999999,-1.97374619699087));
#31444=CARTESIAN_POINT('Ctrl Pts',(373.598680408904,-15.9999999999999,-2.01822719257774));
#31445=CARTESIAN_POINT('Ctrl Pts',(373.539303779228,-16.,-2.08441020473598));
#31446=CARTESIAN_POINT('Ctrl Pts',(373.477048640108,-16.,-2.14810122424028));
#31447=CARTESIAN_POINT('Ctrl Pts',(373.412117880462,-15.9999999999998,-2.2092048034827));
#31448=CARTESIAN_POINT('Ctrl Pts',(373.407552280239,-11.,-2.20655152809227));
#31449=CARTESIAN_POINT('Ctrl Pts',(373.484164508103,-11.0000000000001,-2.13363933676576));
#31450=CARTESIAN_POINT('Ctrl Pts',(373.556850099011,-10.9999999999999,-2.05708919551984));
#31451=CARTESIAN_POINT('Ctrl Pts',(373.625609529926,-11.,-1.97731684646155));
#31452=CARTESIAN_POINT('Ctrl Pts',(373.696087228626,-11.0000000000001,-1.89555102166244));
#31453=CARTESIAN_POINT('Ctrl Pts',(373.76244049017,-10.9999999999999,-1.81039952484827));
#31454=CARTESIAN_POINT('Ctrl Pts',(373.824643791805,-11.,-1.72226175147527));
#31455=CARTESIAN_POINT('Ctrl Pts',(373.88816280824,-11.,-1.63225970129142));
#31456=CARTESIAN_POINT('Ctrl Pts',(373.947354900361,-10.9999999999999,-1.53914316978695));
#31457=CARTESIAN_POINT('Ctrl Pts',(374.002159551767,-10.9999999999999,-1.44329500707418));
#31458=CARTESIAN_POINT('Ctrl Pts',(374.053687620609,-10.9999999999999,-1.3531772780149));
#31459=CARTESIAN_POINT('Ctrl Pts',(374.101337144399,-11.0000000000001,-1.26064392327993));
#31460=CARTESIAN_POINT('Ctrl Pts',(374.145026500752,-11.0000000000001,-1.16598700574379));
#31461=CARTESIAN_POINT('Ctrl Pts',(374.152708549467,-11.0000000000001,-1.14934315670631));
#31462=CARTESIAN_POINT('Ctrl Pts',(374.160268078308,-11.,-1.13263360147186));
#31463=CARTESIAN_POINT('Ctrl Pts',(374.167704536593,-11.0000000000001,-1.11585986664135));
#31464=CARTESIAN_POINT('Ctrl Pts',(374.174057108471,-11.0000000000002,-1.10153095466744));
#31465=CARTESIAN_POINT('Ctrl Pts',(374.180315995137,-10.9999999999999,-1.08716393738812));
#31466=CARTESIAN_POINT('Ctrl Pts',(374.186480716856,-10.9999999999999,-1.0727610067648));
#31467=CARTESIAN_POINT('Ctrl Pts',(374.231299693678,-10.9999999999999,-0.968048313613609));
#31468=CARTESIAN_POINT('Ctrl Pts',(374.271152113617,-11.0000000000001,-0.861423109955285));
#31469=CARTESIAN_POINT('Ctrl Pts',(374.30600663119,-11.,-0.753314769919725));
#31470=CARTESIAN_POINT('Ctrl Pts',(374.34138484736,-10.9999999999999,-0.643582072697306));
#31471=CARTESIAN_POINT('Ctrl Pts',(374.371614293078,-10.9999999999999,-0.532320624946264));
#31472=CARTESIAN_POINT('Ctrl Pts',(374.396622579182,-11.,-0.419943006692207));
#31473=CARTESIAN_POINT('Ctrl Pts',(374.421855131763,-11.0000000000001,-0.306557621155216));
#31474=CARTESIAN_POINT('Ctrl Pts',(374.441772914412,-10.9999999999999,-0.192035136737321));
#31475=CARTESIAN_POINT('Ctrl Pts',(374.456254753839,-10.9999999999999,-0.0767741815375196));
#31476=CARTESIAN_POINT('Ctrl Pts',(374.467116133409,-10.9999999999999,0.00967153486233469));
#31477=CARTESIAN_POINT('Ctrl Pts',(374.474918871082,-11.,0.0965332453698254));
#31478=CARTESIAN_POINT('Ctrl Pts',(374.47959245864,-11.,0.183647619031922));
#31479=CARTESIAN_POINT('Ctrl Pts',(374.480430050729,-11.,0.199260102872992));
#31480=CARTESIAN_POINT('Ctrl Pts',(374.481167091454,-11.,0.214880707141451));
#31481=CARTESIAN_POINT('Ctrl Pts',(374.481803114277,-11.,0.230508496459851));
#31482=CARTESIAN_POINT('Ctrl Pts',(374.482481222596,-10.9999999999999,0.247170373304957));
#31483=CARTESIAN_POINT('Ctrl Pts',(374.483044115965,-10.9999999999997,0.263831297496222));
#31484=CARTESIAN_POINT('Ctrl Pts',(374.483491541806,-10.9999999999998,0.280486880814511));
#31485=CARTESIAN_POINT('Ctrl Pts',(374.486677685243,-10.9999999999998,0.399092183945026));
#31486=CARTESIAN_POINT('Ctrl Pts',(374.484014434623,-10.9999999999998,0.517476627121978));
#31487=CARTESIAN_POINT('Ctrl Pts',(374.475431647664,-10.9999999999999,0.635212121420028));
#31488=CARTESIAN_POINT('Ctrl Pts',(374.467426874872,-10.9999999999999,0.745018631346651));
#31489=CARTESIAN_POINT('Ctrl Pts',(374.45427284864,-10.9999999999998,0.854261519988693));
#31490=CARTESIAN_POINT('Ctrl Pts',(374.435874189068,-10.9999999999999,0.962607274232096));
#31491=CARTESIAN_POINT('Ctrl Pts',(374.416682752686,-11.,1.07562152082828));
#31492=CARTESIAN_POINT('Ctrl Pts',(374.391785849854,-10.9999999999998,1.18766042245905));
#31493=CARTESIAN_POINT('Ctrl Pts',(374.361479323342,-10.9999999999999,1.29845785681547));
#31494=CARTESIAN_POINT('Ctrl Pts',(374.342689269744,-11.,1.36715229229592));
#31495=CARTESIAN_POINT('Ctrl Pts',(374.321818678637,-10.9999999999999,1.43536952436879));
#31496=CARTESIAN_POINT('Ctrl Pts',(374.298928231114,-11.,1.50304501988366));
#31497=CARTESIAN_POINT('Ctrl Pts',(374.286672454928,-11.,1.53927916189878));
#31498=CARTESIAN_POINT('Ctrl Pts',(374.273837535033,-11.,1.57535798511614));
#31499=CARTESIAN_POINT('Ctrl Pts',(374.260431959166,-11.0000000000001,1.61127137589293));
#31500=CARTESIAN_POINT('Ctrl Pts',(374.252732754366,-11.0000000000001,1.63189746114107));
#31501=CARTESIAN_POINT('Ctrl Pts',(374.244843634651,-11.,1.65247297333473));
#31502=CARTESIAN_POINT('Ctrl Pts',(374.236776829888,-11.,1.6729695185202));
#31503=CARTESIAN_POINT('Ctrl Pts',(374.193756623204,-11.,1.78227743361823));
#31504=CARTESIAN_POINT('Ctrl Pts',(374.145638532941,-10.9999999999999,1.88947606107137));
#31505=CARTESIAN_POINT('Ctrl Pts',(374.092775693224,-11.,1.99429708346387));
#31506=CARTESIAN_POINT('Ctrl Pts',(374.03834197434,-11.,2.10223298127993));
#31507=CARTESIAN_POINT('Ctrl Pts',(373.978877168769,-10.9999999999999,2.20764856732848));
#31508=CARTESIAN_POINT('Ctrl Pts',(373.914710641423,-11.,2.31024771811314));
#31509=CARTESIAN_POINT('Ctrl Pts',(373.850544114076,-11.0000000000001,2.41284686889779));
#31510=CARTESIAN_POINT('Ctrl Pts',(373.781675419372,-11.,2.51263031159976));
#31511=CARTESIAN_POINT('Ctrl Pts',(373.70838352593,-11.,2.60928799789692));
#31512=CARTESIAN_POINT('Ctrl Pts',(373.658795943347,-11.,2.67468432996569));
#31513=CARTESIAN_POINT('Ctrl Pts',(373.607182576977,-11.,2.73864953564559));
#31514=CARTESIAN_POINT('Ctrl Pts',(373.55361831323,-11.,2.80108138650798));
#31515=CARTESIAN_POINT('Ctrl Pts',(373.534988737123,-11.,2.82279509702634));
#31516=CARTESIAN_POINT('Ctrl Pts',(373.516123096266,-10.9999999999999,2.8443232731753));
#31517=CARTESIAN_POINT('Ctrl Pts',(373.497024303559,-11.,2.86566142895363));
#31518=CARTESIAN_POINT('Ctrl Pts',(373.485069089254,-11.,2.87901841068074));
#31519=CARTESIAN_POINT('Ctrl Pts',(373.473022095985,-10.9999999999999,2.89230139020273));
#31520=CARTESIAN_POINT('Ctrl Pts',(373.460885295567,-10.9999999999999,2.90550785313149));
#31521=CARTESIAN_POINT('Ctrl Pts',(373.375975367293,-11.0000000000001,2.99790121723507));
#31522=CARTESIAN_POINT('Ctrl Pts',(373.286963615328,-11.,3.08623632965698));
#31523=CARTESIAN_POINT('Ctrl Pts',(373.194175441271,-11.,3.17018989640025));
#31524=CARTESIAN_POINT('Ctrl Pts',(373.119592675862,-11.,3.23767143957404));
#31525=CARTESIAN_POINT('Ctrl Pts',(373.042568901898,-11.,3.30232200719299));
#31526=CARTESIAN_POINT('Ctrl Pts',(372.963251804661,-11.0000000000001,3.36396181620956));
#31527=CARTESIAN_POINT('Ctrl Pts',(372.897202039085,-11.0000000000002,3.41529116483014));
#31528=CARTESIAN_POINT('Ctrl Pts',(372.829561609887,-11.,3.46453261665077));
#31529=CARTESIAN_POINT('Ctrl Pts',(372.760407137997,-11.0000000000001,3.51157458559606));
#31530=CARTESIAN_POINT('Ctrl Pts',(372.744424821001,-11.0000000000001,3.52244647340364));
#31531=CARTESIAN_POINT('Ctrl Pts',(372.72836292761,-11.0000000000001,3.53319989268987));
#31532=CARTESIAN_POINT('Ctrl Pts',(372.712230322745,-11.0000000000001,3.54382840352593));
#31533=CARTESIAN_POINT('Ctrl Pts',(372.60675817946,-11.,3.61331574467032));
#31534=CARTESIAN_POINT('Ctrl Pts',(372.498175010034,-11.0000000000002,3.67752958060433));
#31535=CARTESIAN_POINT('Ctrl Pts',(372.386777109338,-11.0000000000001,3.73612797973573));
#31536=CARTESIAN_POINT('Ctrl Pts',(372.322300834232,-11.,3.77004429664692));
#31537=CARTESIAN_POINT('Ctrl Pts',(372.256880848245,-11.,3.80207888043325));
#31538=CARTESIAN_POINT('Ctrl Pts',(372.190568937043,-11.0000000000001,3.83215976551742));
#31539=CARTESIAN_POINT('Ctrl Pts',(372.094043909479,-11.0000000000001,3.87594614128781));
#31540=CARTESIAN_POINT('Ctrl Pts',(371.995629603314,-11.,3.91559422951229));
#31541=CARTESIAN_POINT('Ctrl Pts',(371.895579440434,-11.,3.95116325459089));
#31542=CARTESIAN_POINT('Ctrl Pts',(373.408085425102,-16.0015042489531,-2.20592963361204));
#31543=CARTESIAN_POINT('Ctrl Pts',(373.397699055235,-16.0010028326354,-2.21804792675504));
#31544=CARTESIAN_POINT('Ctrl Pts',(373.387227097536,-16.0005014163177,-2.23009286410093));
#31545=CARTESIAN_POINT('Ctrl Pts',(373.376670596656,-16.,-2.2420632440818));
#31546=CARTESIAN_POINT('Ctrl Pts',(369.776711150535,-11.0016404554735,3.94875541723466));
#31547=CARTESIAN_POINT('Ctrl Pts',(368.500032745302,-11.0659606286233,3.60684744968143));
#31548=CARTESIAN_POINT('Ctrl Pts',(366.323554905574,-11.1945832157571,1.59361640613361));
#31549=CARTESIAN_POINT('Ctrl Pts',(366.965591470948,-11.3875082168749,-2.82400952883738));
#31550=CARTESIAN_POINT('Ctrl Pts',(370.975575282479,-11.5804154588268,-4.78528756048741));
#31551=CARTESIAN_POINT('Ctrl Pts',(374.860019939513,-11.7733227007787,-2.59106421286309));
#31552=CARTESIAN_POINT('Ctrl Pts',(375.248154941599,-11.9662299427307,1.85501048073415));
#31553=CARTESIAN_POINT('Ctrl Pts',(371.800788741178,-12.1591371846826,4.68898826029466));
#31554=CARTESIAN_POINT('Ctrl Pts',(367.514000337472,-12.3520444266345,3.44915361081735));
#31555=CARTESIAN_POINT('Ctrl Pts',(366.111896528258,-12.5449516685864,-0.787508517572457));
#31556=CARTESIAN_POINT('Ctrl Pts',(368.812861501212,-12.7378589105384,-4.33992202873321));
#31557=CARTESIAN_POINT('Ctrl Pts',(373.270113906834,-12.9307661524903,-4.1216707895165));
#31558=CARTESIAN_POINT('Ctrl Pts',(375.611071197946,-13.1236733944423,-0.322356367943754));
#31559=CARTESIAN_POINT('Ctrl Pts',(373.801807325092,-13.3165806363942,3.75702963470999));
#31560=CARTESIAN_POINT('Ctrl Pts',(369.41428424138,-13.5094878783461,4.57217420235261));
#31561=CARTESIAN_POINT('Ctrl Pts',(366.260536257966,-13.702395120298,1.41484854707178));
#31562=CARTESIAN_POINT('Ctrl Pts',(367.080655435926,-13.89530236225,-2.97174878689068));
#31563=CARTESIAN_POINT('Ctrl Pts',(371.162091027228,-14.0882096042019,-4.77638254206457));
#31564=CARTESIAN_POINT('Ctrl Pts',(374.958746867641,-14.2811168461538,-2.43112555194102));
#31565=CARTESIAN_POINT('Ctrl Pts',(375.171947262906,-14.4740240881058,2.02638683774903));
#31566=CARTESIAN_POINT('Ctrl Pts',(371.616465052591,-14.6669313300577,4.72328855323263));
#31567=CARTESIAN_POINT('Ctrl Pts',(367.381412119708,-14.8598385720096,3.31645516043818));
#31568=CARTESIAN_POINT('Ctrl Pts',(366.146398234732,-15.0527458139616,-0.971894380569737));
#31569=CARTESIAN_POINT('Ctrl Pts',(368.98435744238,-15.2456530559135,-4.41569058707157));
#31570=CARTESIAN_POINT('Ctrl Pts',(373.429777663597,-15.4385602978654,-4.02325864183314));
#31571=CARTESIAN_POINT('Ctrl Pts',(375.619897415873,-15.6314675398174,-0.134607920621325));
#31572=CARTESIAN_POINT('Ctrl Pts',(373.652897933972,-15.8243747817693,3.86969469419586));
#31573=CARTESIAN_POINT('Ctrl Pts',(369.235897717888,-16.0172820237212,4.51521059429547));
#31574=CARTESIAN_POINT('Ctrl Pts',(366.211885374231,-16.2101892656732,1.23202454967953));
#31575=CARTESIAN_POINT('Ctrl Pts',(366.870979860592,-16.3387940936411,-1.6580058124492));
#31576=CARTESIAN_POINT('Ctrl Pts',(367.731076742204,-16.4030965076251,-2.66103287896124));
#31577=CARTESIAN_POINT('Ctrl Pts',(369.837283293296,-10.8664668332409,3.72259896771894));
#31578=CARTESIAN_POINT('Ctrl Pts',(368.633723890076,-10.9307870063907,3.40027304155158));
#31579=CARTESIAN_POINT('Ctrl Pts',(366.58189912421,-11.0594095935245,1.50234546371763));
#31580=CARTESIAN_POINT('Ctrl Pts',(367.187164430099,-11.2523345946423,-2.66227047413349));
#31581=CARTESIAN_POINT('Ctrl Pts',(370.967485067894,-11.4452418365942,-4.51122053676947));
#31582=CARTESIAN_POINT('Ctrl Pts',(374.629456535493,-11.6381490785461,-2.44266659869565));
#31583=CARTESIAN_POINT('Ctrl Pts',(374.995361942496,-11.8310563204981,1.74876875649206));
#31584=CARTESIAN_POINT('Ctrl Pts',(371.745436205636,-12.02396356245,4.42043657128886));
#31585=CARTESIAN_POINT('Ctrl Pts',(367.704164361648,-12.2168708044019,3.25161077718117));
#31586=CARTESIAN_POINT('Ctrl Pts',(366.382363023932,-12.4097780463539,-0.742405665792816));
#31587=CARTESIAN_POINT('Ctrl Pts',(368.928636053727,-12.6026852883058,-4.09136235524481));
#31588=CARTESIAN_POINT('Ctrl Pts',(373.130608941592,-12.7955925302577,-3.88561098501168));
#31589=CARTESIAN_POINT('Ctrl Pts',(375.337492953028,-12.9884997722097,-0.303894102254988));
#31590=CARTESIAN_POINT('Ctrl Pts',(373.631850766121,-13.1814070141616,3.54185386585814));
#31591=CARTESIAN_POINT('Ctrl Pts',(369.495613603651,-13.3743142561135,4.3103127865611));
#31592=CARTESIAN_POINT('Ctrl Pts',(366.522489733719,-13.5672214980655,1.33381614820207));
#31593=CARTESIAN_POINT('Ctrl Pts',(367.295638354663,-13.7601287400174,-2.80154828483818));
#31594=CARTESIAN_POINT('Ctrl Pts',(371.143318525656,-13.9530359819693,-4.5028255340697));
#31595=CARTESIAN_POINT('Ctrl Pts',(374.722529091754,-14.1459432239212,-2.2918880796088));
#31596=CARTESIAN_POINT('Ctrl Pts',(374.923518894229,-14.3388504658732,1.9103299022978));
#31597=CARTESIAN_POINT('Ctrl Pts',(371.571669258747,-14.5317577078251,4.45277238893056));
#31598=CARTESIAN_POINT('Ctrl Pts',(367.57916984808,-14.724664949777,3.12651234433233));
#31599=CARTESIAN_POINT('Ctrl Pts',(366.414888719584,-14.917572191729,-0.916231226185798));
#31600=CARTESIAN_POINT('Ctrl Pts',(369.090309934762,-15.1104794336809,-4.16279143282831));
#31601=CARTESIAN_POINT('Ctrl Pts',(373.281128301063,-15.3033866756328,-3.79283518082333));
#31602=CARTESIAN_POINT('Ctrl Pts',(375.345813668361,-15.4962939175848,-0.126898542301376));
#31603=CARTESIAN_POINT('Ctrl Pts',(373.491469839196,-15.6892011595367,3.64806627706739));
#31604=CARTESIAN_POINT('Ctrl Pts',(369.327443783533,-15.8821084014886,4.25661164629155));
#31605=CARTESIAN_POINT('Ctrl Pts',(366.476625224416,-16.0750156434406,1.16146300093036));
#31606=CARTESIAN_POINT('Ctrl Pts',(367.097971495661,-16.2036204714085,-1.56304710566696));
#31607=CARTESIAN_POINT('Ctrl Pts',(367.908808183507,-16.2679228853925,-2.50862796035731));
#31608=CARTESIAN_POINT('Ctrl Pts',(369.897855436059,-10.7312932110083,3.49644251820321));
#31609=CARTESIAN_POINT('Ctrl Pts',(368.767415034851,-10.7956133841581,3.19369863342172));
#31610=CARTESIAN_POINT('Ctrl Pts',(366.840243342845,-10.9242359712918,1.41107452130166));
#31611=CARTESIAN_POINT('Ctrl Pts',(367.408737389251,-11.1171609724097,-2.50053141942959));
#31612=CARTESIAN_POINT('Ctrl Pts',(370.95939485331,-11.3100682143616,-4.23715351305153));
#31613=CARTESIAN_POINT('Ctrl Pts',(374.398893131472,-11.5029754563135,-2.29426898452822));
#31614=CARTESIAN_POINT('Ctrl Pts',(374.742568943392,-11.6958826982655,1.64252703224997));
#31615=CARTESIAN_POINT('Ctrl Pts',(371.690083670094,-11.8887899402174,4.15188488228307));
#31616=CARTESIAN_POINT('Ctrl Pts',(367.894328385824,-12.0816971821693,3.05406794354497));
#31617=CARTESIAN_POINT('Ctrl Pts',(366.652829519606,-12.2746044241213,-0.697302814013183));
#31618=CARTESIAN_POINT('Ctrl Pts',(369.044410606242,-12.4675116660732,-3.84280268175641));
#31619=CARTESIAN_POINT('Ctrl Pts',(372.991103976351,-12.6604189080251,-3.64955118050687));
#31620=CARTESIAN_POINT('Ctrl Pts',(375.063914708111,-12.8533261499771,-0.285431836566218));
#31621=CARTESIAN_POINT('Ctrl Pts',(373.461894207149,-13.046233391929,3.32667809700629));
#31622=CARTESIAN_POINT('Ctrl Pts',(369.576942965922,-13.2391406338809,4.0484513707696));
#31623=CARTESIAN_POINT('Ctrl Pts',(366.784443209472,-13.4320478758329,1.25278374933238));
#31624=CARTESIAN_POINT('Ctrl Pts',(367.5106212734,-13.6249551177848,-2.63134778278569));
#31625=CARTESIAN_POINT('Ctrl Pts',(371.124546024083,-13.8178623597367,-4.22926852607485));
#31626=CARTESIAN_POINT('Ctrl Pts',(374.486311315867,-14.0107696016886,-2.15265060727657));
#31627=CARTESIAN_POINT('Ctrl Pts',(374.675090525552,-14.2036768436406,1.79427296684655));
#31628=CARTESIAN_POINT('Ctrl Pts',(371.526873464904,-14.3965840855925,4.18225622462848));
#31629=CARTESIAN_POINT('Ctrl Pts',(367.776927576449,-14.5894913275444,2.93656952822648));
#31630=CARTESIAN_POINT('Ctrl Pts',(366.683379204436,-14.7823985694964,-0.860568071801865));
#31631=CARTESIAN_POINT('Ctrl Pts',(369.196262427144,-14.9753058114483,-3.90989227858506));
#31632=CARTESIAN_POINT('Ctrl Pts',(373.13247893853,-15.1682130534002,-3.56241171981353));
#31633=CARTESIAN_POINT('Ctrl Pts',(375.071729920849,-15.3611202953522,-0.119189163981424));
#31634=CARTESIAN_POINT('Ctrl Pts',(373.330041744421,-15.5540275373041,3.42643785993892));
#31635=CARTESIAN_POINT('Ctrl Pts',(369.418989849177,-15.746934779256,3.99801269828764));
#31636=CARTESIAN_POINT('Ctrl Pts',(366.741365074601,-15.939842021208,1.0909014521812));
#31637=CARTESIAN_POINT('Ctrl Pts',(367.32496313073,-16.0684468491759,-1.46808839888473));
#31638=CARTESIAN_POINT('Ctrl Pts',(368.086539624811,-16.1327492631599,-2.35622304175338));
#31639=CARTESIAN_POINT('Ctrl Pts',(369.958427578821,-10.5961195887756,3.27028606868749));
#31640=CARTESIAN_POINT('Ctrl Pts',(368.901106179625,-10.6604397619255,2.98712422529187));
#31641=CARTESIAN_POINT('Ctrl Pts',(367.09858756148,-10.7890623490592,1.31980357888569));
#31642=CARTESIAN_POINT('Ctrl Pts',(367.630310348403,-10.9819873501771,-2.33879236472568));
#31643=CARTESIAN_POINT('Ctrl Pts',(370.951304638724,-11.174894592129,-3.96308648933358));
#31644=CARTESIAN_POINT('Ctrl Pts',(374.168329727452,-11.3678018340809,-2.14587137036077));
#31645=CARTESIAN_POINT('Ctrl Pts',(374.48977594429,-11.5607090760329,1.53628530800788));
#31646=CARTESIAN_POINT('Ctrl Pts',(371.634731134551,-11.7536163179848,3.88333319327727));
#31647=CARTESIAN_POINT('Ctrl Pts',(368.084492409999,-11.9465235599367,2.85652510990878));
#31648=CARTESIAN_POINT('Ctrl Pts',(366.923296015279,-12.1394308018887,-0.652199962233542));
#31649=CARTESIAN_POINT('Ctrl Pts',(369.160185158757,-12.3323380438406,-3.59424300826801));
#31650=CARTESIAN_POINT('Ctrl Pts',(372.851599011108,-12.5252452857925,-3.41349137600206));
#31651=CARTESIAN_POINT('Ctrl Pts',(374.790336463194,-12.7181525277445,-0.266969570877453));
#31652=CARTESIAN_POINT('Ctrl Pts',(373.291937648178,-12.9110597696964,3.11150232815445));
#31653=CARTESIAN_POINT('Ctrl Pts',(369.658272328193,-13.1039670116483,3.78658995497808));
#31654=CARTESIAN_POINT('Ctrl Pts',(367.046396685226,-13.2968742536003,1.17175135046268));
#31655=CARTESIAN_POINT('Ctrl Pts',(367.725604192137,-13.4897814955522,-2.46114728073319));
#31656=CARTESIAN_POINT('Ctrl Pts',(371.105773522511,-13.6826887375041,-3.95571151807998));
#31657=CARTESIAN_POINT('Ctrl Pts',(374.25009353998,-13.875595979456,-2.01341313494433));
#31658=CARTESIAN_POINT('Ctrl Pts',(374.426662156873,-14.068503221408,1.67821603139532));
#31659=CARTESIAN_POINT('Ctrl Pts',(371.482077671061,-14.2614104633599,3.91174006032641));
#31660=CARTESIAN_POINT('Ctrl Pts',(367.974685304821,-14.4543177053119,2.74662671212062));
#31661=CARTESIAN_POINT('Ctrl Pts',(366.951869689287,-14.6472249472638,-0.804904917417929));
#31662=CARTESIAN_POINT('Ctrl Pts',(369.302214919525,-14.8401321892157,-3.6569931243418));
#31663=CARTESIAN_POINT('Ctrl Pts',(372.983829575995,-15.0330394311676,-3.33198825880372));
#31664=CARTESIAN_POINT('Ctrl Pts',(374.797646173337,-15.2259466731196,-0.111479785661475));
#31665=CARTESIAN_POINT('Ctrl Pts',(373.168613649646,-15.4188539150715,3.20480944281046));
#31666=CARTESIAN_POINT('Ctrl Pts',(369.510535914822,-15.6117611570234,3.73941375028372));
#31667=CARTESIAN_POINT('Ctrl Pts',(367.006104924786,-15.8046683989754,1.02033990343203));
#31668=CARTESIAN_POINT('Ctrl Pts',(367.551954765798,-15.9332732269433,-1.37312969210249));
#31669=CARTESIAN_POINT('Ctrl Pts',(368.264271066114,-15.9975756409273,-2.20381812314945));
#31670=CARTESIAN_POINT('Ctrl Pts',(368.26108342621,-16.,-2.20655152809223));
#31671=CARTESIAN_POINT('Ctrl Pts',(368.18351393423,-16.0000000000001,-2.13272830433258));
#31672=CARTESIAN_POINT('Ctrl Pts',(368.109969768842,-16.,-2.05517575529548));
#31673=CARTESIAN_POINT('Ctrl Pts',(368.040450579516,-16.,-1.9743250932332));
#31674=CARTESIAN_POINT('Ctrl Pts',(367.970931390189,-16.0000000000001,-1.89347443117091));
#31675=CARTESIAN_POINT('Ctrl Pts',(367.90543688921,-15.9999999999999,-1.80932506555908));
#31676=CARTESIAN_POINT('Ctrl Pts',(367.843991843118,-16.0000000000001,-1.72226169762899));
#31677=CARTESIAN_POINT('Ctrl Pts',(367.780009545896,-16.0000000000002,-1.63160322085558));
#31678=CARTESIAN_POINT('Ctrl Pts',(367.720417473432,-15.9999999999999,-1.53778471284877));
#31679=CARTESIAN_POINT('Ctrl Pts',(367.665277613433,-16.,-1.44119732543093));
#31680=CARTESIAN_POINT('Ctrl Pts',(367.614209007617,-16.0000000000002,-1.35174147235489));
#31681=CARTESIAN_POINT('Ctrl Pts',(367.566959548454,-15.9999999999999,-1.25990961252799));
#31682=CARTESIAN_POINT('Ctrl Pts',(367.523609095148,-16.0000000000001,-1.16598698107383));
#31683=CARTESIAN_POINT('Ctrl Pts',(367.515926948415,-16.0000000000002,-1.14934292359788));
#31684=CARTESIAN_POINT('Ctrl Pts',(367.508367324632,-16.0000000000002,-1.13263315829243));
#31685=CARTESIAN_POINT('Ctrl Pts',(367.500930774503,-16.0000000000001,-1.11585921181451));
#31686=CARTESIAN_POINT('Ctrl Pts',(367.494578290699,-16.0000000000001,-1.10153049467122));
#31687=CARTESIAN_POINT('Ctrl Pts',(367.488319489826,-15.9999999999999,-1.08716367391313));
#31688=CARTESIAN_POINT('Ctrl Pts',(367.482154851194,-15.9999999999999,-1.07276094050394));
#31689=CARTESIAN_POINT('Ctrl Pts',(367.437335864243,-15.9999999999999,-0.968048246163189));
#31690=CARTESIAN_POINT('Ctrl Pts',(367.397483434743,-16.0000000000001,-0.861423041830749));
#31691=CARTESIAN_POINT('Ctrl Pts',(367.362628908517,-16.0000000000001,-0.753314701397611));
#31692=CARTESIAN_POINT('Ctrl Pts',(367.327250685275,-16.,-0.643582009079649));
#31693=CARTESIAN_POINT('Ctrl Pts',(367.297021232921,-15.9999999999999,-0.532320566665647));
#31694=CARTESIAN_POINT('Ctrl Pts',(367.272012940965,-15.9999999999999,-0.419942953878413));
#31695=CARTESIAN_POINT('Ctrl Pts',(367.246780388205,-16.,-0.306557599580401));
#31696=CARTESIAN_POINT('Ctrl Pts',(367.226862603766,-16.0000000000001,-0.192035147049314));
#31697=CARTESIAN_POINT('Ctrl Pts',(367.21238076122,-16.,-0.0767742238126385));
#31698=CARTESIAN_POINT('Ctrl Pts',(367.20151937931,-15.9999999999999,0.00967146861486187));
#31699=CARTESIAN_POINT('Ctrl Pts',(367.193716638548,-16.,0.0965331551063391));
#31700=CARTESIAN_POINT('Ctrl Pts',(367.189043047261,-15.9999999999999,0.183647504944786));
#31701=CARTESIAN_POINT('Ctrl Pts',(367.188205453357,-15.9999999999999,0.199260005896969));
#31702=CARTESIAN_POINT('Ctrl Pts',(367.187468411071,-16.0000000000002,0.214880627304962));
#31703=CARTESIAN_POINT('Ctrl Pts',(367.186832386945,-16.0000000000001,0.230508433788787));
#31704=CARTESIAN_POINT('Ctrl Pts',(367.186154279982,-16.0000000000001,0.247170261477932));
#31705=CARTESIAN_POINT('Ctrl Pts',(367.185591387335,-16.0000000000002,0.263831136380812));
#31706=CARTESIAN_POINT('Ctrl Pts',(367.185143961572,-16.0000000000002,0.280486670524623));
#31707=CARTESIAN_POINT('Ctrl Pts',(367.181957809614,-16.0000000000002,0.399091961351293));
#31708=CARTESIAN_POINT('Ctrl Pts',(367.184621052563,-16.0000000000002,0.517476392994406));
#31709=CARTESIAN_POINT('Ctrl Pts',(367.193203833027,-16.0000000000002,0.635211876895126));
#31710=CARTESIAN_POINT('Ctrl Pts',(367.201208598629,-16.0000000000002,0.745018361601917));
#31711=CARTESIAN_POINT('Ctrl Pts',(367.214362617238,-16.0000000000002,0.854261226171659));
#31712=CARTESIAN_POINT('Ctrl Pts',(367.232761268974,-16.0000000000002,0.962606957926316));
#31713=CARTESIAN_POINT('Ctrl Pts',(367.25195269881,-16.0000000000001,1.07562119064931));
#31714=CARTESIAN_POINT('Ctrl Pts',(367.276849595831,-16.0000000000002,1.18766007996308));
#31715=CARTESIAN_POINT('Ctrl Pts',(367.307156117133,-16.0000000000002,1.29845750341952));
#31716=CARTESIAN_POINT('Ctrl Pts',(367.325946168543,-16.0000000000001,1.36715193595241));
#31717=CARTESIAN_POINT('Ctrl Pts',(367.346816757925,-15.9999999999999,1.4353691655699));
#31718=CARTESIAN_POINT('Ctrl Pts',(367.369707204142,-16.0000000000001,1.50304465908003));
#31719=CARTESIAN_POINT('Ctrl Pts',(367.381962978616,-16.0000000000002,1.53927879702795));
#31720=CARTESIAN_POINT('Ctrl Pts',(367.394797896825,-15.9999999999999,1.57535761633311));
#31721=CARTESIAN_POINT('Ctrl Pts',(367.408203471026,-15.9999999999999,1.61127100334885));
#31722=CARTESIAN_POINT('Ctrl Pts',(367.415902678343,-15.9999999999999,1.63189709574459));
#31723=CARTESIAN_POINT('Ctrl Pts',(367.423791800755,-16.0000000000001,1.65247261509346));
#31724=CARTESIAN_POINT('Ctrl Pts',(367.431858608384,-16.0000000000001,1.67296916741837));
#31725=CARTESIAN_POINT('Ctrl Pts',(367.475079373834,-16.0000000000003,1.78278667160836));
#31726=CARTESIAN_POINT('Ctrl Pts',(367.523445625448,-16.0000000000002,1.89047517580507));
#31727=CARTESIAN_POINT('Ctrl Pts',(367.576599392367,-16.0000000000002,1.99576259435056));
#31728=CARTESIAN_POINT('Ctrl Pts',(367.630702043565,-16.0000000000002,2.10292957067731));
#31729=CARTESIAN_POINT('Ctrl Pts',(367.689764924591,-16.0000000000001,2.20760965059624));
#31730=CARTESIAN_POINT('Ctrl Pts',(367.753465513287,-16.0000000000001,2.3095128047873));
#31731=CARTESIAN_POINT('Ctrl Pts',(367.818145691291,-16.0000000000001,2.41298302833227));
#31732=CARTESIAN_POINT('Ctrl Pts',(367.887607634854,-16.,2.5135910393457));
#31733=CARTESIAN_POINT('Ctrl Pts',(367.961565405332,-16.0000000000001,2.61101890964699));
#31734=CARTESIAN_POINT('Ctrl Pts',(368.010750766558,-16.0000000000001,2.67581298014525));
#31735=CARTESIAN_POINT('Ctrl Pts',(368.061925634854,-16.0000000000001,2.73920020650163));
#31736=CARTESIAN_POINT('Ctrl Pts',(368.115017126897,-16.,2.80108101804679));
#31737=CARTESIAN_POINT('Ctrl Pts',(368.133646696693,-16.,2.82279472119189));
#31738=CARTESIAN_POINT('Ctrl Pts',(368.15251233108,-15.9999999999999,2.84432289013815));
#31739=CARTESIAN_POINT('Ctrl Pts',(368.171611117157,-15.9999999999999,2.86566103888692));
#31740=CARTESIAN_POINT('Ctrl Pts',(368.183566345187,-15.9999999999999,2.8790180361859));
#31741=CARTESIAN_POINT('Ctrl Pts',(368.195613352392,-15.9999999999999,2.89230103112425));
#31742=CARTESIAN_POINT('Ctrl Pts',(368.207750166955,-15.9999999999999,2.905507509312));
#31743=CARTESIAN_POINT('Ctrl Pts',(368.292660099036,-15.9999999999999,2.99790087662829));
#31744=CARTESIAN_POINT('Ctrl Pts',(368.381671855022,-16.0000000000001,3.08623599275652));
#31745=CARTESIAN_POINT('Ctrl Pts',(368.47446003312,-16.,3.17018956350407));
#31746=CARTESIAN_POINT('Ctrl Pts',(368.549042802181,-15.9999999999999,3.23767111026241));
#31747=CARTESIAN_POINT('Ctrl Pts',(368.626066579836,-16.0000000000001,3.30232168162783));
#31748=CARTESIAN_POINT('Ctrl Pts',(368.705383680702,-16.,3.36396149445182));
#31749=CARTESIAN_POINT('Ctrl Pts',(368.77143344708,-16.,3.4152908445186));
#31750=CARTESIAN_POINT('Ctrl Pts',(368.839073876932,-15.9999999999999,3.46453229796807));
#31751=CARTESIAN_POINT('Ctrl Pts',(368.908228349274,-15.9999999999999,3.51157426867829));
#31752=CARTESIAN_POINT('Ctrl Pts',(368.924210666199,-15.9999999999999,3.52244615677451));
#31753=CARTESIAN_POINT('Ctrl Pts',(368.940272559512,-15.9999999999999,3.53319957636285));
#31754=CARTESIAN_POINT('Ctrl Pts',(368.956405164286,-15.9999999999999,3.54382808750964));
#31755=CARTESIAN_POINT('Ctrl Pts',(369.061877312563,-16.,3.6133154343693));
#31756=CARTESIAN_POINT('Ctrl Pts',(369.170460486771,-15.9999999999999,3.67752927585838));
#31757=CARTESIAN_POINT('Ctrl Pts',(369.28185839183,-16.,3.73612768018094));
#31758=CARTESIAN_POINT('Ctrl Pts',(369.346334673923,-16.,3.77004400244298));
#31759=CARTESIAN_POINT('Ctrl Pts',(369.411754666887,-16.,3.80207859119799));
#31760=CARTESIAN_POINT('Ctrl Pts',(369.478066585006,-16.,3.83215948081421));
#31761=CARTESIAN_POINT('Ctrl Pts',(369.574591622416,-16.0000000000001,3.87594586308027));
#31762=CARTESIAN_POINT('Ctrl Pts',(369.673005938295,-15.9999999999999,3.91559395689521));
#31763=CARTESIAN_POINT('Ctrl Pts',(369.773056110741,-16.,3.95116298671608));
#31764=CARTESIAN_POINT('Ctrl Pts',(369.776413430251,-11.,3.94563850749837));
#31765=CARTESIAN_POINT('Ctrl Pts',(369.659936027211,-10.9999999999999,3.90363340028023));
#31766=CARTESIAN_POINT('Ctrl Pts',(369.545849642241,-11.,3.85602145237529));
#31767=CARTESIAN_POINT('Ctrl Pts',(369.434387235882,-11.,3.80316525575889));
#31768=CARTESIAN_POINT('Ctrl Pts',(369.32129226132,-11.,3.74953488470336));
#31769=CARTESIAN_POINT('Ctrl Pts',(369.210898085145,-11.0000000000001,3.69050490441186));
#31770=CARTESIAN_POINT('Ctrl Pts',(369.103475688714,-11.,3.6264068078231));
#31771=CARTESIAN_POINT('Ctrl Pts',(368.995626170089,-11.,3.56205385079072));
#31772=CARTESIAN_POINT('Ctrl Pts',(368.890771532536,-11.0000000000001,3.49259169503417));
#31773=CARTESIAN_POINT('Ctrl Pts',(368.789222562421,-11.0000000000001,3.41831855725877));
#31774=CARTESIAN_POINT('Ctrl Pts',(368.69784886467,-11.0000000000001,3.3514876358389));
#31775=CARTESIAN_POINT('Ctrl Pts',(368.609151752929,-11.0000000000001,3.28076071756683));
#31776=CARTESIAN_POINT('Ctrl Pts',(368.523388576094,-11.0000000000001,3.20633646559006));
#31777=CARTESIAN_POINT('Ctrl Pts',(368.503754693478,-11.0000000000001,3.18929841871426));
#31778=CARTESIAN_POINT('Ctrl Pts',(368.484274710755,-11.0000000000001,3.17206653900113));
#31779=CARTESIAN_POINT('Ctrl Pts',(368.46495196076,-11.0000000000001,3.15464311726871));
#31780=CARTESIAN_POINT('Ctrl Pts',(368.451707859823,-11.0000000000001,3.14270084424112));
#31781=CARTESIAN_POINT('Ctrl Pts',(368.43853703285,-11.0000000000001,3.13066795174825));
#31782=CARTESIAN_POINT('Ctrl Pts',(368.425452636208,-11.0000000000001,3.11855657911232));
#31783=CARTESIAN_POINT('Ctrl Pts',(368.334977806957,-11.,3.03480993024135));
#31784=CARTESIAN_POINT('Ctrl Pts',(368.248492784418,-10.9999999999999,2.94718935218984));
#31785=CARTESIAN_POINT('Ctrl Pts',(368.16625722767,-10.9999999999999,2.85600833920122));
#31786=CARTESIAN_POINT('Ctrl Pts',(368.084366229379,-11.,2.76520936520406));
#31787=CARTESIAN_POINT('Ctrl Pts',(368.006688685184,-11.,2.67087899756665));
#31788=CARTESIAN_POINT('Ctrl Pts',(367.933523458788,-11.,2.57329789569913));
#31789=CARTESIAN_POINT('Ctrl Pts',(367.862060559945,-11.,2.47798720296711));
#31790=CARTESIAN_POINT('Ctrl Pts',(367.794902169971,-11.0000000000001,2.37957458681458));
#31791=CARTESIAN_POINT('Ctrl Pts',(367.732372661656,-11.,2.2783045497797));
#31792=CARTESIAN_POINT('Ctrl Pts',(367.681195946289,-10.9999999999999,2.19542099607579));
#31793=CARTESIAN_POINT('Ctrl Pts',(367.633120597113,-11.,2.11062295888144));
#31794=CARTESIAN_POINT('Ctrl Pts',(367.588350198513,-11.0000000000001,2.0240403948292));
#31795=CARTESIAN_POINT('Ctrl Pts',(367.577475074151,-11.0000000000001,2.00300872700656));
#31796=CARTESIAN_POINT('Ctrl Pts',(367.566795071804,-11.,1.98187175637645));
#31797=CARTESIAN_POINT('Ctrl Pts',(367.556313334115,-11.,1.96063133738065));
#31798=CARTESIAN_POINT('Ctrl Pts',(367.548771481207,-11.,1.94534836422111));
#31799=CARTESIAN_POINT('Ctrl Pts',(367.541332121455,-10.9999999999999,1.9300113651976));
#31800=CARTESIAN_POINT('Ctrl Pts',(367.534002940154,-10.9999999999999,1.91463508225276));
#31801=CARTESIAN_POINT('Ctrl Pts',(367.482865177981,-10.9999999999999,1.8073504254668));
#31802=CARTESIAN_POINT('Ctrl Pts',(367.437005313807,-11.0000000000001,1.69799133979778));
#31803=CARTESIAN_POINT('Ctrl Pts',(367.39670398105,-11.0000000000001,1.58682023789595));
#31804=CARTESIAN_POINT('Ctrl Pts',(367.356402648294,-11.0000000000002,1.47564913599412));
#31805=CARTESIAN_POINT('Ctrl Pts',(367.321659401167,-10.9999999999998,1.36266534775552));
#31806=CARTESIAN_POINT('Ctrl Pts',(367.292809505677,-11.,1.24811926023833));
#31807=CARTESIAN_POINT('Ctrl Pts',(367.263881051474,-11.0000000000001,1.13326126194863));
#31808=CARTESIAN_POINT('Ctrl Pts',(367.240878654116,-11.,1.01683139042499));
#31809=CARTESIAN_POINT('Ctrl Pts',(367.223722412658,-11.0000000000001,0.899263114940381));
#31810=CARTESIAN_POINT('Ctrl Pts',(367.214331524928,-11.0000000000001,0.834909248245439));
#31811=CARTESIAN_POINT('Ctrl Pts',(367.206693171909,-11.,0.770214393798156));
#31812=CARTESIAN_POINT('Ctrl Pts',(367.200800614037,-11.0000000000001,0.705251301586698));
#31813=CARTESIAN_POINT('Ctrl Pts',(367.197577909856,-11.0000000000001,0.669722277786365));
#31814=CARTESIAN_POINT('Ctrl Pts',(367.194877469672,-11.,0.634113048489866));
#31815=CARTESIAN_POINT('Ctrl Pts',(367.192698731357,-11.,0.598435759622394));
#31816=CARTESIAN_POINT('Ctrl Pts',(367.191630998276,-10.9999999999999,0.580951410386367));
#31817=CARTESIAN_POINT('Ctrl Pts',(367.190688485058,-11.0000000000002,0.563448935452259));
#31818=CARTESIAN_POINT('Ctrl Pts',(367.189871415751,-11.0000000000002,0.545935383445549));
#31819=CARTESIAN_POINT('Ctrl Pts',(367.184455247748,-11.0000000000001,0.429842000501809));
#31820=CARTESIAN_POINT('Ctrl Pts',(367.184562980828,-11.,0.313635830102158));
#31821=CARTESIAN_POINT('Ctrl Pts',(367.190059552093,-11.,0.197720677411417));
#31822=CARTESIAN_POINT('Ctrl Pts',(367.195570191111,-11.0000000000001,0.0815088550914429));
#31823=CARTESIAN_POINT('Ctrl Pts',(367.206497586919,-11.0000000000002,-0.0344113712345558));
#31824=CARTESIAN_POINT('Ctrl Pts',(367.222757524567,-11.,-0.149624567530818));
#31825=CARTESIAN_POINT('Ctrl Pts',(367.23886744374,-10.9999999999998,-0.263774776481907));
#31826=CARTESIAN_POINT('Ctrl Pts',(367.260212326853,-10.9999999999998,-0.377231769472658));
#31827=CARTESIAN_POINT('Ctrl Pts',(367.286756024338,-11.,-0.489570218199307));
#31828=CARTESIAN_POINT('Ctrl Pts',(367.303418137215,-11.0000000000001,-0.560087745541271));
#31829=CARTESIAN_POINT('Ctrl Pts',(367.322129666626,-11.0000000000001,-0.630164056870382));
#31830=CARTESIAN_POINT('Ctrl Pts',(367.342890066273,-10.9999999999999,-0.699687414794692));
#31831=CARTESIAN_POINT('Ctrl Pts',(367.353981140095,-10.9999999999999,-0.736829700502522));
#31832=CARTESIAN_POINT('Ctrl Pts',(367.365657097148,-10.9999999999998,-0.773814068645216));
#31833=CARTESIAN_POINT('Ctrl Pts',(367.377918561647,-10.9999999999998,-0.810622743611728));
#31834=CARTESIAN_POINT('Ctrl Pts',(367.384026834972,-10.9999999999998,-0.828959659847157));
#31835=CARTESIAN_POINT('Ctrl Pts',(367.390281141698,-10.9999999999999,-0.847254832709461));
#31836=CARTESIAN_POINT('Ctrl Pts',(367.396675594858,-10.9999999999999,-0.865489433129636));
#31837=CARTESIAN_POINT('Ctrl Pts',(367.433931723564,-11.0000000000001,-0.971730045597848));
#31838=CARTESIAN_POINT('Ctrl Pts',(367.475980154013,-10.9999999999999,-1.07603545527335));
#31839=CARTESIAN_POINT('Ctrl Pts',(367.522771858589,-10.9999999999999,-1.17800551424189));
#31840=CARTESIAN_POINT('Ctrl Pts',(367.557827270384,-10.9999999999999,-1.25439944860171));
#31841=CARTESIAN_POINT('Ctrl Pts',(367.595545867583,-10.9999999999998,-1.3294822107516));
#31842=CARTESIAN_POINT('Ctrl Pts',(367.635921634894,-11.,-1.40307299805944));
#31843=CARTESIAN_POINT('Ctrl Pts',(367.656229785332,-11.,-1.44008759565322));
#31844=CARTESIAN_POINT('Ctrl Pts',(367.677210355633,-10.9999999999997,-1.47672455143805));
#31845=CARTESIAN_POINT('Ctrl Pts',(367.698863683305,-10.9999999999999,-1.51295958259568));
#31846=CARTESIAN_POINT('Ctrl Pts',(367.711114888811,-11.0000000000001,-1.53346094940336));
#31847=CARTESIAN_POINT('Ctrl Pts',(367.723581468232,-11.,-1.55383363697344));
#31848=CARTESIAN_POINT('Ctrl Pts',(367.736263582017,-10.9999999999999,-1.57407311170418));
#31849=CARTESIAN_POINT('Ctrl Pts',(367.745854445896,-10.9999999999998,-1.58937923893319));
#31850=CARTESIAN_POINT('Ctrl Pts',(367.755567557301,-10.9999999999999,-1.60460745687454));
#31851=CARTESIAN_POINT('Ctrl Pts',(367.765397959284,-10.9999999999999,-1.6197484253644));
#31852=CARTESIAN_POINT('Ctrl Pts',(367.824091279774,-10.9999999999999,-1.71014897231997));
#31853=CARTESIAN_POINT('Ctrl Pts',(367.887011001249,-10.9999999999998,-1.79751936273579));
#31854=CARTESIAN_POINT('Ctrl Pts',(367.954135881222,-10.9999999999999,-1.88147688145987));
#31855=CARTESIAN_POINT('Ctrl Pts',(367.991442551067,-11.,-1.928138796286));
#31856=CARTESIAN_POINT('Ctrl Pts',(368.030048780959,-10.9999999999999,-1.97374586887409));
#31857=CARTESIAN_POINT('Ctrl Pts',(368.069955304757,-10.9999999999999,-2.0182269070666));
#31858=CARTESIAN_POINT('Ctrl Pts',(368.129331934719,-10.9999999999999,-2.08440992412033));
#31859=CARTESIAN_POINT('Ctrl Pts',(368.191587073976,-10.9999999999998,-2.14810094809532));
#31860=CARTESIAN_POINT('Ctrl Pts',(368.256517833619,-11.,-2.20920453143733));
#31861=CARTESIAN_POINT('Origin',(370.834317853224,-11.,1.11022302462516E-15));
#31862=CARTESIAN_POINT('',(377.834317853224,-11.,4.0414518843274));
#31863=CARTESIAN_POINT('',(377.834317853224,-11.,-4.04145188432739));
#31864=CARTESIAN_POINT('',(377.834317853224,-11.,4.0414518843274));
#31865=CARTESIAN_POINT('',(370.834317853224,-11.,-8.08290376865479));
#31866=CARTESIAN_POINT('',(377.834317853224,-11.,-4.04145188432739));
#31867=CARTESIAN_POINT('',(363.834317853224,-11.,-4.0414518843274));
#31868=CARTESIAN_POINT('',(370.834317853224,-11.,-8.08290376865479));
#31869=CARTESIAN_POINT('',(363.834317853224,-11.,4.0414518843274));
#31870=CARTESIAN_POINT('',(363.834317853224,-11.,-4.0414518843274));
#31871=CARTESIAN_POINT('',(370.834317853224,-11.,8.08290376865479));
#31872=CARTESIAN_POINT('',(363.834317853224,-11.,4.0414518843274));
#31873=CARTESIAN_POINT('',(370.834317853224,-11.,8.08290376865479));
#31874=CARTESIAN_POINT('Origin',(370.834317853224,-11.,-8.08290376865479));
#31875=CARTESIAN_POINT('',(377.834317853224,-16.,-4.04145188432739));
#31876=CARTESIAN_POINT('',(377.834317853224,-11.,-4.04145188432739));
#31877=CARTESIAN_POINT('',(370.834317853224,-16.,-8.08290376865479));
#31878=CARTESIAN_POINT('',(377.834317853224,-16.,-4.04145188432739));
#31879=CARTESIAN_POINT('',(370.834317853224,-11.,-8.08290376865479));
#31880=CARTESIAN_POINT('Origin',(363.834317853224,-11.,-4.0414518843274));
#31881=CARTESIAN_POINT('',(363.834317853224,-16.,-4.0414518843274));
#31882=CARTESIAN_POINT('',(370.834317853224,-16.,-8.08290376865479));
#31883=CARTESIAN_POINT('',(363.834317853224,-11.,-4.0414518843274));
#31884=CARTESIAN_POINT('Origin',(363.834317853224,-11.,4.0414518843274));
#31885=CARTESIAN_POINT('',(363.834317853224,-16.,4.0414518843274));
#31886=CARTESIAN_POINT('',(363.834317853224,-16.,-4.0414518843274));
#31887=CARTESIAN_POINT('',(363.834317853224,-11.,4.0414518843274));
#31888=CARTESIAN_POINT('Origin',(370.834317853224,-11.,8.08290376865479));
#31889=CARTESIAN_POINT('',(370.834317853224,-16.,8.08290376865479));
#31890=CARTESIAN_POINT('',(363.834317853224,-16.,4.0414518843274));
#31891=CARTESIAN_POINT('',(370.834317853224,-11.,8.08290376865479));
#31892=CARTESIAN_POINT('Origin',(377.834317853224,-11.,4.0414518843274));
#31893=CARTESIAN_POINT('',(377.834317853224,-16.,4.0414518843274));
#31894=CARTESIAN_POINT('',(370.834317853224,-16.,8.08290376865479));
#31895=CARTESIAN_POINT('',(377.834317853224,-11.,4.0414518843274));
#31896=CARTESIAN_POINT('Origin',(377.834317853224,-11.,-4.04145188432739));
#31897=CARTESIAN_POINT('',(377.834317853224,-16.,4.0414518843274));
#31898=CARTESIAN_POINT('Origin',(370.834317853224,-16.,1.11022302462516E-15));
#51539=UNCERTAINTY_MEASURE_WITH_UNIT(LENGTH_MEASURE(0.01),#51554,
'DISTANCE_ACCURACY_VALUE',
'Maximum model space distance between geometric entities at asserted c
onnectivities');
#51543=UNCERTAINTY_MEASURE_WITH_UNIT(LENGTH_MEASURE(0.01),#51554,
'DISTANCE_ACCURACY_VALUE',
'Maximum model space distance between geometric entities at asserted c
onnectivities');
#51549=(
GEOMETRIC_REPRESENTATION_CONTEXT(3)
GLOBAL_UNCERTAINTY_ASSIGNED_CONTEXT((#51539))
GLOBAL_UNIT_ASSIGNED_CONTEXT((#51554,#51556,#51557))
REPRESENTATION_CONTEXT('','3D')
);
#51553=(
GEOMETRIC_REPRESENTATION_CONTEXT(3)
GLOBAL_UNCERTAINTY_ASSIGNED_CONTEXT((#51543))
GLOBAL_UNIT_ASSIGNED_CONTEXT((#51554,#51556,#51557))
REPRESENTATION_CONTEXT('','3D')
);
#51554=(
LENGTH_UNIT()
NAMED_UNIT(*)
SI_UNIT(.MILLI.,.METRE.)
);
#51556=(
NAMED_UNIT(*)
PLANE_ANGLE_UNIT()
SI_UNIT($,.RADIAN.)
);
#51557=(
NAMED_UNIT(*)
SI_UNIT($,.STERADIAN.)
SOLID_ANGLE_UNIT()
);
#51563=SHAPE_DEFINITION_REPRESENTATION(#51572,#51589);
#51572=PRODUCT_DEFINITION_SHAPE('',$,#51599);
#51589=SHAPE_REPRESENTATION('',(#4507),#51549);
#51593=PRODUCT_DEFINITION_CONTEXT('part definition',#51622,'design');
#51599=PRODUCT_DEFINITION('Nut_01','Nut_01',#51608,#51593);
#51608=PRODUCT_DEFINITION_FORMATION('',$,#51629);
#51622=APPLICATION_CONTEXT(
'Core Data for Automotive Mechanical Design Process');
#51623=PRODUCT_CONTEXT('part definition',#51622,'mechanical');
#51629=PRODUCT('Nut_01','Nut_01',$,(#51623));
#51634=PRESENTATION_STYLE_ASSIGNMENT((#51637));
#51637=SURFACE_STYLE_USAGE(.BOTH.,#51640);
#51640=SURFACE_SIDE_STYLE('',(#51643));
#51643=SURFACE_STYLE_FILL_AREA(#51646);
#51646=FILL_AREA_STYLE('Opaque(203,203,203)',(#51649));
#51649=FILL_AREA_STYLE_COLOUR('Opaque(203,203,203)',#51652);
#51652=COLOUR_RGB('Opaque(203,203,203)', 0.09019608, 0.27058824, 0.51372549);
ENDSEC;
END-ISO-10303-21;
